ISO-10303-21;
HEADER;
FILE_DESCRIPTION (('STEP AP214'),
    '1' );
FILE_NAME ('Adjuster Locknut.step',
    '2026-10-30T09:41:00',
    ( '' ),
    ( '' ),
    'SwSTEP 2.0',
    'SolidWorks 2020',
    '' );
FILE_SCHEMA (( 'AUTOMOTIVE_DESIGN' ));
ENDSEC;

DATA;
#18=CARTESIAN_POINT ( 'NONE',  ( 123.0077516859119839, -9.665098340737509730, -17.37397104707595474 ) ) ;
#40=EDGE_LOOP ( 'NONE', ( #5265, #23177, #27838, #18578 ) ) ;
#59=AXIS2_PLACEMENT_3D ( 'NONE', #1011, #14251, #21539 ) ;
#69=CARTESIAN_POINT ( 'NONE',  ( 121.4103298109119748, -7.200787124940443817, -17.81845355600750835 ) ) ;
#70=CARTESIAN_POINT ( 'NONE',  ( 124.5059548109119731, -5.999156839134619723, -18.26265215102738892 ) ) ;
#80=CARTESIAN_POINT ( 'NONE',  ( 123.7717360609119623, -3.387241619883791355, -18.17469012370385073 ) ) ;
#95=CARTESIAN_POINT ( 'NONE',  ( 119.7434548109119703, -3.132014511563818271, -18.68827187929387179 ) ) ;
#111=AXIS2_PLACEMENT_3D ( 'NONE', #10058, #13020, #24396 ) ;
#118=FACE_OUTER_BOUND ( 'NONE', #4304, .T. ) ;
#136=DIRECTION ( 'NONE',  ( 0.000000000000000000, -0.4669533266896233603, -0.8842819633428546933 ) ) ;
#159=CARTESIAN_POINT ( 'NONE',  ( 122.9382985609119743, -10.36940331770106916, -15.09355782777062061 ) ) ;
#180=CARTESIAN_POINT ( 'NONE',  ( 121.2019704359119743, 1.345710702986147034, -13.97328579221134426 ) ) ;
#187=CARTESIAN_POINT ( 'NONE',  ( 124.5059548109119731, -9.675232987814487373, -12.03232374619203249 ) ) ;
#196=CARTESIAN_POINT ( 'NONE',  ( 123.5633766859119760, -0.06289925094097943703, -9.412459353600674206 ) ) ;
#200=ORIENTED_EDGE ( 'NONE', *, *, #27729, .T. ) ;
#210=CARTESIAN_POINT ( 'NONE',  ( 120.2510376736034345, -8.245233026025740486, -17.07659070123625611 ) ) ;
#274=CARTESIAN_POINT ( 'NONE',  ( 119.9518141859119851, -8.321307733199551748, -9.223433127585318303 ) ) ;
#298=EDGE_LOOP ( 'NONE', ( #6324, #200, #13819, #23872, #43619, #8175, #10670, #40408, #38496, #9642, #19801, #11801, #12135, #8822, #43173 ) ) ;
#303=CARTESIAN_POINT ( 'NONE',  ( 123.7717360609119623, -6.564341423271550902, -7.887810678476487425 ) ) ;
#319=ORIENTED_EDGE ( 'NONE', *, *, #19756, .T. ) ;
#368=ADVANCED_FACE ( 'NONE', ( #7092 ), #38148, .T. ) ;
#385=CARTESIAN_POINT ( 'NONE',  ( 120.0212673109119805, 0.2312338769422704887, -16.08380026872395874 ) ) ;
#418=CARTESIAN_POINT ( 'NONE',  ( 124.7442371152574054, -12.24640110593768227, -10.93193462351065470 ) ) ;
#420=CARTESIAN_POINT ( 'NONE',  ( 122.3132204359119868, 1.345710702986147034, -13.97328579221134426 ) ) ;
#441=ORIENTED_EDGE ( 'NONE', *, *, #35642, .T. ) ;
#457=ORIENTED_EDGE ( 'NONE', *, *, #36836, .F. ) ;
#463=ORIENTED_EDGE ( 'NONE', *, *, #12759, .F. ) ;
#505=AXIS2_PLACEMENT_3D ( 'NONE', #40612, #43354, #19626 ) ;
#528=CARTESIAN_POINT ( 'NONE',  ( 123.8411891859119862, -8.844754642576884152, -8.592115655440050404 ) ) ;
#539=EDGE_LOOP ( 'NONE', ( #15498, #3012, #28270, #31753 ) ) ;
#557=CARTESIAN_POINT ( 'NONE',  ( 119.7434548109119703, -4.863998795839242995, -13.39321520033831447 ) ) ;
#568=ORIENTED_EDGE ( 'NONE', *, *, #1973, .T. ) ;
#610=CARTESIAN_POINT ( 'NONE',  ( 121.9659548109119811, -7.554583864224885481, -18.48844787311982785 ) ) ;
#627=CARTESIAN_POINT ( 'NONE',  ( 123.6792205938796485, -6.000230167480150811, -18.26468474152937205 ) ) ;
#630=CARTESIAN_POINT ( 'NONE',  ( 123.4939235609119663, 0.6414057260225851653, -11.69287257290600657 ) ) ;
#641=CARTESIAN_POINT ( 'NONE',  ( 125.2183010572641422, -10.90914942692569589, -9.272323934217878261 ) ) ;
#653=ADVANCED_FACE ( 'NONE', ( #22123 ), #35789, .F. ) ;
#660=CARTESIAN_POINT ( 'NONE',  ( 120.6463454359119822, -11.07370829466463569, -12.81314460846529002 ) ) ;
#685=DIRECTION ( 'NONE',  ( -1.000000000000000000, 0.000000000000000000, -0.000000000000000000 ) ) ;
#688=DIRECTION ( 'NONE',  ( -1.000000000000000000, 0.000000000000000000, -0.000000000000000000 ) ) ;
#690=CARTESIAN_POINT ( 'NONE',  ( 122.5664060953690466, -6.001247023715324147, -18.26661038929047010 ) ) ;
#696=DIRECTION ( 'NONE',  ( 0.000000000000000000, -0.4669533266896290225, -0.8842819633428516957 ) ) ;
#726=CARTESIAN_POINT ( 'NONE',  ( 122.3826735609119680, -9.645473719204776586, -14.86997237629376656 ) ) ;
#739=CARTESIAN_POINT ( 'NONE',  ( 124.5602934112120721, -9.863183861322463386, -13.54995704067371598 ) ) ;
#741=CARTESIAN_POINT ( 'NONE',  ( 121.4797829359119987, -4.283928203966213211, -7.183505701512925334 ) ) ;
#744=CARTESIAN_POINT ( 'NONE',  ( 125.1433143116118032, -2.283722140743223328, -6.422401579036027819 ) ) ;
#752=CARTESIAN_POINT ( 'NONE',  ( 119.7434548109119419, -2.229855236528029305, -9.108032788432828042 ) ) ;
#768=EDGE_LOOP ( 'NONE', ( #33338, #27679, #441, #42888 ) ) ;
#829=CARTESIAN_POINT ( 'NONE',  ( 123.5633766859119760, -0.06289925094097943703, -9.412459353600674206 ) ) ;
#847=CARTESIAN_POINT ( 'NONE',  ( 122.1743141859119817, -0.8832429491016019485, -18.19431474523657855 ) ) ;
#852=CARTESIAN_POINT ( 'NONE',  ( 123.6328298109119714, -2.173413727453600508, -8.297982527556802879 ) ) ;
#866=CARTESIAN_POINT ( 'NONE',  ( 124.1726284085844298, -11.17717881402670699, -8.479713305622000874 ) ) ;
#884=CARTESIAN_POINT ( 'NONE',  ( 119.8129079359119942, -5.444069387712269226, -19.60292469916370450 ) ) ;
#885=PLANE ( 'NONE',  #8115 ) ;
#946=CIRCLE ( 'NONE', #26438, 8.000000000000001776 ) ;
#956=UNCERTAINTY_MEASURE_WITH_UNIT (LENGTH_MEASURE( 1.000000000000000082E-05 ), #5660, 'distance_accuracy_value', 'NONE');
#960=CARTESIAN_POINT ( 'NONE',  ( 120.0212673109119805, 0.2312338769422704887, -16.08380026872395874 ) ) ;
#961=CIRCLE ( 'NONE', #4601, 8.000000000000001776 ) ;
#975=CARTESIAN_POINT ( 'NONE',  ( 121.6881423109119709, -9.959231468620755479, -10.70263013195267199 ) ) ;
#979=CARTESIAN_POINT ( 'NONE',  ( 124.6565730087411765, -2.409824777551811792, -5.955873678245978908 ) ) ;
#1011=CARTESIAN_POINT ( 'NONE',  ( 125.4584548109119737, -4.863998795839242995, -13.39321520033831447 ) ) ;
#1055=CARTESIAN_POINT ( 'NONE',  ( 123.2161110609119561, -3.163656168406935087, -18.89861972220014508 ) ) ;
#1077=CARTESIAN_POINT ( 'NONE',  ( 122.9382985609119743, -10.36940331770106916, -15.09355782777062061 ) ) ;
#1078=CARTESIAN_POINT ( 'NONE',  ( 123.6808719482204992, -5.999156839134923480, -18.26265215102791117 ) ) ;
#1080=CARTESIAN_POINT ( 'NONE',  ( 121.9659548109119811, -7.554583864224885481, -18.48844787311982785 ) ) ;
#1087=CARTESIAN_POINT ( 'NONE',  ( 125.4584548109119737, -4.863998795839242995, -13.39321520033831447 ) ) ;
#1106=CARTESIAN_POINT ( 'NONE',  ( 120.4379860609119675, -6.564341423271550902, -7.887810678476487425 ) ) ;
#1122=( BOUNDED_CURVE ( )  B_SPLINE_CURVE ( 2, ( #19826, #23016, #26445, #40580, #5905, #5451, #44003, #36681, #2485 ),
 .UNSPECIFIED., .F., .T. ) 
 B_SPLINE_CURVE_WITH_KNOTS ( ( 3, 2, 2, 2, 3 ),
 ( 0.5030750193655029179, 0.6250000000000000000, 0.7500000000000000000, 0.8750000000000000000, 0.9588811029394139762 ),
 .UNSPECIFIED. ) 
 CURVE ( )  GEOMETRIC_REPRESENTATION_ITEM ( )  RATIONAL_B_SPLINE_CURVE ( ( 0.9963469806984119881, 0.9257521078043979834, 1.000000000000000000, 0.9238795325112869605, 1.000000000000000000, 0.9238795325112869605, 1.000000000000000000, 0.9489194498462629745, 0.9663939858628869395 ) ) 
 REPRESENTATION_ITEM ( '' )  );
#1136=ORIENTED_EDGE ( 'NONE', *, *, #40982, .F. ) ;
#1152=EDGE_CURVE ( 'NONE', #10924, #15883, #40363, .T. ) ;
#1167=CARTESIAN_POINT ( 'NONE',  ( 119.7563403099118773, -6.348382822066793274, -18.92399070498282754 ) ) ;
#1186=CARTESIAN_POINT ( 'NONE',  ( 120.9241579359119925, -5.444069387712269226, -19.60292469916370450 ) ) ;
#1201=CARTESIAN_POINT ( 'NONE',  ( 121.9659548109119811, -7.554583864224885481, -18.48844787311982785 ) ) ;
#1249=CARTESIAN_POINT ( 'NONE',  ( 125.0849378844206257, -6.072675180497891567, -6.000667556518594736 ) ) ;
#1271=CARTESIAN_POINT ( 'NONE',  ( 119.7434548109119703, -5.853704621469987934, -5.454671103420249523 ) ) ;
#1282=CARTESIAN_POINT ( 'NONE',  ( 123.1466579359119891, -5.444069387712269226, -19.60292469916370450 ) ) ;
#1302=DIRECTION ( 'NONE',  ( 0.000000000000000000, 0.4669533266896290780, 0.8842819633428518067 ) ) ;
#1304=CARTESIAN_POINT ( 'NONE',  ( 120.7852516859119731, -0.6942167230862511529, -9.935906262978006609 ) ) ;
#1312=CARTESIAN_POINT ( 'NONE',  ( 124.5198337258228918, -9.766803879443250125, -12.40978687061016572 ) ) ;
#1329=CARTESIAN_POINT ( 'NONE',  ( 120.2296266859119669, -0.06289925094097945091, -9.412459353600674206 ) ) ;
#1334=CARTESIAN_POINT ( 'NONE',  ( 123.5633766859119760, -0.06289925094097943703, -9.412459353600674206 ) ) ;
#1386=CARTESIAN_POINT ( 'NONE',  ( 120.1511205389825250, -6.126425863531494542, -18.50366489541501380 ) ) ;
#1387=( BOUNDED_SURFACE ( )  B_SPLINE_SURFACE ( 1, 2, ( 
 ( #25518, #884, #11607, #39421, #17994, #43067, #18455, #15247, #18222, #31893, #11835, #7954, #38727, #660, #28492, #7499, #35298, #8412, #14803, #32782, #8186, #35982, #4753, #4300, #32116, #1554, #15476, #25294, #18674, #29382, #11386, #19120, #23224, #22757, #39871, #43975, #8636, #36434, #33004, #2459, #26188, #25966, #12290, #33913, #40097, #8856, #33684, #33234, #2229, #22537, #9315, #36657, #9540, #1778, #23455, #16381, #43522, #5430, #43749, #19570, #26641, #5201, #15704, #20031, #44429 ),
 ( #37103, #12971, #19347, #37340, #5878, #2007, #30508, #26414, #26867, #16158, #15933, #5650, #29832, #29606, #12516, #40324, #9088, #40555, #22990, #33449, #36880, #12739, #30062, #19799, #30283, #44209, #40782, #6112, #2684, #16615, #37574, #7017, #13642, #17724, #20259, #34145, #13197, #31623, #3586, #20487, #41904, #34586, #27772, #27551, #6344, #41019, #31396, #24572, #44885, #10222, #20708, #41463, #2914, #10446, #10003, #27097, #31180, #9773, #23685, #16845, #34802, #13423, #30737, #44660, #21142 ) ),
 .UNSPECIFIED., .F., .F., .T. ) 
 B_SPLINE_SURFACE_WITH_KNOTS ( ( 2, 2 ),
 ( 3, 2, 2, 2, 2, 2, 2, 2, 2, 2, 2, 2, 2, 2, 2, 2, 2, 2, 2, 2, 2, 2, 2, 2, 2, 2, 2, 2, 2, 2, 2, 2, 3 ),
 ( 0.000000000000000000, 1.000000000000000000 ),
 ( 0.000000000000000000, 0.03125000000000000000, 0.06250000000000000000, 0.09375000000000000000, 0.1250000000000000000, 0.1562500000000000000, 0.1875000000000000000, 0.2187500000000000000, 0.2500000000000000000, 0.2812500000000000000, 0.3125000000000000000, 0.3437500000000000000, 0.3750000000000000000, 0.4062500000000000000, 0.4375000000000000000, 0.4687500000000000000, 0.5000000000000000000, 0.5312500000000000000, 0.5625000000000000000, 0.5937500000000000000, 0.6250000000000000000, 0.6562500000000000000, 0.6875000000000000000, 0.7187500000000000000, 0.7500000000000000000, 0.7812500000000000000, 0.8125000000000000000, 0.8437500000000000000, 0.8750000000000000000, 0.9062500000000000000, 0.9375000000000000000, 0.9687500000000000000, 1.000000000000000000 ),
 .UNSPECIFIED. ) 
 GEOMETRIC_REPRESENTATION_ITEM ( )  RATIONAL_B_SPLINE_SURFACE ( (
 ( 1.000000000000000000, 0.9238795325112869605, 1.000000000000000000, 0.9238795325112869605, 1.000000000000000000, 0.9238795325112869605, 1.000000000000000000, 0.9238795325112869605, 1.000000000000000000, 0.9238795325112869605, 1.000000000000000000, 0.9238795325112869605, 1.000000000000000000, 0.9238795325112869605, 1.000000000000000000, 0.9238795325112869605, 1.000000000000000000, 0.9238795325112869605, 1.000000000000000000, 0.9238795325112869605, 1.000000000000000000, 0.9238795325112869605, 1.000000000000000000, 0.9238795325112869605, 1.000000000000000000, 0.9238795325112869605, 1.000000000000000000, 0.9238795325112869605, 1.000000000000000000, 0.9238795325112869605, 1.000000000000000000, 0.9238795325112869605, 1.000000000000000000, 0.9238795325112869605, 1.000000000000000000, 0.9238795325112869605, 1.000000000000000000, 0.9238795325112869605, 1.000000000000000000, 0.9238795325112869605, 1.000000000000000000, 0.9238795325112869605, 1.000000000000000000, 0.9238795325112869605, 1.000000000000000000, 0.9238795325112869605, 1.000000000000000000, 0.9238795325112869605, 1.000000000000000000, 0.9238795325112869605, 1.000000000000000000, 0.9238795325112869605, 1.000000000000000000, 0.9238795325112869605, 1.000000000000000000, 0.9238795325112869605, 1.000000000000000000, 0.9238795325112869605, 1.000000000000000000, 0.9238795325112869605, 1.000000000000000000, 0.9238795325112869605, 1.000000000000000000, 0.9238795325112869605, 1.000000000000000000),
 ( 1.000000000000000000, 0.9238795325112869605, 1.000000000000000000, 0.9238795325112869605, 1.000000000000000000, 0.9238795325112869605, 1.000000000000000000, 0.9238795325112869605, 1.000000000000000000, 0.9238795325112869605, 1.000000000000000000, 0.9238795325112869605, 1.000000000000000000, 0.9238795325112869605, 1.000000000000000000, 0.9238795325112869605, 1.000000000000000000, 0.9238795325112869605, 1.000000000000000000, 0.9238795325112869605, 1.000000000000000000, 0.9238795325112869605, 1.000000000000000000, 0.9238795325112869605, 1.000000000000000000, 0.9238795325112869605, 1.000000000000000000, 0.9238795325112869605, 1.000000000000000000, 0.9238795325112869605, 1.000000000000000000, 0.9238795325112869605, 1.000000000000000000, 0.9238795325112869605, 1.000000000000000000, 0.9238795325112869605, 1.000000000000000000, 0.9238795325112869605, 1.000000000000000000, 0.9238795325112869605, 1.000000000000000000, 0.9238795325112869605, 1.000000000000000000, 0.9238795325112869605, 1.000000000000000000, 0.9238795325112869605, 1.000000000000000000, 0.9238795325112869605, 1.000000000000000000, 0.9238795325112869605, 1.000000000000000000, 0.9238795325112869605, 1.000000000000000000, 0.9238795325112869605, 1.000000000000000000, 0.9238795325112869605, 1.000000000000000000, 0.9238795325112869605, 1.000000000000000000, 0.9238795325112869605, 1.000000000000000000, 0.9238795325112869605, 1.000000000000000000, 0.9238795325112869605, 1.000000000000000000) ) ) 
 REPRESENTATION_ITEM ( '' )  SURFACE ( )  );
#1402=CARTESIAN_POINT ( 'NONE',  ( 123.7022829359119811, -5.367793381288652910, -18.78638297431638904 ) ) ;
#1411=VERTEX_POINT ( 'NONE', #42600 ) ;
#1412=VERTEX_POINT ( 'NONE', #25272 ) ;
#1451=AXIS2_PLACEMENT_3D ( 'NONE', #41210, #27296, #19768 ) ;
#1471=CARTESIAN_POINT ( 'NONE',  ( 123.1466579359119891, -4.360204210389833968, -8.000047426360245240 ) ) ;
#1472=AXIS2_PLACEMENT_3D ( 'NONE', #16927, #34007, #3226 ) ;
#1482=CARTESIAN_POINT ( 'NONE',  ( 122.6213246589382209, -8.341213398351550623, -17.25835129106723542 ) ) ;
#1500=EDGE_CURVE ( 'NONE', #13929, #30417, #29624, .T. ) ;
#1501=CARTESIAN_POINT ( 'NONE',  ( 119.8823610609119754, -6.340755971794695078, -8.611740276972781771 ) ) ;
#1521=CARTESIAN_POINT ( 'NONE',  ( 123.6786990974279945, -6.000569120582374794, -18.26532662605526269 ) ) ;
#1523=CARTESIAN_POINT ( 'NONE',  ( 122.5910329359119970, -4.283928203966213211, -7.183505701512925334 ) ) ;
#1536=CARTESIAN_POINT ( 'NONE',  ( 124.0393428911674505, -11.97802596815495590, -17.05247829970954143 ) ) ;
#1544=ORIENTED_EDGE ( 'NONE', *, *, #25156, .F. ) ;
#1554=CARTESIAN_POINT ( 'NONE',  ( 121.4797829359119987, -4.283928203966213211, -7.183505701512925334 ) ) ;
#1555=CARTESIAN_POINT ( 'NONE',  ( 123.4244704359119709, 1.345710702986147034, -13.97328579221134426 ) ) ;
#1586=CARTESIAN_POINT ( 'NONE',  ( 125.3439553448850461, -2.495517763063633598, -20.06068668164824231 ) ) ;
#1589=CARTESIAN_POINT ( 'NONE',  ( 119.7821199480702603, -6.365377317481695663, -18.95617363400926081 ) ) ;
#1623=CARTESIAN_POINT ( 'NONE',  ( 119.9518141859119851, -0.8832429491016019485, -18.19431474523657855 ) ) ;
#1646=B_SPLINE_CURVE_WITH_KNOTS ( 'NONE', 3,
 ( #21398, #25274, #21846, #22077, #25046, #17753, #418, #15008, #39171, #7935, #4052, #35741, #32327, #28921, #3614, #11590, #42829, #17530, #31876, #35510, #31427, #641, #14556, #28474, #24818, #41934, #38483, #7258, #42157, #4282, #14334, #35049, #32098, #3833, #866, #14785 ),
 .UNSPECIFIED., .F., .F.,
 ( 4, 2, 2, 2, 2, 1, 2, 2, 2, 2, 2, 2, 2, 1, 2, 2, 2, 2, 4 ),
 ( 0.000000000000000000, 0.06250000000005807854, 0.1250000000001161571, 0.1875000000001742495, 0.2187500000002066125, 0.2343750000002195188, 0.2421875000002254585, 0.2500000000002314260, 0.3750000000001816325, 0.5000000000001318945, 0.6250000000000820455, 0.6875000000000570655, 0.7187500000000491829, 0.7343750000000451861, 0.7421875000000479616, 0.7500000000000507372, 0.8125000000000400791, 0.8750000000000293099, 1.000000000000000000 ),
 .UNSPECIFIED. ) ;
#1653=CIRCLE ( 'NONE', #29338, 8.000000000000001776 ) ;
#1689=CARTESIAN_POINT ( 'NONE',  ( 125.1375072647497291, -6.121180527655630144, -6.072778184783654609 ) ) ;
#1692=CARTESIAN_POINT ( 'NONE',  ( 120.3685329359119862, -5.367793381288652910, -18.78638297431638904 ) ) ;
#1731=CARTESIAN_POINT ( 'NONE',  ( 124.4356136130535333, -8.422568683347400054, -17.41241596312869788 ) ) ;
#1754=CARTESIAN_POINT ( 'NONE',  ( 124.5165996254432201, -9.747892374099686563, -12.32126250935987954 ) ) ;
#1758=CARTESIAN_POINT ( 'NONE',  ( 125.2824180292811604, -11.90974677766837075, -14.90133849250740816 ) ) ;
#1774=CARTESIAN_POINT ( 'NONE',  ( 120.5074391859119913, -8.844754642576884152, -8.592115655440052180 ) ) ;
#1778=CARTESIAN_POINT ( 'NONE',  ( 123.4244704359119709, 1.345710702986147034, -13.97328579221134426 ) ) ;
#1779=CARTESIAN_POINT ( 'NONE',  ( 121.2714235609119697, 0.6414057260225851653, -11.69287257290600657 ) ) ;
#1810=CARTESIAN_POINT ( 'NONE',  ( 121.3587993874819944, -6.063848558940142297, -18.38516058545102183 ) ) ;
#1826=CARTESIAN_POINT ( 'NONE',  ( 123.7717360609119623, -3.387241619883791355, -18.17469012370385073 ) ) ;
#1844=CARTESIAN_POINT ( 'NONE',  ( 121.8270485609119760, -10.36940331770106916, -15.09355782777062061 ) ) ;
#1918=CARTESIAN_POINT ( 'NONE',  ( 122.7993923109119692, -0.4387604401700512802, -15.73000352943951619 ) ) ;
#1944=CARTESIAN_POINT ( 'NONE',  ( 125.1589444732352234, 1.195138823160687869, -17.64039077345892181 ) ) ;
#1971=CARTESIAN_POINT ( 'NONE',  ( 119.7434548109119703, -4.863998795839242995, -13.39321520033831447 ) ) ;
#1973=EDGE_CURVE ( 'NONE', #45054, #24842, #32375, .T. ) ;
#1975=CARTESIAN_POINT ( 'NONE',  ( 121.4103298109119748, -7.200787124940443817, -17.81845355600750835 ) ) ;
#1982=DIRECTION ( 'NONE',  ( 1.000000000000000000, 0.000000000000000000, 0.000000000000000000 ) ) ;
#1986=CARTESIAN_POINT ( 'NONE',  ( 125.2442149668909224, -11.55290408709314320, -16.24813457787868032 ) ) ;
#2007=CARTESIAN_POINT ( 'NONE',  ( 119.5350954359119839, 0.5291689781388270175, -13.89700978578772705 ) ) ;
#2008=CARTESIAN_POINT ( 'NONE',  ( 122.6604860609119640, -6.564341423271550902, -7.887810678476487425 ) ) ;
#2033=CARTESIAN_POINT ( 'NONE',  ( 124.3431925510704303, -1.240377469759584628, -20.47314632408184920 ) ) ;
#2038=CARTESIAN_POINT ( 'NONE',  ( 125.3463361817452579, -3.037870719615010540, -20.22337043927895550 ) ) ;
#2043=CARTESIAN_POINT ( 'NONE',  ( 121.4797829359119987, -5.367793381288652910, -18.78638297431638904 ) ) ;
#2075=CARTESIAN_POINT ( 'NONE',  ( 122.5215798109119874, -2.173413727453600508, -8.297982527556802879 ) ) ;
#2079=CARTESIAN_POINT ( 'NONE',  ( 124.3273610609119686, -6.340755971794695078, -8.611740276972781771 ) ) ;
#2135=CARTESIAN_POINT ( 'NONE',  ( 120.6463454359119822, 0.5291689781388270175, -13.89700978578772705 ) ) ;
#2139=CARTESIAN_POINT ( 'NONE',  ( 123.4939235609119663, -9.645473719204776586, -14.86997237629376656 ) ) ;
#2149=DIRECTION ( 'NONE',  ( 0.000000000000000000, 0.2950959089608259922, -0.9554676365605399013 ) ) ;
#2162=CARTESIAN_POINT ( 'NONE',  ( 125.3296504289671844, 1.640368036495027715, -16.28920770532023710 ) ) ;
#2166=DIRECTION ( 'NONE',  ( 1.000000000000000000, 0.000000000000000000, 0.000000000000000000 ) ) ;
#2196=CARTESIAN_POINT ( 'NONE',  ( 121.8965016859119856, -0.6942167230862511529, -9.935906262978006609 ) ) ;
#2206=CARTESIAN_POINT ( 'NONE',  ( 125.3421052277123096, -11.71169103848138526, -15.18956764462613584 ) ) ;
#2207=FACE_OUTER_BOUND ( 'NONE', #20726, .T. ) ;
#2209=CARTESIAN_POINT ( 'NONE',  ( 119.7434548109119419, -0.7786512460255691215, -16.99959486913572704 ) ) ;
#2229=CARTESIAN_POINT ( 'NONE',  ( 123.0772048109119652, -7.554583864224885481, -18.48844787311982785 ) ) ;
#2230=CARTESIAN_POINT ( 'NONE',  ( 122.1048610609119720, -3.163656168406935087, -18.89861972220014508 ) ) ;
#2256=DIRECTION ( 'NONE',  ( 1.000000000000000000, 0.000000000000000000, 0.000000000000000000 ) ) ;
#2266=CARTESIAN_POINT ( 'NONE',  ( 121.6186891859119896, -1.406689858478933353, -17.56299727309130887 ) ) ;
#2279=EDGE_LOOP ( 'NONE', ( #24807, #42920, #8491, #13924 ) ) ;
#2280=CARTESIAN_POINT ( 'NONE',  ( 124.7221293297047851, -9.583721038254804370, -19.61132113298129553 ) ) ;
#2289=ORIENTED_EDGE ( 'NONE', *, *, #1500, .F. ) ;
#2305=CARTESIAN_POINT ( 'NONE',  ( 120.9936110609119737, -6.340755971794695078, -8.611740276972781771 ) ) ;
#2328=CYLINDRICAL_SURFACE ( 'NONE', #20561, 8.000000000000001776 ) ;
#2341=CARTESIAN_POINT ( 'NONE',  ( 125.4584548109119737, -8.702576499751430106, -17.94267422983053706 ) ) ;
#2342=CARTESIAN_POINT ( 'NONE',  ( 121.6881423109119709, -0.4387604401700512802, -15.73000352943951619 ) ) ;
#2362=DIRECTION ( 'NONE',  ( 0.000000000000000000, 0.4669533266896289669, 0.8842819633428518067 ) ) ;
#2393=CARTESIAN_POINT ( 'NONE',  ( 124.9801526047702538, 2.307970676211291483, -15.90402515948385265 ) ) ;
#2424=CARTESIAN_POINT ( 'NONE',  ( 123.3550173109119612, -9.289237151508434209, -11.05642687123711276 ) ) ;
#2429=CARTESIAN_POINT ( 'NONE',  ( 122.8688454359119646, -11.07370829466463391, -12.81314460846528469 ) ) ;
#2432=CARTESIAN_POINT ( 'NONE',  ( 121.7575954359119521, -11.07370829466463569, -12.81314460846529002 ) ) ;
#2439=CARTESIAN_POINT ( 'NONE',  ( 119.7434548109119703, 0.2385497399887595849, -14.97457365435098886 ) ) ;
#2459=CARTESIAN_POINT ( 'NONE',  ( 122.4521266859119635, -0.06289925094097943703, -9.412459353600674206 ) ) ;
#2460=CARTESIAN_POINT ( 'NONE',  ( 119.1878298109119783, -7.200787124940443817, -17.81845355600750835 ) ) ;
#2476=ORIENTED_EDGE ( 'NONE', *, *, #22496, .T. ) ;
#2480=EDGE_CURVE ( 'NONE', #17949, #13081, #30990, .T. ) ;
#2485=CARTESIAN_POINT ( 'NONE',  ( 120.2510376736034345, -8.245233026025740486, -17.07659070123625256 ) ) ;
#2491=CARTESIAN_POINT ( 'NONE',  ( 125.3245149615581653, -2.345172624729188193, -20.05245885555360630 ) ) ;
#2494=CARTESIAN_POINT ( 'NONE',  ( 123.1466579359119891, -4.360204210389833968, -8.000047426360245240 ) ) ;
#2513=CARTESIAN_POINT ( 'NONE',  ( 123.1676081739442878, -4.756192495830094735, -19.39047411591439740 ) ) ;
#2517=VERTEX_POINT ( 'NONE', #9923 ) ;
#2526=VERTEX_POINT ( 'NONE', #6721 ) ;
#2532=CARTESIAN_POINT ( 'NONE',  ( 122.1048610609119720, -6.340755971794695078, -8.611740276972781771 ) ) ;
#2582=VERTEX_POINT ( 'NONE', #1589 ) ;
#2596=CARTESIAN_POINT ( 'NONE',  ( 121.8965016859119856, -0.6942167230862511529, -9.935906262978006609 ) ) ;
#2604=VERTEX_POINT ( 'NONE', #43331 ) ;
#2620=LINE ( 'NONE', #6508, #6760 ) ;
#2649=CARTESIAN_POINT ( 'NONE',  ( 123.5633766859119760, -9.033780868592240054, -16.85052413769862056 ) ) ;
#2664=CARTESIAN_POINT ( 'NONE',  ( 119.7434548109119703, 0.2775794806942583071, -14.81454154325457928 ) ) ;
#2684=CARTESIAN_POINT ( 'NONE',  ( 121.1325173109119788, -9.289237151508434209, -11.05642687123711276 ) ) ;
#2685=CARTESIAN_POINT ( 'NONE',  ( 120.2990798109119766, -7.200787124940443817, -17.81845355600750835 ) ) ;
#2704=ADVANCED_FACE ( 'NONE', ( #21680 ), #17131, .F. ) ;
#2722=CARTESIAN_POINT ( 'NONE',  ( 121.9659548109119811, -2.527210466738041728, -8.967976844669124148 ) ) ;
#2736=ORIENTED_EDGE ( 'NONE', *, *, #23139, .F. ) ;
#2745=VERTEX_POINT ( 'NONE', #70 ) ;
#2757=CARTESIAN_POINT ( 'NONE',  ( 123.9800954359119771, -11.07370829466463569, -12.81314460846529002 ) ) ;
#2762=CARTESIAN_POINT ( 'NONE',  ( 120.8547048109119686, -2.527210466738041728, -8.967976844669124148 ) ) ;
#2825=CARTESIAN_POINT ( 'NONE',  ( 123.4939235609119663, -9.645473719204776586, -14.86997237629376656 ) ) ;
#2853=CARTESIAN_POINT ( 'NONE',  ( 120.0907204359119760, -10.25716656981731489, -12.88942061488890545 ) ) ;
#2879=CARTESIAN_POINT ( 'NONE',  ( 124.0527235609119714, -0.08666061303663243065, -11.91773565553389425 ) ) ;
#2887=CARTESIAN_POINT ( 'NONE',  ( 122.9382985609119743, -10.36940331770107093, -15.09355782777061350 ) ) ;
#2895=CARTESIAN_POINT ( 'NONE',  ( 124.0495485609119726, -0.08252387247379561197, -11.91645802438259771 ) ) ;
#2913=DIRECTION ( 'NONE',  ( -1.000000000000000000, 0.000000000000000000, -0.000000000000000000 ) ) ;
#2914=CARTESIAN_POINT ( 'NONE',  ( 122.7993923109119692, -0.4387604401700512802, -15.73000352943951619 ) ) ;
#2915=CARTESIAN_POINT ( 'NONE',  ( 121.2019704359119743, -10.25716656981731489, -12.88942061488890545 ) ) ;
#2916=VERTEX_POINT ( 'NONE', #37925 ) ;
#2935=FACE_OUTER_BOUND ( 'NONE', #42752, .T. ) ;
#2952=CARTESIAN_POINT ( 'NONE',  ( 123.2855641859119942, -8.321307733199551748, -9.223433127585318303 ) ) ;
#2976=VECTOR ( 'NONE', #3623, 1000.000000000000000 ) ;
#2989=CARTESIAN_POINT ( 'NONE',  ( 123.6328298109119714, -7.200787124940443817, -17.81845355600750835 ) ) ;
#3004=DIRECTION ( 'NONE',  ( 0.000000000000000000, -0.4669533266896290225, -0.8842819633428516957 ) ) ;
#3012=ORIENTED_EDGE ( 'NONE', *, *, #20300, .F. ) ;
#3021=ORIENTED_EDGE ( 'NONE', *, *, #35385, .T. ) ;
#3030=CARTESIAN_POINT ( 'NONE',  ( 120.0180923109119675, -9.285408612553503360, -11.05844856689016886 ) ) ;
#3054=CARTESIAN_POINT ( 'NONE',  ( 123.6328298109119714, -7.200787124940443817, -17.81845355600750835 ) ) ;
#3057=CARTESIAN_POINT ( 'NONE',  ( 124.7472578386062452, 2.844596103920410179, -12.34114520301823781 ) ) ;
#3075=CARTESIAN_POINT ( 'NONE',  ( 122.0046199480702569, -6.365377317481695663, -18.95617363400926081 ) ) ;
#3115=CARTESIAN_POINT ( 'NONE',  ( 122.6604860609119640, -6.564341423271553566, -7.887810678476492754 ) ) ;
#3124=CARTESIAN_POINT ( 'NONE',  ( 124.3968141859119925, -8.321307733199789780, -9.223433127585511926 ) ) ;
#3135=CARTESIAN_POINT ( 'NONE',  ( 123.9584548109119737, -9.675291321254654520, -19.78473021908636298 ) ) ;
#3141=CARTESIAN_POINT ( 'NONE',  ( 123.8411891859119862, -1.406689858478935573, -17.56299727309130887 ) ) ;
#3142=CARTESIAN_POINT ( 'NONE',  ( 121.6881423109119709, -9.959231468620755479, -10.70263013195267199 ) ) ;
#3148=CARTESIAN_POINT ( 'NONE',  ( 124.1916298109119765, -2.529232162390850913, -8.971805383624186447 ) ) ;
#3149=CARTESIAN_POINT ( 'NONE',  ( 119.6045485609119794, -0.08252387247370887580, -11.91645802438286417 ) ) ;
#3150=ORIENTED_EDGE ( 'NONE', *, *, #39135, .F. ) ;
#3152=ORIENTED_EDGE ( 'NONE', *, *, #22778, .F. ) ;
#3165=MECHANICAL_DESIGN_GEOMETRIC_PRESENTATION_REPRESENTATION('',(#37398),#22108);
#3166=CARTESIAN_POINT ( 'NONE',  ( 121.4103298109119748, -2.173413727453600508, -8.297982527556802879 ) ) ;
#3173=FACE_OUTER_BOUND ( 'NONE', #539, .T. ) ;
#3179=CARTESIAN_POINT ( 'NONE',  ( 124.1190016859119680, -9.665098340737509730, -17.37397104707595474 ) ) ;
#3188=EDGE_CURVE ( 'NONE', #5920, #30137, #13528, .T. ) ;
#3189=CARTESIAN_POINT ( 'NONE',  ( 123.0862602976252020, -8.580000213326620440, -17.71054824844518905 ) ) ;
#3199=CYLINDRICAL_SURFACE ( 'NONE', #16531, 1.587500000000000577 ) ;
#3208=EDGE_LOOP ( 'NONE', ( #28421, #11225, #13823, #21479 ) ) ;
#3213=CARTESIAN_POINT ( 'NONE',  ( 123.7022829359119811, -4.283928203966213211, -7.183505701512925334 ) ) ;
#3226=DIRECTION ( 'NONE',  ( 0.000000000000000000, -0.4669533266896266355, -0.8842819633428529169 ) ) ;
#3276=CARTESIAN_POINT ( 'NONE',  ( 121.3408766859119794, -9.033780868592240054, -16.85052413769862056 ) ) ;
#3297=CARTESIAN_POINT ( 'NONE',  ( 124.6894688159050872, -8.253847584685239269, -17.09290432062678278 ) ) ;
#3305=CARTESIAN_POINT ( 'NONE',  ( 119.8129079359119942, -4.360204210389833968, -8.000047426360245240 ) ) ;
#3326=AXIS2_PLACEMENT_3D ( 'NONE', #41163, #30884, #27248 ) ;
#3354=CARTESIAN_POINT ( 'NONE',  ( 121.9272896737536911, -8.611453504372539314, -17.77011218421760574 ) ) ;
#3363=CARTESIAN_POINT ( 'NONE',  ( 123.7263390224331516, -4.681800857092183854, -18.57451437749315559 ) ) ;
#3364=CARTESIAN_POINT ( 'NONE',  ( 120.5074391859119913, -8.844754642576884152, -8.592115655440050404 ) ) ;
#3378=( NAMED_UNIT ( * ) SI_UNIT ( $, .STERADIAN. ) SOLID_ANGLE_UNIT ( ) );
#3396=CARTESIAN_POINT ( 'NONE',  ( 125.4584548109119737, -7.411001340234434132, -5.146477690568067587 ) ) ;
#3405=CARTESIAN_POINT ( 'NONE',  ( 122.1743141859119817, -0.8832429491016019485, -18.19431474523657855 ) ) ;
#3411=VECTOR ( 'NONE', #44028, 1000.000000000000000 ) ;
#3414=CARTESIAN_POINT ( 'NONE',  ( 123.1339422641554506, -8.548534124195541040, -17.65096007659765220 ) ) ;
#3439=CARTESIAN_POINT ( 'NONE',  ( 120.6463454359119822, -11.07370829466463569, -12.81314460846529002 ) ) ;
#3444=CIRCLE ( 'NONE', #21632, 8.000000000000001776 ) ;
#3454=DIRECTION ( 'NONE',  ( 1.000000000000000000, 0.000000000000000000, 0.000000000000000000 ) ) ;
#3478=CARTESIAN_POINT ( 'NONE',  ( 123.6328298109119714, -7.200787124940443817, -17.81845355600750835 ) ) ;
#3499=CARTESIAN_POINT ( 'NONE',  ( 122.3132204359119868, -10.25716656981731489, -12.88942061488890545 ) ) ;
#3502=CARTESIAN_POINT ( 'NONE',  ( 124.6574308310801058, -0.1064883412648260086, -7.172770542335224597 ) ) ;
#3511=CARTESIAN_POINT ( 'NONE',  ( 122.6009548109119720, 2.753894863294152007, -15.83610205775420177 ) ) ;
#3522=LINE ( 'NONE', #30675, #3832 ) ;
#3551=DIRECTION ( 'NONE',  ( 0.000000000000000000, -0.9554676365605411226, -0.2950959089608217178 ) ) ;
#3565=B_SPLINE_CURVE_WITH_KNOTS ( 'NONE', 3,
 ( #27559, #6356, #33924, #17298, #20495, #31190, #27107, #45108, #13432, #34155 ),
 .UNSPECIFIED., .F., .F.,
 ( 4, 3, 3, 4 ),
 ( 9.263427422397549112E-19, 1.415135068336276058E-06, 2.830270136674489704E-06, 5.511645061733400693E-06 ),
 .UNSPECIFIED. ) ;
#3586=CARTESIAN_POINT ( 'NONE',  ( 121.8270485609119760, -0.08252387247370887580, -11.91645802438286417 ) ) ;
#3601=CARTESIAN_POINT ( 'NONE',  ( 120.5768923109119868, -9.959231468620755479, -10.70263013195267199 ) ) ;
#3608=CARTESIAN_POINT ( 'NONE',  ( 124.4694423109119725, -9.285408612553634811, -11.05844856689041755 ) ) ;
#3614=CARTESIAN_POINT ( 'NONE',  ( 125.1433143116076678, -11.83481241714331489, -10.81293854524298936 ) ) ;
#3616=CARTESIAN_POINT ( 'NONE',  ( 121.4103298109119748, -2.173413727453600508, -8.297982527556802879 ) ) ;
#3623=DIRECTION ( 'NONE',  ( 1.000000000000000000, 0.000000000000000000, 0.000000000000000000 ) ) ;
#3648=EDGE_LOOP ( 'NONE', ( #18266, #15979, #3658, #17310 ) ) ;
#3658=ORIENTED_EDGE ( 'NONE', *, *, #36456, .F. ) ;
#3689=CARTESIAN_POINT ( 'NONE',  ( 119.2541079359119749, -5.367357518394803684, -18.78171702160297585 ) ) ;
#3695=AXIS2_PLACEMENT_3D ( 'NONE', #40723, #9712, #26812 ) ;
#3716=CARTESIAN_POINT ( 'NONE',  ( 123.1466579359119891, -5.444069387712269226, -19.60292469916370450 ) ) ;
#3717=ORIENTED_EDGE ( 'NONE', *, *, #12759, .T. ) ;
#3719=CARTESIAN_POINT ( 'NONE',  ( 125.1589444732310312, -0.6168232227114794908, -7.334077581337427709 ) ) ;
#3722=VECTOR ( 'NONE', #11508, 1000.000000000000000 ) ;
#3728=CARTESIAN_POINT ( 'NONE',  ( 119.7434548109120129, -2.395764543994020279, -18.34942947847187611 ) ) ;
#3781=CARTESIAN_POINT ( 'NONE',  ( 122.3890647965036464, -8.305800998871424312, -17.19128988610634678 ) ) ;
#3792=CARTESIAN_POINT ( 'NONE',  ( 120.8547048109119686, -7.554583864224885481, -18.48844787311982785 ) ) ;
#3825=DIRECTION ( 'NONE',  ( 0.000000000000000000, 0.4669533266896289669, 0.8842819633428518067 ) ) ;
#3832=VECTOR ( 'NONE', #13358, 1000.000000000000000 ) ;
#3833=CARTESIAN_POINT ( 'NONE',  ( 124.3741441133355892, -11.15020770235569358, -8.516513975753223775 ) ) ;
#3835=CARTESIAN_POINT ( 'NONE',  ( 120.7852516859119731, -9.665098340737509730, -17.37397104707595474 ) ) ;
#3842=CARTESIAN_POINT ( 'NONE',  ( 119.7434548109119703, -1.575707845324203493, -20.23615509330177531 ) ) ;
#3845=CARTESIAN_POINT ( 'NONE',  ( 121.4551560953690483, -6.001247023715324147, -18.26661038929047010 ) ) ;
#3851=FACE_OUTER_BOUND ( 'NONE', #298, .T. ) ;
#3880=ORIENTED_EDGE ( 'NONE', *, *, #22278, .F. ) ;
#3888=CARTESIAN_POINT ( 'NONE',  ( 122.8300460087703954, -6.176492496456559955, -18.59847741292036716 ) ) ;
#3933=CLOSED_SHELL ( 'NONE', ( #33804, #43683, #2704, #14896, #35491, #14168, #32857, #17653, #12249, #18716, #14159, #37025, #39249, #42653, #37086, #27839, #42869, #27517, #653, #5131, #368, #39206, #43029, #30592, #5249, #37298, #29906, #24048, #28542, #15585, #31710, #37869, #29228, #36415, #38743, #43433 ) ) ;
#3938=CARTESIAN_POINT ( 'NONE',  ( 124.5665232958111091, -9.854882086978124178, -13.73083157374175300 ) ) ;
#3941=CARTESIAN_POINT ( 'NONE',  ( 125.0660727672592856, -0.4645083225204098554, -7.304893862189946852 ) ) ;
#3984=AXIS2_PLACEMENT_3D ( 'NONE', #3396, #13447, #40811 ) ;
#3995=CARTESIAN_POINT ( 'NONE',  ( 121.5582890828414122, -8.372502050422333753, -17.31760344562334808 ) ) ;
#4020=CARTESIAN_POINT ( 'NONE',  ( 121.7575954359119805, -11.07370829466463569, -12.81314460846529002 ) ) ;
#4042=CARTESIAN_POINT ( 'NONE',  ( 119.3267360609119692, -3.387241619883791355, -18.17469012370385073 ) ) ;
#4044=VERTEX_POINT ( 'NONE', #6713 ) ;
#4052=CARTESIAN_POINT ( 'NONE',  ( 124.9801526047702680, -12.03596826789013363, -10.88240524119288288 ) ) ;
#4064=CARTESIAN_POINT ( 'NONE',  ( 121.8965016859119856, -0.6942167230862464899, -9.935906262978006609 ) ) ;
#4065=CIRCLE ( 'NONE', #7023, 8.000000000000001776 ) ;
#4071=DIRECTION ( 'NONE',  ( 0.000000000000000000, 0.8842819633428519177, -0.4669533266896288004 ) ) ;
#4072=CARTESIAN_POINT ( 'NONE',  ( 120.6343014173871211, -8.493878760966627084, -17.54745775818410536 ) ) ;
#4117=CIRCLE ( 'NONE', #23078, 1.587500000000000355 ) ;
#4165=CARTESIAN_POINT ( 'NONE',  ( 124.5696098453081788, -9.847885663951533530, -13.82108784073833085 ) ) ;
#4166=CARTESIAN_POINT ( 'NONE',  ( 122.3132204359119868, 1.345710702986147034, -13.97328579221134426 ) ) ;
#4178=CARTESIAN_POINT ( 'NONE',  ( 119.7434548109119845, -1.419520476163944167, -9.663672953983557079 ) ) ;
#4197=CARTESIAN_POINT ( 'NONE',  ( 122.6009548109119720, -5.853704621469987934, -5.454671103420249523 ) ) ;
#4224=LINE ( 'NONE', #25213, #41087 ) ;
#4248=CARTESIAN_POINT ( 'NONE',  ( 122.2437673109119629, -9.289237151508434209, -11.05642687123711276 ) ) ;
#4265=CARTESIAN_POINT ( 'NONE',  ( 122.2437673109119629, 0.2312338769422704887, -16.08380026872395874 ) ) ;
#4266=CARTESIAN_POINT ( 'NONE',  ( 123.6805967241997877, -5.999335727763315695, -18.26299091719257461 ) ) ;
#4269=CARTESIAN_POINT ( 'NONE',  ( 123.2161110609119561, -3.163656168406935087, -18.89861972220014508 ) ) ;
#4282=CARTESIAN_POINT ( 'NONE',  ( 124.9774582099991846, -10.98257783126069853, -8.877266956160429601 ) ) ;
#4300=CARTESIAN_POINT ( 'NONE',  ( 121.3408766859119794, -0.06289925094097943703, -9.412459353600674206 ) ) ;
#4302=CARTESIAN_POINT ( 'NONE',  ( 120.7251408503701384, -8.552676153439012552, -17.65880394779906837 ) ) ;
#4304=EDGE_LOOP ( 'NONE', ( #26211, #21951, #33680 ) ) ;
#4319=DIRECTION ( 'NONE',  ( -1.000000000000000000, 0.000000000000000000, -0.000000000000000000 ) ) ;
#4358=CARTESIAN_POINT ( 'NONE',  ( 119.7434548109119703, -6.339884145921025116, -18.90789653539788517 ) ) ;
#4375=CARTESIAN_POINT ( 'NONE',  ( 120.7852516859119731, -9.665098340737509730, -17.37397104707595474 ) ) ;
#4382=FACE_OUTER_BOUND ( 'NONE', #8454, .T. ) ;
#4391=CARTESIAN_POINT ( 'NONE',  ( 124.5508470055817156, -9.863829598939307886, -13.27840026003464935 ) ) ;
#4392=CARTESIAN_POINT ( 'NONE',  ( 123.9106423109119675, -9.959231468620755479, -10.70263013195267199 ) ) ;
#4395=CARTESIAN_POINT ( 'NONE',  ( 125.0048763211382408, -2.344029031882285175, -6.249864847596490414 ) ) ;
#4478=CARTESIAN_POINT ( 'NONE',  ( 121.7575954359119805, 0.5291689781388270175, -13.89700978578772705 ) ) ;
#4496=CARTESIAN_POINT ( 'NONE',  ( 122.0354079359119908, -5.444069387712269226, -19.60292469916370450 ) ) ;
#4497=LINE ( 'NONE', #21830, #11907 ) ;
#4500=CARTESIAN_POINT ( 'NONE',  ( 123.9800954359119771, -11.07370829466463569, -12.81314460846529002 ) ) ;
#4528=CARTESIAN_POINT ( 'NONE',  ( 119.7821199480702603, -6.365377317481695663, -18.95617363400926081 ) ) ;
#4558=PRODUCT_DEFINITION_FORMATION_WITH_SPECIFIED_SOURCE ( 'ANY', '', #10294, .NOT_KNOWN. ) ;
#4600=CARTESIAN_POINT ( 'NONE',  ( 120.0907204359119760, 1.345710702986147034, -13.97328579221134426 ) ) ;
#4601=AXIS2_PLACEMENT_3D ( 'NONE', #1971, #36846, #25930 ) ;
#4614=CARTESIAN_POINT ( 'NONE',  ( 121.2714235609119697, 0.6414057260225851653, -11.69287257290600657 ) ) ;
#4657=ORIENTED_EDGE ( 'NONE', *, *, #38994, .F. ) ;
#4662=CARTESIAN_POINT ( 'NONE',  ( 125.0302870206146082, -8.104358653442693239, -6.574584932803245962 ) ) ;
#4687=EDGE_CURVE ( 'NONE', #28617, #13270, #42710, .T. ) ;
#4697=CARTESIAN_POINT ( 'NONE',  ( 123.4244704359119709, 1.345710702986147034, -13.97328579221134426 ) ) ;
#4721=CARTESIAN_POINT ( 'NONE',  ( 123.0772048109119652, -7.554583864224885481, -18.48844787311982785 ) ) ;
#4724=CARTESIAN_POINT ( 'NONE',  ( 120.1601735609119856, -9.645473719204776586, -14.86997237629376656 ) ) ;
#4732=CARTESIAN_POINT ( 'NONE',  ( 124.5122867449678097, -9.720823321642505732, -12.20364227757116282 ) ) ;
#4741=DIRECTION ( 'NONE',  ( 1.000000000000000000, 0.000000000000000000, 0.000000000000000000 ) ) ;
#4751=ORIENTED_EDGE ( 'NONE', *, *, #20284, .T. ) ;
#4753=CARTESIAN_POINT ( 'NONE',  ( 121.2714235609119697, 0.6414057260225851653, -11.69287257290600657 ) ) ;
#4754=CARTESIAN_POINT ( 'NONE',  ( 121.4103298109119748, -2.173413727453600508, -8.297982527556802879 ) ) ;
#4782=DIRECTION ( 'NONE',  ( -1.000000000000000000, 0.000000000000000000, -0.000000000000000000 ) ) ;
#4822=CARTESIAN_POINT ( 'NONE',  ( 121.2019704359119743, 1.345710702986147034, -13.97328579221134426 ) ) ;
#4870=CARTESIAN_POINT ( 'NONE',  ( 121.6307382662982945, -6.118135741080345191, -18.48796566952144005 ) ) ;
#4920=CARTESIAN_POINT ( 'NONE',  ( 119.6740016859119748, -0.6942167230862511529, -9.935906262978006609 ) ) ;
#4944=CARTESIAN_POINT ( 'NONE',  ( 123.9106423109119675, -9.959231468620755479, -10.70263013195267199 ) ) ;
#4953=CARTESIAN_POINT ( 'NONE',  ( 124.5273704333169320, -9.803742449528428438, -12.61775372557454844 ) ) ;
#4958=CARTESIAN_POINT ( 'NONE',  ( 124.9868051361382868, -12.36944789948101331, -14.53642012793133986 ) ) ;
#4975=CARTESIAN_POINT ( 'NONE',  ( 120.2990798109119766, -2.173413727453600508, -8.297982527556802879 ) ) ;
#4980=CARTESIAN_POINT ( 'NONE',  ( 120.9241579359119925, -5.444069387712269226, -19.60292469916370450 ) ) ;
#5011=CARTESIAN_POINT ( 'NONE',  ( 125.3046178784917828, -3.279438446396415241, -20.37743778007813233 ) ) ;
#5047=CARTESIAN_POINT ( 'NONE',  ( 119.8823610609119754, -3.163656168406935087, -18.89861972220014508 ) ) ;
#5063=DIRECTION ( 'NONE',  ( 0.000000000000000000, -0.4669533266896290225, -0.8842819633428516957 ) ) ;
#5094=AXIS2_PLACEMENT_3D ( 'NONE', #44178, #41435, #3551 ) ;
#5096=CARTESIAN_POINT ( 'NONE',  ( 125.4584548109119737, -7.476587315910852460, -21.06050163197695824 ) ) ;
#5109=CARTESIAN_POINT ( 'NONE',  ( 123.9584548109119737, -8.523281198020143279, -6.279169073056789507 ) ) ;
#5122=ORIENTED_EDGE ( 'NONE', *, *, #26712, .F. ) ;
#5131=ADVANCED_FACE ( 'NONE', ( #29860 ), #13593, .T. ) ;
#5168=CARTESIAN_POINT ( 'NONE',  ( 121.0630641859119976, -8.321307733199551748, -9.223433127585318303 ) ) ;
#5175=CARTESIAN_POINT ( 'NONE',  ( 124.5068972094509689, -9.682373403232579889, -12.05773893725193879 ) ) ;
#5177=CARTESIAN_POINT ( 'NONE',  ( 121.2714235609119697, 0.6414057260225808355, -11.69287257290601545 ) ) ;
#5180=CARTESIAN_POINT ( 'NONE',  ( 125.2986504416607261, -11.52710089177262098, -16.05128639071223162 ) ) ;
#5201=CARTESIAN_POINT ( 'NONE',  ( 123.9800954359119771, -11.07370829466463569, -12.81314460846529002 ) ) ;
#5202=CARTESIAN_POINT ( 'NONE',  ( 121.1325173109119788, 0.2312338769422704887, -16.08380026872395874 ) ) ;
#5209=VECTOR ( 'NONE', #37485, 1000.000000000000000 ) ;
#5238=CARTESIAN_POINT ( 'NONE',  ( 125.3082514830540788, -3.264913200334888632, -20.36649584582930572 ) ) ;
#5249=ADVANCED_FACE ( 'NONE', ( #8885 ), #43547, .T. ) ;
#5255=CARTESIAN_POINT ( 'NONE',  ( 119.7434548109119703, -2.527210466738042172, -8.967976844669124148 ) ) ;
#5265=ORIENTED_EDGE ( 'NONE', *, *, #43179, .F. ) ;
#5275=CARTESIAN_POINT ( 'NONE',  ( 121.3408766859119794, -0.06289925094097943703, -9.412459353600674206 ) ) ;
#5281=CARTESIAN_POINT ( 'NONE',  ( 120.5074391859119913, -1.406689858478933353, -17.56299727309130887 ) ) ;
#5317=DIRECTION ( 'NONE',  ( 1.000000000000000000, 0.000000000000000000, 0.000000000000000000 ) ) ;
#5326=DIRECTION ( 'NONE',  ( 0.000000000000000000, -0.4669533266896288004, -0.8842819633428519177 ) ) ;
#5342=CARTESIAN_POINT ( 'NONE',  ( 124.6565730087413044, -8.387630329567796750, -6.398857485523961941 ) ) ;
#5344=EDGE_CURVE ( 'NONE', #13081, #33790, #4117, .T. ) ;
#5346=CARTESIAN_POINT ( 'NONE',  ( 121.1325173109119788, -9.289237151508434209, -11.05642687123711276 ) ) ;
#5372=CARTESIAN_POINT ( 'NONE',  ( 124.6565730087442745, 2.573342726250678059, -15.84738921862590288 ) ) ;
#5399=CARTESIAN_POINT ( 'NONE',  ( 122.1743141859119817, -8.321307733199551748, -9.223433127585318303 ) ) ;
#5406=CARTESIAN_POINT ( 'NONE',  ( 119.7434548109119703, -4.863998795839242995, -13.39321520033831447 ) ) ;
#5430=CARTESIAN_POINT ( 'NONE',  ( 123.7022829359119811, -4.283928203966213211, -7.183505701512925334 ) ) ;
#5431=CARTESIAN_POINT ( 'NONE',  ( 121.7575954359119805, -11.07370829466463569, -12.81314460846529002 ) ) ;
#5451=CARTESIAN_POINT ( 'NONE',  ( 120.0875454359120056, -10.25250061710389105, -12.88985647778275911 ) ) ;
#5457=CARTESIAN_POINT ( 'NONE',  ( 125.3319029555670312, -2.398109642850332790, -20.05449063107751684 ) ) ;
#5460=CARTESIAN_POINT ( 'NONE',  ( 121.2714235609119697, -9.645473719204776586, -14.86997237629376656 ) ) ;
#5473=CARTESIAN_POINT ( 'NONE',  ( 125.1645598511810817, -9.397726027288767270, -19.25909742224127186 ) ) ;
#5492=CARTESIAN_POINT ( 'NONE',  ( 123.3550173109119612, 0.2312338769422704887, -16.08380026872395874 ) ) ;
#5496=CARTESIAN_POINT ( 'NONE',  ( 121.4797829359119987, -5.367793381288652910, -18.78638297431638904 ) ) ;
#5505=( BOUNDED_SURFACE ( )  B_SPLINE_SURFACE ( 1, 2, ( 
 ( #5855, #16136, #43954, #19328, #19778, #40534, #33660, #23662, #44638, #13403, #16360, #37548, #16595, #12950, #40997, #40759, #6088 ),
 ( #41222, #23433, #30488, #13174, #27076, #6321, #2895, #27305, #9980, #6996, #24762, #3124, #38217, #17048, #20908, #41668, #28416 ) ),
 .UNSPECIFIED., .F., .F., .F. ) 
 B_SPLINE_SURFACE_WITH_KNOTS ( ( 2, 2 ),
 ( 3, 2, 2, 2, 2, 2, 2, 2, 3 ),
 ( 0.000000000000000000, 1.000000000000000000 ),
 ( 0.000000000000000000, 0.1250000000000000000, 0.2500000000000000000, 0.3750000000000000000, 0.5000000000000000000, 0.6250000000000000000, 0.7500000000000000000, 0.8750000000000000000, 1.000000000000000000 ),
 .UNSPECIFIED. ) 
 GEOMETRIC_REPRESENTATION_ITEM ( )  RATIONAL_B_SPLINE_SURFACE ( (
 ( 1.000000000000000000, 0.9238795325112869605, 1.000000000000000000, 0.9238795325112869605, 1.000000000000000000, 0.9238795325112869605, 1.000000000000000000, 0.9238795325112869605, 1.000000000000000000, 0.9238795325112869605, 1.000000000000000000, 0.9238795325112869605, 1.000000000000000000, 0.9238795325112869605, 1.000000000000000000, 0.9238795325112869605, 1.000000000000000000),
 ( 1.000000000000000000, 0.9238795325112869605, 1.000000000000000000, 0.9238795325112869605, 1.000000000000000000, 0.9238795325112869605, 1.000000000000000000, 0.9238795325112869605, 1.000000000000000000, 0.9238795325112869605, 1.000000000000000000, 0.9238795325112869605, 1.000000000000000000, 0.9238795325112869605, 1.000000000000000000, 0.9238795325112869605, 1.000000000000000000) ) ) 
 REPRESENTATION_ITEM ( '' )  SURFACE ( )  );
#5550=AXIS2_PLACEMENT_3D ( 'NONE', #36411, #32984, #26168 ) ;
#5559=CARTESIAN_POINT ( 'NONE',  ( 125.1433143116104389, -7.968577257696042970, -6.639574498171168848 ) ) ;
#5562=CARTESIAN_POINT ( 'NONE',  ( 120.8547048109119686, -2.527210466738041728, -8.967976844669124148 ) ) ;
#5587=CARTESIAN_POINT ( 'NONE',  ( 125.1028739313169496, 1.212150000717685305, -17.73793242834041095 ) ) ;
#5620=CARTESIAN_POINT ( 'NONE',  ( 125.3303382280792846, 2.061758691653259312, -11.74840549411501556 ) ) ;
#5626=CARTESIAN_POINT ( 'NONE',  ( 121.8270485609119760, -10.36940331770107093, -15.09355782777061350 ) ) ;
#5628=CARTESIAN_POINT ( 'NONE',  ( 125.2572271076672905, -11.54560042640431838, -16.20890238838691744 ) ) ;
#5632=CARTESIAN_POINT ( 'NONE',  ( 119.7434548109119703, -6.019411175499098654, -18.97193101650639591 ) ) ;
#5650=CARTESIAN_POINT ( 'NONE',  ( 119.9518141859119851, -8.321307733199551748, -9.223433127585318303 ) ) ;
#5651=CARTESIAN_POINT ( 'NONE',  ( 122.5910329359119970, -4.283928203966213211, -7.183505701512925334 ) ) ;
#5660=( LENGTH_UNIT ( ) NAMED_UNIT ( * ) SI_UNIT ( .MILLI., .METRE. ) );
#5682=CARTESIAN_POINT ( 'NONE',  ( 125.3562121110092846, -2.843430562235182535, -20.14166698885114926 ) ) ;
#5685=CARTESIAN_POINT ( 'NONE',  ( 124.3968141859119783, -8.321307733199551748, -9.223433127585318303 ) ) ;
#5718=CARTESIAN_POINT ( 'NONE',  ( 123.4939235609119663, 0.6414057260225851653, -11.69287257290600657 ) ) ;
#5722=CARTESIAN_POINT ( 'NONE',  ( 120.9241579359119925, -4.360204210389833968, -8.000047426360245240 ) ) ;
#5756=CARTESIAN_POINT ( 'NONE',  ( 121.1325173109119788, -9.289237151508434209, -11.05642687123711276 ) ) ;
#5812=CARTESIAN_POINT ( 'NONE',  ( 124.9542645564618653, 2.335564274171338273, -15.89604958949715829 ) ) ;
#5844=CARTESIAN_POINT ( 'NONE',  ( 121.6186891859119896, -1.406689858478933353, -17.56299727309130887 ) ) ;
#5855=CARTESIAN_POINT ( 'NONE',  ( 123.6360048109119703, -7.198765429287139916, -17.81462501705270540 ) ) ;
#5868=CARTESIAN_POINT ( 'NONE',  ( 124.6989476299233530, -12.60226495975998517, -14.43526558578360053 ) ) ;
#5878=CARTESIAN_POINT ( 'NONE',  ( 119.4656423109119743, -0.4387604401700512802, -15.73000352943951619 ) ) ;
#5879=CARTESIAN_POINT ( 'NONE',  ( 120.6463454359119822, 0.5291689781388270175, -13.89700978578772705 ) ) ;
#5905=CARTESIAN_POINT ( 'NONE',  ( 120.0180923109119675, -9.285408612553503360, -11.05844856689016886 ) ) ;
#5915=CARTESIAN_POINT ( 'NONE',  ( 124.3273610609119686, -6.340755971794695078, -8.611740276972781771 ) ) ;
#5920=VERTEX_POINT ( 'NONE', #42373 ) ;
#5924=LINE ( 'NONE', #19847, #28365 ) ;
#5947=CARTESIAN_POINT ( 'NONE',  ( 121.8965016859119856, -9.665098340737509730, -17.37397104707595474 ) ) ;
#5951=CARTESIAN_POINT ( 'NONE',  ( 124.3968141859119783, -8.321307733199551748, -9.223433127585318303 ) ) ;
#5986=CARTESIAN_POINT ( 'NONE',  ( 123.5812993874819909, -6.063848558940142297, -18.38516058545102183 ) ) ;
#5990=CARTESIAN_POINT ( 'NONE',  ( 123.4939235609119663, -9.645473719204776586, -14.86997237629376656 ) ) ;
#6008=ORIENTED_EDGE ( 'NONE', *, *, #43865, .F. ) ;
#6009=CARTESIAN_POINT ( 'NONE',  ( 120.6463454359119822, 0.5291689781388270175, -13.89700978578772705 ) ) ;
#6014=CARTESIAN_POINT ( 'NONE',  ( 121.5492360609119800, -3.387241619883791355, -18.17469012370385073 ) ) ;
#6024=ORIENTED_EDGE ( 'NONE', *, *, #28670, .F. ) ;
#6073=CARTESIAN_POINT ( 'NONE',  ( 123.0772048109119652, -2.527210466738041728, -8.967976844669124148 ) ) ;
#6076=FACE_OUTER_BOUND ( 'NONE', #21053, .T. ) ;
#6082=CARTESIAN_POINT ( 'NONE',  ( 120.9451081739443055, -4.756192495830076084, -19.39047411591439385 ) ) ;
#6086=VECTOR ( 'NONE', #5317, 1000.000000000000000 ) ;
#6088=CARTESIAN_POINT ( 'NONE',  ( 124.7472548109119828, -7.198765429287139916, -17.81462501705270540 ) ) ;
#6090=CARTESIAN_POINT ( 'NONE',  ( 119.7434548109119845, 0.3713923125418727711, -14.33547248937080631 ) ) ;
#6112=CARTESIAN_POINT ( 'NONE',  ( 121.0630641859119976, -8.321307733199551748, -9.223433127585318303 ) ) ;
#6113=CARTESIAN_POINT ( 'NONE',  ( 121.8965016859119856, -0.6942167230862511529, -9.935906262978006609 ) ) ;
#6126=AXIS2_PLACEMENT_3D ( 'NONE', #30820, #17585, #44968 ) ;
#6145=AXIS2_PLACEMENT_3D ( 'NONE', #34992, #38004, #27753 ) ;
#6149=CARTESIAN_POINT ( 'NONE',  ( 121.4103298109119748, -7.200787124940443817, -17.81845355600750835 ) ) ;
#6164=CARTESIAN_POINT ( 'NONE',  ( 123.9584548109119737, -9.675291321254654520, -19.78473021908636298 ) ) ;
#6167=CARTESIAN_POINT ( 'NONE',  ( 123.3550173109119612, 0.2312338769422730977, -16.08380026872395163 ) ) ;
#6183=CARTESIAN_POINT ( 'NONE',  ( 122.7299391859119737, -8.844754642576884152, -8.592115655440050404 ) ) ;
#6187=CARTESIAN_POINT ( 'NONE',  ( 124.6746266859119743, -9.033780868592240054, -16.85052413769862056 ) ) ;
#6210=CARTESIAN_POINT ( 'NONE',  ( 121.1899213555256409, -8.364211927971188842, -17.30190421972978143 ) ) ;
#6223=DIRECTION ( 'NONE',  ( 0.000000000000000000, 0.4669533266896290780, 0.8842819633428518067 ) ) ;
#6246=CARTESIAN_POINT ( 'NONE',  ( 120.4379860609119675, -3.387241619883791355, -18.17469012370385073 ) ) ;
#6254=CARTESIAN_POINT ( 'NONE',  ( 124.4662673109119737, -9.289237151508434209, -11.05642687123711276 ) ) ;
#6255=ORIENTED_EDGE ( 'NONE', *, *, #4687, .F. ) ;
#6319=CARTESIAN_POINT ( 'NONE',  ( 122.6150890224331675, -4.681800857092183854, -18.57451437749315559 ) ) ;
#6320=FACE_OUTER_BOUND ( 'NONE', #12308, .T. ) ;
#6321=CARTESIAN_POINT ( 'NONE',  ( 123.9800954359119771, 0.5291689781388532188, -13.89700978578742152 ) ) ;
#6323=CARTESIAN_POINT ( 'NONE',  ( 119.7434548109119561, -4.722584480144054631, -19.03897489626359274 ) ) ;
#6324=ORIENTED_EDGE ( 'NONE', *, *, #10043, .T. ) ;
#6333=CARTESIAN_POINT ( 'NONE',  ( 124.9235546484006250, -12.43496779199546687, -14.50182173845576727 ) ) ;
#6344=CARTESIAN_POINT ( 'NONE',  ( 122.2437673109119629, -9.289237151508434209, -11.05642687123711276 ) ) ;
#6345=ADVANCED_BREP_SHAPE_REPRESENTATION ( '', ( #21657, #12375 ), #32226 ) ;
#6346=CARTESIAN_POINT ( 'NONE',  ( 119.5350954359119839, 0.5291689781388270175, -13.89700978578772705 ) ) ;
#6356=CARTESIAN_POINT ( 'NONE',  ( 120.2513128976245724, -8.245411914654436458, -17.07692946740144180 ) ) ;
#6377=EDGE_CURVE ( 'NONE', #2745, #2517, #30035, .T. ) ;
#6384=CARTESIAN_POINT ( 'NONE',  ( 120.1601735609119856, 0.6414057260225851653, -11.69287257290600657 ) ) ;
#6405=CARTESIAN_POINT ( 'NONE',  ( 124.1497896737536877, -8.611453504372539314, -17.77011218421760574 ) ) ;
#6406=ORIENTED_EDGE ( 'NONE', *, *, #13986, .F. ) ;
#6410=AXIS2_PLACEMENT_3D ( 'NONE', #19499, #29080, #2149 ) ;
#6418=CARTESIAN_POINT ( 'NONE',  ( 123.9106423109119675, -9.959231468620755479, -10.70263013195267199 ) ) ;
#6422=CARTESIAN_POINT ( 'NONE',  ( 123.9106423109119675, -0.4387604401700512802, -15.73000352943951619 ) ) ;
#6434=ORIENTED_EDGE ( 'NONE', *, *, #36836, .T. ) ;
#6436=CARTESIAN_POINT ( 'NONE',  ( 119.7434548109119703, -12.48189245497263755, -10.95032834292243074 ) ) ;
#6443=EDGE_CURVE ( 'NONE', #20552, #13839, #37478, .T. ) ;
#6459=CARTESIAN_POINT ( 'NONE',  ( 119.2572829359120021, -5.367793381288652910, -18.78638297431638904 ) ) ;
#6472=ORIENTED_EDGE ( 'NONE', *, *, #18619, .T. ) ;
#6483=CARTESIAN_POINT ( 'NONE',  ( 119.7434548109119703, -7.554583864224885481, -18.48844787311982785 ) ) ;
#6486=CARTESIAN_POINT ( 'NONE',  ( 125.0849378844212367, 2.528548847979777303, -12.18453881567924135 ) ) ;
#6508=CARTESIAN_POINT ( 'NONE',  ( 125.4584548109119737, -1.575707845324203493, -20.23615509330177531 ) ) ;
#6521=ORIENTED_EDGE ( 'NONE', *, *, #32029, .F. ) ;
#6542=CARTESIAN_POINT ( 'NONE',  ( 121.7455514173871194, -8.493878760966627084, -17.54745775818410536 ) ) ;
#6570=CARTESIAN_POINT ( 'NONE',  ( 120.9241579359119925, -4.360204210389833968, -8.000047426360245240 ) ) ;
#6602=CARTESIAN_POINT ( 'NONE',  ( 120.8933699480702586, -6.365377317481695663, -18.95617363400926081 ) ) ;
#6605=CARTESIAN_POINT ( 'NONE',  ( 121.3408766859119794, -0.06289925094097943703, -9.412459353600674206 ) ) ;
#6645=CARTESIAN_POINT ( 'NONE',  ( 121.8965016859119856, -9.665098340737509730, -17.37397104707595474 ) ) ;
#6666=EDGE_CURVE ( 'NONE', #13270, #16241, #28196, .T. ) ;
#6683=CARTESIAN_POINT ( 'NONE',  ( 120.2959048109119777, -7.198765429287387718, -17.81462501705257395 ) ) ;
#6700=CARTESIAN_POINT ( 'NONE',  ( 121.1325173109119788, -9.289237151508434209, -11.05642687123711276 ) ) ;
#6702=AXIS2_PLACEMENT_3D ( 'NONE', #25084, #4319, #25312 ) ;
#6711=CARTESIAN_POINT ( 'NONE',  ( 122.0354079359119908, -4.360204210389833968, -8.000047426360245240 ) ) ;
#6713=CARTESIAN_POINT ( 'NONE',  ( 123.0385396737536752, -8.611453504372539314, -17.77011218421760574 ) ) ;
#6721=CARTESIAN_POINT ( 'NONE',  ( 123.9584548109119737, -8.523281198020143279, -6.279169073056789507 ) ) ;
#6760=VECTOR ( 'NONE', #26806, 1000.000000000000000 ) ;
#6770=CARTESIAN_POINT ( 'NONE',  ( 122.5910329359119828, -4.283928203966204329, -7.183505701512929775 ) ) ;
#6794=CARTESIAN_POINT ( 'NONE',  ( 120.9241579359119925, -5.444069387712269226, -19.60292469916370450 ) ) ;
#6833=CARTESIAN_POINT ( 'NONE',  ( 121.1325173109119788, 0.2312338769422704887, -16.08380026872395874 ) ) ;
#6847=CARTESIAN_POINT ( 'NONE',  ( 123.9106423109119675, -9.959231468620748373, -10.70263013195265778 ) ) ;
#6911=UNCERTAINTY_MEASURE_WITH_UNIT (LENGTH_MEASURE( 1.000000000000000082E-05 ), #38688, 'distance_accuracy_value', 'NONE');
#6917=CARTESIAN_POINT ( 'NONE',  ( 121.8965016859119856, -0.6942167230862511529, -9.935906262978006609 ) ) ;
#6928=CARTESIAN_POINT ( 'NONE',  ( 122.1743141859119817, -8.321307733199551748, -9.223433127585318303 ) ) ;
#6932=CARTESIAN_POINT ( 'NONE',  ( 124.4646854081434526, 2.188825697814051452, -9.798915638107947856 ) ) ;
#6988=CARTESIAN_POINT ( 'NONE',  ( 124.6259452904873655, -9.410405169419663096, -15.50563694605804876 ) ) ;
#6994=CARTESIAN_POINT ( 'NONE',  ( 123.5880035264548837, -8.247323210606174015, -17.08054893949881858 ) ) ;
#6996=CARTESIAN_POINT ( 'NONE',  ( 124.2579079359120016, -4.360204210390138613, -8.000047426360218594 ) ) ;
#7012=CARTESIAN_POINT ( 'NONE',  ( 122.7993923109119692, -9.959231468620755479, -10.70263013195267199 ) ) ;
#7017=CARTESIAN_POINT ( 'NONE',  ( 121.3408766859119794, -9.033780868592240054, -16.85052413769862056 ) ) ;
#7023=AXIS2_PLACEMENT_3D ( 'NONE', #557, #24953, #39308 ) ;
#7034=CARTESIAN_POINT ( 'NONE',  ( 120.2990798109119766, -2.173413727453600508, -8.297982527556802879 ) ) ;
#7046=CYLINDRICAL_SURFACE ( 'NONE', #20864, 1.587500000000000355 ) ;
#7048=CARTESIAN_POINT ( 'NONE',  ( 120.8547048109119686, -7.554583864224885481, -18.48844787311982785 ) ) ;
#7058=CARTESIAN_POINT ( 'NONE',  ( 123.5003147965036447, -8.305800998871427865, -17.19128988610635744 ) ) ;
#7092=FACE_OUTER_BOUND ( 'NONE', #36289, .T. ) ;
#7134=VERTEX_POINT ( 'NONE', #1271 ) ;
#7141=CARTESIAN_POINT ( 'NONE',  ( 121.6186891859119896, -8.844754642576884152, -8.592115655440050404 ) ) ;
#7150=ORIENTED_EDGE ( 'NONE', *, *, #1973, .F. ) ;
#7179=VERTEX_POINT ( 'NONE', #3297 ) ;
#7210=CARTESIAN_POINT ( 'NONE',  ( 122.1655659103642222, -8.454079026182057532, -17.47208793939445215 ) ) ;
#7253=FACE_OUTER_BOUND ( 'NONE', #14340, .T. ) ;
#7258=CARTESIAN_POINT ( 'NONE',  ( 125.0532895624267553, -10.95664536207781659, -8.976081904060929872 ) ) ;
#7260=CARTESIAN_POINT ( 'NONE',  ( 123.7717360609119623, -6.564341423271550902, -7.887810678476487425 ) ) ;
#7270=CARTESIAN_POINT ( 'NONE',  ( 121.5492360609119800, -3.387241619883789134, -18.17469012370384718 ) ) ;
#7276=CARTESIAN_POINT ( 'NONE',  ( 125.3134144568203681, -8.454919450556467098, -17.47367947343729710 ) ) ;
#7286=DIRECTION ( 'NONE',  ( -1.000000000000000000, 0.000000000000000000, -0.000000000000000000 ) ) ;
#7349=CARTESIAN_POINT ( 'NONE',  ( 121.5492360609119800, -3.387241619883791355, -18.17469012370385073 ) ) ;
#7361=CARTESIAN_POINT ( 'NONE',  ( 124.5827871365980144, -9.800012535114518641, -14.21035762377393041 ) ) ;
#7363=VERTEX_POINT ( 'NONE', #3075 ) ;
#7365=CARTESIAN_POINT ( 'NONE',  ( 125.2512653913828728, -0.8349821636219845189, -7.351438796280286070 ) ) ;
#7374=CARTESIAN_POINT ( 'NONE',  ( 119.7434548109119703, -0.7361556930925071685, -10.35768125360512393 ) ) ;
#7392=DIRECTION ( 'NONE',  ( 0.000000000000000000, -0.4669533266896290225, -0.8842819633428516957 ) ) ;
#7439=CARTESIAN_POINT ( 'NONE',  ( 120.9936110609119737, -3.163656168406935087, -18.89861972220014508 ) ) ;
#7464=CARTESIAN_POINT ( 'NONE',  ( 123.1466579359119891, -5.444069387712269226, -19.60292469916370450 ) ) ;
#7472=CARTESIAN_POINT ( 'NONE',  ( 124.3305360609119816, -6.339478340643663223, -8.615877017535705562 ) ) ;
#7481=CARTESIAN_POINT ( 'NONE',  ( 124.0495485609119584, -10.36940331770106916, -15.09355782777062061 ) ) ;
#7499=CARTESIAN_POINT ( 'NONE',  ( 120.7852516859119731, -9.665098340737509730, -17.37397104707595474 ) ) ;
#7513=( BOUNDED_SURFACE ( )  B_SPLINE_SURFACE ( 1, 2, ( 
 ( #31280, #6459, #23570, #41572, #34031, #13967, #20593, #30623, #10551, #34469, #28103, #274, #37905, #30845, #10332, #21027, #41126 ),
 ( #34900, #3689, #16951, #17611, #9648, #13300, #9885, #17174, #23796, #37686, #20368, #34255, #3030, #13750, #20809, #44768, #6683 ) ),
 .UNSPECIFIED., .F., .F., .T. ) 
 B_SPLINE_SURFACE_WITH_KNOTS ( ( 2, 2 ),
 ( 3, 2, 2, 2, 2, 2, 2, 2, 3 ),
 ( 0.000000000000000000, 1.000000000000000000 ),
 ( 0.000000000000000000, 0.1250000000000000000, 0.2500000000000000000, 0.3750000000000000000, 0.5000000000000000000, 0.6250000000000000000, 0.7500000000000000000, 0.8750000000000000000, 1.000000000000000000 ),
 .UNSPECIFIED. ) 
 GEOMETRIC_REPRESENTATION_ITEM ( )  RATIONAL_B_SPLINE_SURFACE ( (
 ( 1.000000000000000000, 0.9238795325112869605, 1.000000000000000000, 0.9238795325112869605, 1.000000000000000000, 0.9238795325112869605, 1.000000000000000000, 0.9238795325112869605, 1.000000000000000000, 0.9238795325112869605, 1.000000000000000000, 0.9238795325112869605, 1.000000000000000000, 0.9238795325112869605, 1.000000000000000000, 0.9238795325112869605, 1.000000000000000000),
 ( 1.000000000000000000, 0.9238795325112869605, 1.000000000000000000, 0.9238795325112869605, 1.000000000000000000, 0.9238795325112869605, 1.000000000000000000, 0.9238795325112869605, 1.000000000000000000, 0.9238795325112869605, 1.000000000000000000, 0.9238795325112869605, 1.000000000000000000, 0.9238795325112869605, 1.000000000000000000, 0.9238795325112869605, 1.000000000000000000) ) ) 
 REPRESENTATION_ITEM ( '' )  SURFACE ( )  );
#7535=CARTESIAN_POINT ( 'NONE',  ( 123.0681493241987425, -6.333924026435813204, -18.89660969823682279 ) ) ;
#7559=CARTESIAN_POINT ( 'NONE',  ( 120.2475493874819961, -6.063848558940142297, -18.38516058545102183 ) ) ;
#7575=CARTESIAN_POINT ( 'NONE',  ( 121.3408766859119794, -9.033780868592240054, -16.85052413769862056 ) ) ;
#7584=VERTEX_POINT ( 'NONE', #38839 ) ;
#7587=CARTESIAN_POINT ( 'NONE',  ( 124.5726818087965171, -9.839536840243070515, -13.91122383889339353 ) ) ;
#7589=CARTESIAN_POINT ( 'NONE',  ( 121.3408766859119794, -0.06289925094097943703, -9.412459353600674206 ) ) ;
#7616=ORIENTED_EDGE ( 'NONE', *, *, #28641, .T. ) ;
#7617=CARTESIAN_POINT ( 'NONE',  ( 121.8615784624957570, -6.270977643812233104, -18.77740645536396258 ) ) ;
#7620=CARTESIAN_POINT ( 'NONE',  ( 123.9584548109119737, -4.863998795839242995, -13.39321520033831447 ) ) ;
#7640=AXIS2_PLACEMENT_3D ( 'NONE', #35681, #39113, #10862 ) ;
#7671=CARTESIAN_POINT ( 'NONE',  ( 124.1884548109119777, -7.554583864224885481, -18.48844787311982785 ) ) ;
#7685=PRODUCT_CONTEXT ( 'NONE', #25371, 'mechanical' ) ;
#7694=CARTESIAN_POINT ( 'NONE',  ( 122.1048610609119720, -3.163656168406935087, -18.89861972220014508 ) ) ;
#7750=VERTEX_POINT ( 'NONE', #15807 ) ;
#7769=B_SPLINE_CURVE_WITH_KNOTS ( 'NONE', 3,
 ( #25745, #25968, #29608, #9091, #43524, #22993, #12292, #26644, #43069, #11837 ),
 .UNSPECIFIED., .F., .F.,
 ( 4, 3, 3, 4 ),
 ( 2.168404344971010024E-18, 0.0002476486541971034965, 0.0004952973025691040062, 0.0009610892161188160261 ),
 .UNSPECIFIED. ) ;
#7808=CARTESIAN_POINT ( 'NONE',  ( 122.1048610609119720, -6.340755971794695078, -8.611740276972781771 ) ) ;
#7823=CARTESIAN_POINT ( 'NONE',  ( 124.5380943420727249, -9.841908302772747419, -12.91703728233334125 ) ) ;
#7824=CARTESIAN_POINT ( 'NONE',  ( 121.5492360609119800, -6.564341423271550902, -7.887810678476487425 ) ) ;
#7827=CARTESIAN_POINT ( 'NONE',  ( 119.7434548109119703, -2.578558445503555951, -8.944152590684078419 ) ) ;
#7834=ORIENTED_EDGE ( 'NONE', *, *, #5344, .F. ) ;
#7902=CARTESIAN_POINT ( 'NONE',  ( 121.4103298109119748, -7.200787124940443817, -17.81845355600750835 ) ) ;
#7920=CARTESIAN_POINT ( 'NONE',  ( 121.7575954359119805, -11.07370829466463569, -12.81314460846529002 ) ) ;
#7923=CARTESIAN_POINT ( 'NONE',  ( 122.1743141859119817, -0.8832429491016019485, -18.19431474523657855 ) ) ;
#7926=CARTESIAN_POINT ( 'NONE',  ( 122.3253830209070259, -6.157706758239399392, -18.56290235964623392 ) ) ;
#7935=CARTESIAN_POINT ( 'NONE',  ( 124.9542645564618510, -12.06356186585028745, -10.89038081117960033 ) ) ;
#7954=CARTESIAN_POINT ( 'NONE',  ( 120.5074391859119913, -8.844754642576884152, -8.592115655440050404 ) ) ;
#7958=ORIENTED_EDGE ( 'NONE', *, *, #32029, .T. ) ;
#7972=VERTEX_POINT ( 'NONE', #33558 ) ;
#8027=CARTESIAN_POINT ( 'NONE',  ( 122.3132204359119868, -10.25716656981731489, -12.88942061488890545 ) ) ;
#8034=B_SPLINE_CURVE_WITH_KNOTS ( 'NONE', 3,
 ( #19318, #26157, #12485, #13555, #6932, #20401, #9059, #12262, #33203, #45020, #34501, #38157, #15903, #43494, #34285, #23829, #44571, #43716, #37716, #5620, #13778, #41155, #20177, #27689, #41603, #6486, #40295, #8826, #22959, #27465, #20839, #3057, #36852, #22729, #34061, #10362 ),
 .UNSPECIFIED., .F., .F.,
 ( 4, 2, 2, 2, 2, 1, 2, 2, 2, 2, 2, 2, 2, 1, 2, 2, 2, 2, 4 ),
 ( 0.000000000000000000, 0.06249999999995659028, 0.1249999999999131806, 0.1874999999998697708, 0.2187499999998515632, 0.2343749999998424594, 0.2421874999998402667, 0.2499999999998380740, 0.3749999999998612221, 0.4999999999998843148, 0.6249999999999074074, 0.6874999999999189537, 0.7187499999999243938, 0.7343749999999275024, 0.7421874999999237277, 0.7499999999999199529, 0.8124999999999399369, 0.8749999999999599209, 1.000000000000000000 ),
 .UNSPECIFIED. ) ;
#8045=CARTESIAN_POINT ( 'NONE',  ( 120.7157985609119635, -10.36940331770106916, -15.09355782777062061 ) ) ;
#8048=CARTESIAN_POINT ( 'NONE',  ( 123.9584548109119737, -2.421111938423274879, -5.775321541204940345 ) ) ;
#8099=CARTESIAN_POINT ( 'NONE',  ( 122.6009548109119720, -3.874292970208447873, -21.33175929725637587 ) ) ;
#8115=AXIS2_PLACEMENT_3D ( 'NONE', #35299, #4071, #17995 ) ;
#8128=CARTESIAN_POINT ( 'NONE',  ( 123.9584548109119737, 2.753894863294152007, -15.83610205775420177 ) ) ;
#8135=CARTESIAN_POINT ( 'NONE',  ( 119.5350954359119839, 0.5291689781388270175, -13.89700978578772705 ) ) ;
#8153=CARTESIAN_POINT ( 'NONE',  ( 121.9659548109119811, -7.554583864224885481, -18.48844787311982785 ) ) ;
#8156=CARTESIAN_POINT ( 'NONE',  ( 122.0354079359119908, -5.444069387712269226, -19.60292469916370450 ) ) ;
#8175=ORIENTED_EDGE ( 'NONE', *, *, #29512, .F. ) ;
#8186=CARTESIAN_POINT ( 'NONE',  ( 121.1325173109119788, 0.2312338769422704887, -16.08380026872395874 ) ) ;
#8187=CARTESIAN_POINT ( 'NONE',  ( 121.4797829359119987, -4.283928203966213211, -7.183505701512925334 ) ) ;
#8188=CARTESIAN_POINT ( 'NONE',  ( 120.3988246589382243, -8.341213398351554176, -17.25835129106724608 ) ) ;
#8196=CARTESIAN_POINT ( 'NONE',  ( 122.6009548109119720, -12.48189245497263755, -10.95032834292243074 ) ) ;
#8255=CARTESIAN_POINT ( 'NONE',  ( 121.0630641859119976, -0.8832429491016019485, -18.19431474523657855 ) ) ;
#8268=CARTESIAN_POINT ( 'NONE',  ( 124.5884359875738170, -9.769705091392824059, -14.37932942410840198 ) ) ;
#8320=CARTESIAN_POINT ( 'NONE',  ( 125.0480389746924885, -6.045022021006678514, -5.955407747331282309 ) ) ;
#8322=( BOUNDED_CURVE ( )  B_SPLINE_CURVE ( 2, ( #3845, #20968, #7270, #17113, #17765, #35292, #31661, #4064, #17989, #31888, #29378, #35978, #40092, #42618, #11380, #35522, #8852 ),
 .UNSPECIFIED., .F., .T. ) 
 B_SPLINE_CURVE_WITH_KNOTS ( ( 3, 2, 2, 2, 2, 2, 2, 2, 3 ),
 ( 0.5102707595410509445, 0.5312500000000000000, 0.5625000000000000000, 0.5937500000000000000, 0.6250000000000000000, 0.6562500000000000000, 0.6875000000000000000, 0.7187500000000000000, 0.7397292404589489445 ),
 .UNSPECIFIED. ) 
 CURVE ( )  GEOMETRIC_REPRESENTATION_ITEM ( )  RATIONAL_B_SPLINE_CURVE ( ( 0.9664089390052280626, 0.9488976130786129781, 1.000000000000000000, 0.9238795325112869605, 1.000000000000000000, 0.9238795325112869605, 1.000000000000000000, 0.9238795325112869605, 1.000000000000000000, 0.9238795325112869605, 1.000000000000000000, 0.9238795325112869605, 1.000000000000000000, 0.9238795325112869605, 1.000000000000000000, 0.9488976130786129781, 0.9664089390052290618 ) ) 
 REPRESENTATION_ITEM ( '' )  );
#8327=B_SPLINE_CURVE_WITH_KNOTS ( 'NONE', 3,
 ( #34774, #41438, #17470, #6988, #23885, #30709, #24755, #28190 ),
 .UNSPECIFIED., .F., .F.,
 ( 4, 2, 2, 4 ),
 ( 0.000000000000000000, 0.2500000000000000000, 0.5000000000000000000, 1.000000000000000000 ),
 .UNSPECIFIED. ) ;
#8354=CARTESIAN_POINT ( 'NONE',  ( 121.0630641859119976, -8.321307733199551748, -9.223433127585318303 ) ) ;
#8365=EDGE_CURVE ( 'NONE', #26397, #31784, #5924, .T. ) ;
#8378=CARTESIAN_POINT ( 'NONE',  ( 123.3550173109119612, 0.2312338769422704887, -16.08380026872395874 ) ) ;
#8412=CARTESIAN_POINT ( 'NONE',  ( 120.9241579359119925, -5.444069387712269226, -19.60292469916370450 ) ) ;
#8413=CARTESIAN_POINT ( 'NONE',  ( 123.6328298109119714, -2.173413727453600508, -8.297982527556802879 ) ) ;
#8450=CARTESIAN_POINT ( 'NONE',  ( 120.9936110609119737, -6.340755971794695078, -8.611740276972781771 ) ) ;
#8454=EDGE_LOOP ( 'NONE', ( #23604, #18020, #38830, #17425 ) ) ;
#8480=CARTESIAN_POINT ( 'NONE',  ( 122.1743141859119817, -8.321307733199551748, -9.223433127585318303 ) ) ;
#8491=ORIENTED_EDGE ( 'NONE', *, *, #44553, .T. ) ;
#8544=CARTESIAN_POINT ( 'NONE',  ( 125.1028739313154148, -6.088305799123888917, -6.024550168534809735 ) ) ;
#8551=CARTESIAN_POINT ( 'NONE',  ( 123.2855641859119942, -8.321307733199551748, -9.223433127585318303 ) ) ;
#8618=CARTESIAN_POINT ( 'NONE',  ( 125.2748812523276598, -11.53675367988898159, -16.14795873962287232 ) ) ;
#8636=CARTESIAN_POINT ( 'NONE',  ( 122.2437673109119629, 0.2312338769422704887, -16.08380026872395874 ) ) ;
#8637=FACE_OUTER_BOUND ( 'NONE', #32018, .T. ) ;
#8700=CARTESIAN_POINT ( 'NONE',  ( 122.5215798109119874, -7.200787124940443817, -17.81845355600750835 ) ) ;
#8725=VERTEX_POINT ( 'NONE', #41944 ) ;
#8764=CARTESIAN_POINT ( 'NONE',  ( 125.2231329858104516, -7.806516698891761585, -6.696497996897097238 ) ) ;
#8771=CARTESIAN_POINT ( 'NONE',  ( 123.5633766859119760, -9.033780868592240054, -16.85052413769862056 ) ) ;
#8772=CIRCLE ( 'NONE', #18967, 8.000000000000001776 ) ;
#8810=B_SPLINE_CURVE_WITH_KNOTS ( 'NONE', 3,
 ( #30091, #39676, #22122, #2033, #23017, #19596, #36015, #43549 ),
 .UNSPECIFIED., .F., .F.,
 ( 4, 2, 2, 4 ),
 ( 0.000000000000000000, 0.2500000000000005551, 0.5000000000000011102, 1.000000000000000000 ),
 .UNSPECIFIED. ) ;
#8822=ORIENTED_EDGE ( 'NONE', *, *, #38675, .T. ) ;
#8823=CARTESIAN_POINT ( 'NONE',  ( 121.4797829359119987, -5.367793381288652910, -18.78638297431638904 ) ) ;
#8825=CARTESIAN_POINT ( 'NONE',  ( 122.1863582044368286, -6.247802574075781656, -18.73351920797576042 ) ) ;
#8826=CARTESIAN_POINT ( 'NONE',  ( 125.0532895624266416, 2.567537813723679285, -12.20844840518084240 ) ) ;
#8837=CARTESIAN_POINT ( 'NONE',  ( 124.5763124458833317, -11.88415338737963367, -16.94877137765329422 ) ) ;
#8841=ORIENTED_EDGE ( 'NONE', *, *, #8880, .T. ) ;
#8852=CARTESIAN_POINT ( 'NONE',  ( 122.4767535264548854, -8.247323210606174015, -17.08054893949881858 ) ) ;
#8856=CARTESIAN_POINT ( 'NONE',  ( 122.8688454359119646, -11.07370829466463569, -12.81314460846529002 ) ) ;
#8857=CARTESIAN_POINT ( 'NONE',  ( 120.7157985609119635, -10.36940331770106916, -15.09355782777062061 ) ) ;
#8880=EDGE_CURVE ( 'NONE', #32564, #29158, #23543, .T. ) ;
#8885=FACE_OUTER_BOUND ( 'NONE', #13769, .T. ) ;
#8895=CARTESIAN_POINT ( 'NONE',  ( 125.1416936109526716, -1.781206261049963491, -20.14521123147079606 ) ) ;
#8898=CARTESIAN_POINT ( 'NONE',  ( 122.5910329359119970, -5.367793381288652910, -18.78638297431638904 ) ) ;
#8912=CARTESIAN_POINT ( 'NONE',  ( 125.4584548109119737, -8.963735245270648022, -18.43723750849711962 ) ) ;
#8930=CARTESIAN_POINT ( 'NONE',  ( 123.1466579359119891, -5.444069387712269226, -19.60292469916370450 ) ) ;
#8934=ORIENTED_EDGE ( 'NONE', *, *, #6666, .F. ) ;
#8935=CARTESIAN_POINT ( 'NONE',  ( 124.2579079359120016, -4.360204210389833968, -8.000047426360245240 ) ) ;
#8998=CARTESIAN_POINT ( 'NONE',  ( 125.3563494635840954, -7.185071377748551313, -6.737895779717858247 ) ) ;
#9006=CARTESIAN_POINT ( 'NONE',  ( 123.2161110609119703, -6.340755971794695078, -8.611740276972781771 ) ) ;
#9027=CARTESIAN_POINT ( 'NONE',  ( 125.3303382280814589, 1.196307385452442196, -17.12740918756453112 ) ) ;
#9059=CARTESIAN_POINT ( 'NONE',  ( 124.7442371152539096, 2.096536125358192226, -9.913456651695405242 ) ) ;
#9066=CARTESIAN_POINT ( 'NONE',  ( 125.1679698639839273, -11.59951594357973725, -16.43112627289485062 ) ) ;
#9088=CARTESIAN_POINT ( 'NONE',  ( 120.2990798109119766, -7.200787124940443817, -17.81845355600750835 ) ) ;
#9089=CARTESIAN_POINT ( 'NONE',  ( 122.1743141859119817, -0.8832429491016019485, -18.19431474523657855 ) ) ;
#9091=CARTESIAN_POINT ( 'NONE',  ( 123.7325746589382192, -8.341213398351550623, -17.25835129106723542 ) ) ;
#9120=CARTESIAN_POINT ( 'NONE',  ( 125.3567159805640756, -2.805979814341523326, -20.12909359689052380 ) ) ;
#9123=CARTESIAN_POINT ( 'NONE',  ( 123.9106423109119675, -0.4387604401700512802, -15.73000352943951619 ) ) ;
#9156=EDGE_CURVE ( 'NONE', #13839, #43475, #7769, .T. ) ;
#9159=CARTESIAN_POINT ( 'NONE',  ( 124.1190016859119680, -9.665098340737509730, -17.37397104707595474 ) ) ;
#9163=CARTESIAN_POINT ( 'NONE',  ( 122.2437673109119629, -9.289237151508434209, -11.05642687123711276 ) ) ;
#9199=CARTESIAN_POINT ( 'NONE',  ( 120.3439060953690642, -6.001247023715329476, -18.26661038929047720 ) ) ;
#9200=CARTESIAN_POINT ( 'NONE',  ( 119.2572829359120021, -5.367793381288652910, -18.78638297431638904 ) ) ;
#9221=FACE_OUTER_BOUND ( 'NONE', #3208, .T. ) ;
#9227=FACE_OUTER_BOUND ( 'NONE', #38110, .T. ) ;
#9246=DIRECTION ( 'NONE',  ( 1.000000000000000000, 0.000000000000000000, 0.000000000000000000 ) ) ;
#9253=CARTESIAN_POINT ( 'NONE',  ( 125.1375072647520312, 1.201293586859333296, -17.68058412753241626 ) ) ;
#9284=CARTESIAN_POINT ( 'NONE',  ( 121.5492360609119800, -3.387241619883791355, -18.17469012370385073 ) ) ;
#9288=CARTESIAN_POINT ( 'NONE',  ( 122.0563581739442895, -4.756192495830085853, -19.39047411591440095 ) ) ;
#9293=CARTESIAN_POINT ( 'NONE',  ( 124.7127519260344997, -11.83533031758874898, -16.88573608159204653 ) ) ;
#9297=CARTESIAN_POINT ( 'NONE',  ( 119.7434548109119845, 0.09318999503389145678, -15.44192152833163334 ) ) ;
#9315=CARTESIAN_POINT ( 'NONE',  ( 123.2161110609119561, -3.163656168406935087, -18.89861972220014508 ) ) ;
#9316=CARTESIAN_POINT ( 'NONE',  ( 122.3826735609119680, -9.645473719204776586, -14.86997237629376656 ) ) ;
#9339=FACE_OUTER_BOUND ( 'NONE', #35606, .T. ) ;
#9345=CARTESIAN_POINT ( 'NONE',  ( 125.3503171566262324, -2.572797884969513671, -20.07118512341956063 ) ) ;
#9348=CARTESIAN_POINT ( 'NONE',  ( 122.1048610609119720, -6.340755971794695078, -8.611740276972781771 ) ) ;
#9383=CARTESIAN_POINT ( 'NONE',  ( 123.4244704359119709, -10.25716656981731489, -12.88942061488890545 ) ) ;
#9419=CARTESIAN_POINT ( 'NONE',  ( 123.1466579359119891, -4.360204210389833968, -8.000047426360245240 ) ) ;
#9505=CARTESIAN_POINT ( 'NONE',  ( 123.4939235609119663, -9.645473719204776586, -14.86997237629376656 ) ) ;
#9517=CARTESIAN_POINT ( 'NONE',  ( 119.7434548109119703, -0.2404488592019161652, -16.18068212994647226 ) ) ;
#9540=CARTESIAN_POINT ( 'NONE',  ( 123.3550173109119612, 0.2312338769422704887, -16.08380026872395874 ) ) ;
#9541=CARTESIAN_POINT ( 'NONE',  ( 121.8270485609119760, -0.08252387247370887580, -11.91645802438286417 ) ) ;
#9577=CARTESIAN_POINT ( 'NONE',  ( 124.7440798109119697, -7.200787124940443817, -17.81845355600750835 ) ) ;
#9594=CARTESIAN_POINT ( 'NONE',  ( 123.4244704359119709, 1.345710702986147034, -13.97328579221134603 ) ) ;
#9609=CARTESIAN_POINT ( 'NONE',  ( 122.1743141859119817, -0.8832429491016019485, -18.19431474523657855 ) ) ;
#9613=CARTESIAN_POINT ( 'NONE',  ( 123.4939235609119663, -9.645473719204776586, -14.86997237629376656 ) ) ;
#9642=ORIENTED_EDGE ( 'NONE', *, *, #18470, .T. ) ;
#9648=CARTESIAN_POINT ( 'NONE',  ( 119.4624673109119755, -0.4425889791249831839, -15.72798183378646186 ) ) ;
#9652=CARTESIAN_POINT ( 'NONE',  ( 122.5910329359119970, -5.367793381288652910, -18.78638297431638904 ) ) ;
#9671=CARTESIAN_POINT ( 'NONE',  ( 121.1325173109119788, -9.289237151508432433, -11.05642687123711276 ) ) ;
#9677=CARTESIAN_POINT ( 'NONE',  ( 121.6881423109119709, -0.4387604401700512802, -15.73000352943951619 ) ) ;
#9712=DIRECTION ( 'NONE',  ( -1.000000000000000000, 0.000000000000000000, -0.000000000000000000 ) ) ;
#9727=ORIENTED_EDGE ( 'NONE', *, *, #11666, .T. ) ;
#9735=CARTESIAN_POINT ( 'NONE',  ( 123.9138173109119663, -0.4425889791248522331, -15.72798183378621140 ) ) ;
#9749=AXIS2_PLACEMENT_3D ( 'NONE', #22591, #2913, #41243 ) ;
#9773=CARTESIAN_POINT ( 'NONE',  ( 123.1466579359119891, -4.360204210389833968, -8.000047426360245240 ) ) ;
#9774=CARTESIAN_POINT ( 'NONE',  ( 124.1190016859119680, -9.665098340737509730, -17.37397104707595474 ) ) ;
#9797=ORIENTED_EDGE ( 'NONE', *, *, #20886, .F. ) ;
#9811=CARTESIAN_POINT ( 'NONE',  ( 122.9382985609119743, -0.08252387247370887580, -11.91645802438286417 ) ) ;
#9831=CARTESIAN_POINT ( 'NONE',  ( 124.3404700565388907, -8.485573535863879968, -17.53172993199661889 ) ) ;
#9842=B_SPLINE_CURVE_WITH_KNOTS ( 'NONE', 3,
 ( #39852, #1536, #15228, #40303, #43275, #25946, #8837, #40073, #9293, #15913, #43953, #12271, #29136, #9066, #43048, #1986, #5628, #8618, #12495, #22968, #18657, #5180, #22736, #22515, #11815, #12716, #36859, #15457, #25723, #19549, #29811, #32763, #36638, #2206, #18872, #16135, #30036, #39629, #19097, #1758, #15684, #29586, #26619, #22297, #40532, #43727, #32546, #36193, #4958 ),
 .UNSPECIFIED., .F., .F.,
 ( 4, 2, 2, 2, 2, 2, 2, 2, 2, 1, 2, 2, 2, 2, 2, 2, 2, 1, 2, 2, 2, 2, 1, 2, 2, 4 ),
 ( 0.000000000000000000, 0.06250000000002639555, 0.1250000000000527911, 0.1875000000000791867, 0.2187500000000920375, 0.2500000000001049161, 0.3750000000001461609, 0.4375000000001676992, 0.4687500000001784684, 0.4843750000001839640, 0.4921875000001855738, 0.5000000000001870726, 0.5625000000001556533, 0.5937500000001373346, 0.6250000000001189049, 0.6875000000000800471, 0.7187500000000606182, 0.7343750000000504041, 0.7421875000000455191, 0.7500000000000407452, 0.8125000000000127676, 0.8437499999999957812, 0.8593749999999867883, 0.8671874999999870104, 0.8749999999999871214, 1.000000000000000000 ),
 .UNSPECIFIED. ) ;
#9843=CIRCLE ( 'NONE', #37483, 5.000000000000000000 ) ;
#9844=CARTESIAN_POINT ( 'NONE',  ( 124.0495485609119584, -10.36940331770106916, -15.09355782777062061 ) ) ;
#9849=CARTESIAN_POINT ( 'NONE',  ( 122.6604860609119640, -3.387241619883791355, -18.17469012370385073 ) ) ;
#9885=CARTESIAN_POINT ( 'NONE',  ( 119.6013735609119806, -0.08666061303654916392, -11.91773565553416425 ) ) ;
#9888=CARTESIAN_POINT ( 'NONE',  ( 122.9382985609119743, -0.08252387247370887580, -11.91645802438286417 ) ) ;
#9913=CARTESIAN_POINT ( 'NONE',  ( 123.7022829359119811, -5.367793381288652910, -18.78638297431638904 ) ) ;
#9923=CARTESIAN_POINT ( 'NONE',  ( 123.6808719482204992, -5.999156839134923480, -18.26265215102791117 ) ) ;
#9980=CARTESIAN_POINT ( 'NONE',  ( 124.1884548109119777, -2.527210466738289529, -8.967976844668992698 ) ) ;
#9984=CARTESIAN_POINT ( 'NONE',  ( 121.9750102976252180, -8.580000213326620440, -17.71054824844518905 ) ) ;
#9997=CARTESIAN_POINT ( 'NONE',  ( 120.2296266859119953, -0.06289925094097943703, -9.412459353600674206 ) ) ;
#10003=CARTESIAN_POINT ( 'NONE',  ( 122.9382985609119743, -0.08252387247370887580, -11.91645802438286417 ) ) ;
#10004=CARTESIAN_POINT ( 'NONE',  ( 120.0212673109119805, -9.289237151508434209, -11.05642687123711276 ) ) ;
#10031=CARTESIAN_POINT ( 'NONE',  ( 125.2726254169155595, -6.179026137057662460, -18.60327543567144204 ) ) ;
#10040=CARTESIAN_POINT ( 'NONE',  ( 121.9659548109119811, -7.554583864224885481, -18.48844787311982785 ) ) ;
#10043=EDGE_CURVE ( 'NONE', #34025, #2582, #25621, .T. ) ;
#10053=B_SPLINE_CURVE_WITH_KNOTS ( 'NONE', 3,
 ( #1078, #4266, #42586, #35261, #11800, #18856, #627, #1521, #38921, #25484 ),
 .UNSPECIFIED., .F., .F.,
 ( 4, 3, 3, 4 ),
 ( 7.296002358821220333E-16, 1.415135068336139897E-06, 2.830270136673649871E-06, 5.511645062456799864E-06 ),
 .UNSPECIFIED. ) ;
#10058=CARTESIAN_POINT ( 'NONE',  ( 124.5059548109119731, -4.863998795839242995, -13.39321520033831447 ) ) ;
#10078=CARTESIAN_POINT ( 'NONE',  ( 120.9241579359119925, -5.444069387712269226, -19.60292469916370450 ) ) ;
#10087=DIRECTION ( 'NONE',  ( -1.000000000000000000, 0.000000000000000000, -0.000000000000000000 ) ) ;
#10138=CARTESIAN_POINT ( 'NONE',  ( 124.3273610609119686, -6.340755971794695078, -8.611740276972781771 ) ) ;
#10217=CARTESIAN_POINT ( 'NONE',  ( 122.3826735609119680, 0.6414057260225851653, -11.69287257290600657 ) ) ;
#10222=CARTESIAN_POINT ( 'NONE',  ( 122.5910329359119970, -5.367793381288652910, -18.78638297431638904 ) ) ;
#10223=CARTESIAN_POINT ( 'NONE',  ( 122.2437673109119629, -9.289237151508434209, -11.05642687123711276 ) ) ;
#10241=CARTESIAN_POINT ( 'NONE',  ( 120.7157985609119635, -10.36940331770106916, -15.09355782777062061 ) ) ;
#10249=DIRECTION ( 'NONE',  ( 1.000000000000000000, 0.000000000000000000, 0.000000000000000000 ) ) ;
#10256=CARTESIAN_POINT ( 'NONE',  ( 121.7575954359119805, -11.07370829466463569, -12.81314460846529002 ) ) ;
#10272=CARTESIAN_POINT ( 'NONE',  ( 123.8411891859119862, -8.844754642576873493, -8.592115655440052180 ) ) ;
#10294=PRODUCT ( 'Adjuster Locknut', 'Adjuster Locknut', '', ( #7685 ) ) ;
#10296=CARTESIAN_POINT ( 'NONE',  ( 122.7299391859119737, -8.844754642576884152, -8.592115655440050404 ) ) ;
#10326=ORIENTED_EDGE ( 'NONE', *, *, #35612, .T. ) ;
#10332=CARTESIAN_POINT ( 'NONE',  ( 120.1601735609119856, -9.645473719204776586, -14.86997237629376656 ) ) ;
#10359=CARTESIAN_POINT ( 'NONE',  ( 121.2714235609119697, -9.645473719204776586, -14.86997237629376656 ) ) ;
#10362=CARTESIAN_POINT ( 'NONE',  ( 123.9584548109119737, 3.074545301078819737, -12.40350937470759973 ) ) ;
#10375=EDGE_LOOP ( 'NONE', ( #2289, #25120, #18961, #10801 ) ) ;
#10440=CARTESIAN_POINT ( 'NONE',  ( 122.5215798109119874, -2.173413727453600508, -8.297982527556802879 ) ) ;
#10446=CARTESIAN_POINT ( 'NONE',  ( 122.8688454359119646, 0.5291689781388270175, -13.89700978578772705 ) ) ;
#10454=SURFACE_STYLE_FILL_AREA ( #28448 ) ;
#10465=CARTESIAN_POINT ( 'NONE',  ( 120.3685329359119862, -4.283928203966213211, -7.183505701512925334 ) ) ;
#10472=CARTESIAN_POINT ( 'NONE',  ( 125.0949563211859754, -6.092355046118379747, -18.43914408017989004 ) ) ;
#10478=CARTESIAN_POINT ( 'NONE',  ( 120.9842687714537988, -6.306599966548167124, -18.84486539759072699 ) ) ;
#10513=CARTESIAN_POINT ( 'NONE',  ( 124.0495485609119584, -10.36940331770106916, -15.09355782777062061 ) ) ;
#10551=CARTESIAN_POINT ( 'NONE',  ( 119.7434548109119703, -2.527210466738041728, -8.967976844669124148 ) ) ;
#10579=CARTESIAN_POINT ( 'NONE',  ( 121.4103298109119748, -7.200787124940443817, -17.81845355600750835 ) ) ;
#10582=CARTESIAN_POINT ( 'NONE',  ( 119.7434548109119703, -2.564829167770875884, -8.950426663462648591 ) ) ;
#10589=CARTESIAN_POINT ( 'NONE',  ( 125.1630841924336295, -7.152576104508079347, -20.44691296307176387 ) ) ;
#10619=EDGE_LOOP ( 'NONE', ( #10326, #44174, #6008, #24994 ) ) ;
#10644=CARTESIAN_POINT ( 'NONE',  ( 124.5059548109119731, -4.863998795839242995, -13.39321520033831447 ) ) ;
#10661=CARTESIAN_POINT ( 'NONE',  ( 120.7157985609119635, -10.36940331770106916, -15.09355782777062061 ) ) ;
#10670=ORIENTED_EDGE ( 'NONE', *, *, #27590, .T. ) ;
#10682=ORIENTED_EDGE ( 'NONE', *, *, #34847, .T. ) ;
#10727=DIRECTION ( 'NONE',  ( 1.000000000000000000, 0.000000000000000000, 0.000000000000000000 ) ) ;
#10798=CARTESIAN_POINT ( 'NONE',  ( 124.5592491210230435, -9.863888965223885918, -13.51979257824428871 ) ) ;
#10799=EDGE_CURVE ( 'NONE', #16241, #38271, #32739, .T. ) ;
#10801=ORIENTED_EDGE ( 'NONE', *, *, #40662, .F. ) ;
#10862=DIRECTION ( 'NONE',  ( 0.000000000000000000, -0.4669533266896293000, -0.8842819633428516957 ) ) ;
#10883=CARTESIAN_POINT ( 'NONE',  ( 120.6463454359119822, -11.07370829466463569, -12.81314460846529002 ) ) ;
#10905=CARTESIAN_POINT ( 'NONE',  ( 119.3961891859119930, -1.406689858478933353, -17.56299727309130887 ) ) ;
#10918=CARTESIAN_POINT ( 'NONE',  ( 119.7434548109119703, -12.80254289275730173, -14.38292102596908784 ) ) ;
#10922=CARTESIAN_POINT ( 'NONE',  ( 122.6009548109119720, 1.449227268523328505, -18.30678586333412738 ) ) ;
#10924=VERTEX_POINT ( 'NONE', #44975 ) ;
#10931=ORIENTED_EDGE ( 'NONE', *, *, #20330, .F. ) ;
#10978=ORIENTED_EDGE ( 'NONE', *, *, #36456, .T. ) ;
#11010=CARTESIAN_POINT ( 'NONE',  ( 120.8547048109119686, -2.527210466738041728, -8.967976844669124148 ) ) ;
#11023=CARTESIAN_POINT ( 'NONE',  ( 124.5466134613335214, -9.859322667160077103, -13.15779651595278565 ) ) ;
#11024=CARTESIAN_POINT ( 'NONE',  ( 122.7993923109119692, -9.959231468620755479, -10.70263013195267199 ) ) ;
#11033=CARTESIAN_POINT ( 'NONE',  ( 125.2713867217341885, -7.074789275518575948, -20.29960597128161837 ) ) ;
#11051=CIRCLE ( 'NONE', #111, 5.000000000000000000 ) ;
#11067=VERTEX_POINT ( 'NONE', #15512 ) ;
#11105=CARTESIAN_POINT ( 'NONE',  ( 122.0354079359119908, -4.360204210389833968, -8.000047426360245240 ) ) ;
#11115=ORIENTED_EDGE ( 'NONE', *, *, #8880, .F. ) ;
#11129=CARTESIAN_POINT ( 'NONE',  ( 119.7434548109119703, -2.527210466738041728, -8.967976844669124148 ) ) ;
#11225=ORIENTED_EDGE ( 'NONE', *, *, #16779, .T. ) ;
#11234=CARTESIAN_POINT ( 'NONE',  ( 123.8411891859119862, -1.406689858478933353, -17.56299727309130887 ) ) ;
#11238=FACE_OUTER_BOUND ( 'NONE', #22988, .T. ) ;
#11244=ORIENTED_EDGE ( 'NONE', *, *, #27590, .F. ) ;
#11248=CARTESIAN_POINT ( 'NONE',  ( 123.4244704359119709, 1.345710702986147034, -13.97328579221134426 ) ) ;
#11251=CARTESIAN_POINT ( 'NONE',  ( 125.0480389746927159, -0.4397842399129161528, -7.298781581902527904 ) ) ;
#11328=CARTESIAN_POINT ( 'NONE',  ( 120.2296266859119953, -9.033780868592240054, -16.85052413769862056 ) ) ;
#11336=ORIENTED_EDGE ( 'NONE', *, *, #6443, .F. ) ;
#11346=CARTESIAN_POINT ( 'NONE',  ( 120.3685329359119862, -4.283928203966213211, -7.183505701512925334 ) ) ;
#11351=CARTESIAN_POINT ( 'NONE',  ( 120.3685329359119862, -5.367793381288652910, -18.78638297431638904 ) ) ;
#11361=CARTESIAN_POINT ( 'NONE',  ( 124.5219894712939919, -9.778352389574830994, -12.46904186487667054 ) ) ;
#11380=CARTESIAN_POINT ( 'NONE',  ( 122.3826735609119680, -9.645473719204778362, -14.86997237629376123 ) ) ;
#11386=CARTESIAN_POINT ( 'NONE',  ( 121.8270485609119760, -10.36940331770106916, -15.09355782777062061 ) ) ;
#11404=ORIENTED_EDGE ( 'NONE', *, *, #13912, .F. ) ;
#11430=CARTESIAN_POINT ( 'NONE',  ( 120.9241579359119925, -4.360204210389833968, -8.000047426360245240 ) ) ;
#11464=CARTESIAN_POINT ( 'NONE',  ( 123.4939235609119663, -9.645473719204776586, -14.86997237629376656 ) ) ;
#11477=CARTESIAN_POINT ( 'NONE',  ( 124.5359554805749269, -9.835730394904578233, -12.85701071798697015 ) ) ;
#11481=CARTESIAN_POINT ( 'NONE',  ( 124.9063227527172160, -0.2774853123688953982, -7.249199867253821594 ) ) ;
#11487=CARTESIAN_POINT ( 'NONE',  ( 119.7434548109119703, -12.36944789948969614, -14.53642012792675509 ) ) ;
#11504=ORIENTED_EDGE ( 'NONE', *, *, #36012, .T. ) ;
#11508=DIRECTION ( 'NONE',  ( -1.000000000000000000, 0.000000000000000000, -0.000000000000000000 ) ) ;
#11539=CARTESIAN_POINT ( 'NONE',  ( 122.4767535264548854, -8.247323210606174015, -17.08054893949881858 ) ) ;
#11557=CARTESIAN_POINT ( 'NONE',  ( 120.5074391859119913, -1.406689858478933353, -17.56299727309130887 ) ) ;
#11575=CARTESIAN_POINT ( 'NONE',  ( 120.9936110609119737, -3.163656168406935087, -18.89861972220014508 ) ) ;
#11578=CARTESIAN_POINT ( 'NONE',  ( 122.2437673109119629, 0.2312338769422704887, -16.08380026872395874 ) ) ;
#11590=CARTESIAN_POINT ( 'NONE',  ( 125.2231329858062594, -11.67996730509178249, -10.73859541710734788 ) ) ;
#11607=CARTESIAN_POINT ( 'NONE',  ( 119.8823610609119754, -3.163656168406935087, -18.89861972220014508 ) ) ;
#11662=CARTESIAN_POINT ( 'NONE',  ( 120.1993349628857146, -6.095137211460705196, -18.44441274085889049 ) ) ;
#11666=EDGE_CURVE ( 'NONE', #4044, #13839, #36413, .T. ) ;
#11674=EDGE_CURVE ( 'NONE', #31995, #42647, #8322, .T. ) ;
#11681=CARTESIAN_POINT ( 'NONE',  ( 119.7434548109119703, -7.554583864224885481, -18.48844787311982785 ) ) ;
#11683=DIRECTION ( 'NONE',  ( -1.000000000000000000, 0.000000000000000000, -0.000000000000000000 ) ) ;
#11693=CARTESIAN_POINT ( 'NONE',  ( 124.5623748110993319, -9.860959602566504500, -13.61026352087490565 ) ) ;
#11695=VERTEX_POINT ( 'NONE', #43290 ) ;
#11746=CARTESIAN_POINT ( 'NONE',  ( 125.1589444732324807, -6.145249445731414184, -6.105551253155266700 ) ) ;
#11779=CARTESIAN_POINT ( 'NONE',  ( 120.3685329359119862, -5.367793381288652910, -18.78638297431638904 ) ) ;
#11800=CARTESIAN_POINT ( 'NONE',  ( 123.6797710478795835, -5.999872392221376138, -18.26400721298383800 ) ) ;
#11801=ORIENTED_EDGE ( 'NONE', *, *, #23916, .T. ) ;
#11802=CARTESIAN_POINT ( 'NONE',  ( 120.9241579359119925, -4.360204210389833968, -8.000047426360245240 ) ) ;
#11815=CARTESIAN_POINT ( 'NONE',  ( 125.3417925815060698, -11.53121377071529530, -15.77642740804299493 ) ) ;
#11835=CARTESIAN_POINT ( 'NONE',  ( 120.4379860609119675, -6.564341423271550902, -7.887810678476487425 ) ) ;
#11836=CARTESIAN_POINT ( 'NONE',  ( 121.6186891859119896, -8.844754642576884152, -8.592115655440050404 ) ) ;
#11837=CARTESIAN_POINT ( 'NONE',  ( 124.1497896737536877, -8.611453504372539314, -17.77011218421760574 ) ) ;
#11844=EDGE_CURVE ( 'NONE', #2582, #29158, #40974, .T. ) ;
#11871=CARTESIAN_POINT ( 'NONE',  ( 124.7803599147174367, -3.802325732078021492, -21.07728963076554862 ) ) ;
#11874=CARTESIAN_POINT ( 'NONE',  ( 120.5768923109119868, -0.4387604401700512802, -15.73000352943951619 ) ) ;
#11890=CARTESIAN_POINT ( 'NONE',  ( 119.7692287164846476, -6.356880537135879194, -18.94008305455118801 ) ) ;
#11906=CARTESIAN_POINT ( 'NONE',  ( 124.2579079359120016, -4.360204210389833968, -8.000047426360245240 ) ) ;
#11907=VECTOR ( 'NONE', #1302, 999.9999999999998863 ) ;
#11972=CARTESIAN_POINT ( 'NONE',  ( 123.9584548109119737, -5.853704621469987934, -5.454671103420249523 ) ) ;
#11978=CARTESIAN_POINT ( 'NONE',  ( 123.4244704359119709, -10.25716656981731489, -12.88942061488890545 ) ) ;
#11999=CARTESIAN_POINT ( 'NONE',  ( 124.7472578386058615, 1.330726760588684332, -18.10008909799004329 ) ) ;
#12005=CARTESIAN_POINT ( 'NONE',  ( 120.6463454359119822, 0.5291689781388270175, -13.89700978578772705 ) ) ;
#12044=B_SPLINE_CURVE_WITH_KNOTS ( 'NONE', 3,
 ( #44207, #11890, #1167, #4358 ),
 .UNSPECIFIED., .F., .F.,
 ( 4, 4 ),
 ( 4.131326245856534688E-18, 6.689972255565380249E-05 ),
 .UNSPECIFIED. ) ;
#12065=CARTESIAN_POINT ( 'NONE',  ( 120.0212673109119805, 0.2312338769422704887, -16.08380026872395874 ) ) ;
#12094=CARTESIAN_POINT ( 'NONE',  ( 124.9868051361299166, -1.575707845324203493, -20.23615509330177531 ) ) ;
#12096=CARTESIAN_POINT ( 'NONE',  ( 125.3553822467254122, -2.689292442315842191, -20.09621397316101366 ) ) ;
#12131=CARTESIAN_POINT ( 'NONE',  ( 124.4662673109119737, -9.289237151508434209, -11.05642687123711276 ) ) ;
#12135=ORIENTED_EDGE ( 'NONE', *, *, #41766, .T. ) ;
#12136=CARTESIAN_POINT ( 'NONE',  ( 120.5768923109119868, -0.4387604401700512802, -15.73000352943951619 ) ) ;
#12146=AXIS2_PLACEMENT_3D ( 'NONE', #29408, #40350, #19594 ) ;
#12219=ORIENTED_EDGE ( 'NONE', *, *, #1152, .T. ) ;
#12249=ADVANCED_FACE ( 'NONE', ( #31616 ), #39211, .F. ) ;
#12259=CARTESIAN_POINT ( 'NONE',  ( 123.9584548109119737, -4.863998795839242995, -13.39321520033831447 ) ) ;
#12261=CARTESIAN_POINT ( 'NONE',  ( 122.3736205389825216, -6.126425863531494542, -18.50366489541501380 ) ) ;
#12262=CARTESIAN_POINT ( 'NONE',  ( 124.8633137343409771, 2.042755831848476866, -9.994361272893446113 ) ) ;
#12269=CARTESIAN_POINT ( 'NONE',  ( 121.4797829359119987, -4.283928203966219428, -7.183505701512921782 ) ) ;
#12271=CARTESIAN_POINT ( 'NONE',  ( 124.9558295300363966, -11.72760118899441117, -16.72555640187829340 ) ) ;
#12290=CARTESIAN_POINT ( 'NONE',  ( 122.6604860609119640, -6.564341423271550902, -7.887810678476487425 ) ) ;
#12291=CARTESIAN_POINT ( 'NONE',  ( 122.0354079359119908, -5.444069387712269226, -19.60292469916370450 ) ) ;
#12292=CARTESIAN_POINT ( 'NONE',  ( 123.8772847346423163, -8.435056900666539903, -17.43606523319152757 ) ) ;
#12308=EDGE_LOOP ( 'NONE', ( #30166, #18888, #31604, #10931 ) ) ;
#12312=CARTESIAN_POINT ( 'NONE',  ( 120.2542535264548889, -8.247323210606168686, -17.08054893949881148 ) ) ;
#12321=CARTESIAN_POINT ( 'NONE',  ( 124.9764995119678730, -3.726932892905140182, -20.90982082926597840 ) ) ;
#12324=CARTESIAN_POINT ( 'NONE',  ( 120.0907204359119760, 1.345710702986147034, -13.97328579221134426 ) ) ;
#12338=CARTESIAN_POINT ( 'NONE',  ( 124.3522778485100702, -9.656977264654683424, -19.75004840186534949 ) ) ;
#12339=CARTESIAN_POINT ( 'NONE',  ( 124.2579079359119731, -4.360204210389825086, -8.000047426360248792 ) ) ;
#12357=CARTESIAN_POINT ( 'NONE',  ( 123.7717360609119623, -6.564341423271550902, -7.887810678476487425 ) ) ;
#12364=CARTESIAN_POINT ( 'NONE',  ( 122.0354079359119908, -4.360204210389833968, -8.000047426360245240 ) ) ;
#12375=AXIS2_PLACEMENT_3D ( 'NONE', #42185, #21649, #10727 ) ;
#12423=CARTESIAN_POINT ( 'NONE',  ( 124.4646854081441631, -8.458298358070186040, -6.340390706684574162 ) ) ;
#12430=CARTESIAN_POINT ( 'NONE',  ( 122.7299391859119737, -1.406689858478933353, -17.56299727309130887 ) ) ;
#12442=CARTESIAN_POINT ( 'NONE',  ( 122.7177766009169204, -8.403782945130243931, -17.37684090985457885 ) ) ;
#12452=CARTESIAN_POINT ( 'NONE',  ( 124.4646854081411362, 2.664654824213256834, -15.83876163224986655 ) ) ;
#12457=LINE ( 'NONE', #15645, #24096 ) ;
#12485=CARTESIAN_POINT ( 'NONE',  ( 124.1685108350118725, 2.242028142391200518, -9.741928829300908532 ) ) ;
#12495=CARTESIAN_POINT ( 'NONE',  ( 125.2832423080317881, -11.53285783966026834, -16.11696395382945113 ) ) ;
#12516=CARTESIAN_POINT ( 'NONE',  ( 120.1601735609119856, -9.645473719204776586, -14.86997237629376656 ) ) ;
#12517=CARTESIAN_POINT ( 'NONE',  ( 121.0630641859119976, -0.8832429491016019485, -18.19431474523657855 ) ) ;
#12547=CARTESIAN_POINT ( 'NONE',  ( 125.3005380000369371, -2.213024231627517491, -20.05538928696255851 ) ) ;
#12550=CARTESIAN_POINT ( 'NONE',  ( 122.3132204359119868, -10.25716656981731489, -12.88942061488890545 ) ) ;
#12586=CARTESIAN_POINT ( 'NONE',  ( 123.4244704359119709, 1.345710702986147034, -13.97328579221134426 ) ) ;
#12591=CARTESIAN_POINT ( 'NONE',  ( 123.7022829359119811, -5.367793381288652910, -18.78638297431638904 ) ) ;
#12621=B_SPLINE_CURVE_WITH_KNOTS ( 'NONE', 3,
 ( #21227, #7535, #15279, #24648, #38764, #35106, #3888, #17808, #35562, #690 ),
 .UNSPECIFIED., .F., .F.,
 ( 4, 3, 3, 4 ),
 ( 0.000000000000000000, 0.0002476486808869835118, 0.0004952973797228650337, 0.0009539399846111519445 ),
 .UNSPECIFIED. ) ;
#12631=CARTESIAN_POINT ( 'NONE',  ( 120.7503284624957729, -6.270977643812245539, -18.77740645536395547 ) ) ;
#12654=CARTESIAN_POINT ( 'NONE',  ( 124.7442371152529006, -8.343757344481284477, -6.432680279141536950 ) ) ;
#12707=CARTESIAN_POINT ( 'NONE',  ( 123.1466579359119891, -4.360204210389833968, -8.000047426360245240 ) ) ;
#12711=PRODUCT_DEFINITION ( 'UNKNOWN', '', #4558, #39259 ) ;
#12712=CARTESIAN_POINT ( 'NONE',  ( 122.4521266859119777, -0.06289925094098039460, -9.412459353600686640 ) ) ;
#12716=CARTESIAN_POINT ( 'NONE',  ( 125.3455228489891198, -11.53585155397754924, -15.73626133961844609 ) ) ;
#12739=CARTESIAN_POINT ( 'NONE',  ( 120.6463454359119822, 0.5291689781388270175, -13.89700978578772705 ) ) ;
#12740=CARTESIAN_POINT ( 'NONE',  ( 122.3826735609119680, 0.6414057260225851653, -11.69287257290600657 ) ) ;
#12758=EDGE_CURVE ( 'NONE', #7750, #30137, #22972, .T. ) ;
#12759=EDGE_CURVE ( 'NONE', #23986, #25646, #23449, .T. ) ;
#12773=CARTESIAN_POINT ( 'NONE',  ( 125.3563243388396984, -2.728216552653024873, -20.10610198443428231 ) ) ;
#12776=CARTESIAN_POINT ( 'NONE',  ( 122.1743141859119817, -8.321307733199551748, -9.223433127585318303 ) ) ;
#12801=CYLINDRICAL_SURFACE ( 'NONE', #505, 1.587500000000000355 ) ;
#12817=CARTESIAN_POINT ( 'NONE',  ( 124.4662673109119737, -9.289237151508434209, -11.05642687123711276 ) ) ;
#12857=CARTESIAN_POINT ( 'NONE',  ( 122.6604860609119640, -3.387241619883791355, -18.17469012370385073 ) ) ;
#12878=CARTESIAN_POINT ( 'NONE',  ( 120.7157985609119635, -0.08252387247371148482, -11.91645802438286772 ) ) ;
#12893=ORIENTED_EDGE ( 'NONE', *, *, #34453, .T. ) ;
#12916=DIRECTION ( 'NONE',  ( 1.000000000000000000, 0.000000000000000000, 0.000000000000000000 ) ) ;
#12938=CARTESIAN_POINT ( 'NONE',  ( 121.2714235609119697, -9.645473719204776586, -14.86997237629376656 ) ) ;
#12945=CARTESIAN_POINT ( 'NONE',  ( 120.8933699480702586, -6.365377317481695663, -18.95617363400926081 ) ) ;
#12946=CARTESIAN_POINT ( 'NONE',  ( 123.0077516859119839, -0.6942167230862511529, -9.935906262978004833 ) ) ;
#12950=CARTESIAN_POINT ( 'NONE',  ( 124.5388954359119822, -10.25250061710393190, -12.88985647778305932 ) ) ;
#12952=CARTESIAN_POINT ( 'NONE',  ( 119.7434548109119845, 0.2675062114431748794, -12.38956156844279910 ) ) ;
#12962=CARTESIAN_POINT ( 'NONE',  ( 123.9584548109119737, -12.80254289275730173, -14.38292102596908784 ) ) ;
#12971=CARTESIAN_POINT ( 'NONE',  ( 119.2572829359120021, -5.367793381288652910, -18.78638297431638904 ) ) ;
#12972=CARTESIAN_POINT ( 'NONE',  ( 121.2714235609119697, -9.645473719204776586, -14.86997237629376656 ) ) ;
#13003=CARTESIAN_POINT ( 'NONE',  ( 124.0495485609119584, -0.08252387247370887580, -11.91645802438286417 ) ) ;
#13020=DIRECTION ( 'NONE',  ( 1.000000000000000000, 0.000000000000000000, 0.000000000000000000 ) ) ;
#13034=CARTESIAN_POINT ( 'NONE',  ( 124.1884548109119777, -7.554583864224885481, -18.48844787311982785 ) ) ;
#13038=CARTESIAN_POINT ( 'NONE',  ( 121.6881423109119709, -0.4387604401700512802, -15.73000352943951619 ) ) ;
#13050=EDGE_CURVE ( 'NONE', #45054, #7584, #18448, .T. ) ;
#13062=CARTESIAN_POINT ( 'NONE',  ( 125.4584548109119737, -4.863998795839242995, -13.39321520033831447 ) ) ;
#13077=CARTESIAN_POINT ( 'NONE',  ( 123.4366330209070099, -6.157706758239399392, -18.56290235964623392 ) ) ;
#13081=VERTEX_POINT ( 'NONE', #3842 ) ;
#13103=CARTESIAN_POINT ( 'NONE',  ( 123.1466579359119891, -4.360204210389833968, -8.000047426360245240 ) ) ;
#13159=ORIENTED_EDGE ( 'NONE', *, *, #18470, .F. ) ;
#13173=DIRECTION ( 'NONE',  ( -1.000000000000000000, 0.000000000000000000, -0.000000000000000000 ) ) ;
#13174=CARTESIAN_POINT ( 'NONE',  ( 123.8411891859119862, -1.406689858478695543, -17.56299727309111347 ) ) ;
#13197=CARTESIAN_POINT ( 'NONE',  ( 121.6881423109119709, -0.4387604401700512802, -15.73000352943951619 ) ) ;
#13198=CARTESIAN_POINT ( 'NONE',  ( 122.5910329359119970, -5.367793381288652910, -18.78638297431638904 ) ) ;
#13208=LINE ( 'NONE', #23697, #27911 ) ;
#13222=DIRECTION ( 'NONE',  ( 0.000000000000000000, -0.4669533266896289669, -0.8842819633428519177 ) ) ;
#13229=CARTESIAN_POINT ( 'NONE',  ( 121.2019704359119743, -10.25716656981731489, -12.88942061488890545 ) ) ;
#13247=CARTESIAN_POINT ( 'NONE',  ( 124.0495485609119584, -10.36940331770107093, -15.09355782777061350 ) ) ;
#13259=ORIENTED_EDGE ( 'NONE', *, *, #38644, .T. ) ;
#13260=CARTESIAN_POINT ( 'NONE',  ( 123.2161110609119561, -3.163656168406935087, -18.89861972220014508 ) ) ;
#13264=CARTESIAN_POINT ( 'NONE',  ( 122.4521266859119635, -9.033780868592240054, -16.85052413769862056 ) ) ;
#13270=VERTEX_POINT ( 'NONE', #17763 ) ;
#13285=EDGE_LOOP ( 'NONE', ( #568, #28012, #40340, #30867 ) ) ;
#13300=CARTESIAN_POINT ( 'NONE',  ( 119.5319204359119993, 0.5245030254254168245, -13.89657392289387516 ) ) ;
#13302=VECTOR ( 'NONE', #15039, 1000.000000000000000 ) ;
#13305=ORIENTED_EDGE ( 'NONE', *, *, #35388, .T. ) ;
#13317=STYLED_ITEM ( 'NONE', ( #31403 ), #6345 ) ;
#13333=CARTESIAN_POINT ( 'NONE',  ( 124.3968141859119783, -8.321307733199551748, -9.223433127585318303 ) ) ;
#13358=DIRECTION ( 'NONE',  ( -1.000000000000000000, 0.000000000000000000, -0.000000000000000000 ) ) ;
#13396=CARTESIAN_POINT ( 'NONE',  ( 121.4618602343419411, -8.309924745830986836, -17.19909913565936321 ) ) ;
#13397=( BOUNDED_CURVE ( )  B_SPLINE_CURVE ( 2, ( #27736, #24317, #23416, #34109, #9735, #19763, #2879, #30923, #30473 ),
 .UNSPECIFIED., .F., .F. ) 
 B_SPLINE_CURVE_WITH_KNOTS ( ( 3, 2, 2, 2, 3 ),
 ( 0.04111889706057585137, 0.1249999999999965999, 0.2499999999999915068, 0.3749999999999864553, 0.4999999999999819589 ),
 .UNSPECIFIED. ) 
 CURVE ( )  GEOMETRIC_REPRESENTATION_ITEM ( )  RATIONAL_B_SPLINE_CURVE ( ( 0.9663939858628909363, 0.9489194498462569793, 1.000000000000000000, 0.9238795325112869605, 1.000000000000000000, 0.9238795325112869605, 1.000000000000000000, 0.9238795325112979517, 0.9999999999999890088 ) ) 
 REPRESENTATION_ITEM ( '' )  );
#13401=CARTESIAN_POINT ( 'NONE',  ( 122.5664060953690466, -6.001247023715324147, -18.26661038929047010 ) ) ;
#13403=CARTESIAN_POINT ( 'NONE',  ( 124.2610829359120004, -4.360640073283988727, -8.004713379073630009 ) ) ;
#13423=CARTESIAN_POINT ( 'NONE',  ( 123.4244704359119709, -10.25716656981731489, -12.88942061488890545 ) ) ;
#13424=CARTESIAN_POINT ( 'NONE',  ( 121.0630641859119976, -8.321307733199551748, -9.223433127585318303 ) ) ;
#13432=CARTESIAN_POINT ( 'NONE',  ( 120.2537320239009375, -8.246984259551265239, -17.07990705884998661 ) ) ;
#13441=CARTESIAN_POINT ( 'NONE',  ( 121.1325173109119788, 0.2312338769422704887, -16.08380026872395874 ) ) ;
#13447=DIRECTION ( 'NONE',  ( -1.000000000000000000, 0.000000000000000000, -0.000000000000000000 ) ) ;
#13456=CARTESIAN_POINT ( 'NONE',  ( 121.2714235609119697, 0.6414057260225851653, -11.69287257290600657 ) ) ;
#13473=CARTESIAN_POINT ( 'NONE',  ( 123.2161110609119561, -3.163656168406935087, -18.89861972220014508 ) ) ;
#13476=DIRECTION ( 'NONE',  ( -1.000000000000000000, 0.000000000000000000, -0.000000000000000000 ) ) ;
#13492=CARTESIAN_POINT ( 'NONE',  ( 123.1466579359119891, -5.444069387712269226, -19.60292469916370450 ) ) ;
#13502=CARTESIAN_POINT ( 'NONE',  ( 122.6009548109119720, -12.80254289275730173, -14.38292102596908784 ) ) ;
#13528=CIRCLE ( 'NONE', #18584, 1.587500000000000355 ) ;
#13541=ORIENTED_EDGE ( 'NONE', *, *, #35642, .F. ) ;
#13546=CARTESIAN_POINT ( 'NONE',  ( 121.3168205993907378, -9.245649465415475277, -16.16453161350214884 ) ) ;
#13552=CARTESIAN_POINT ( 'NONE',  ( 119.8823610609119754, -3.163656168406935087, -18.89861972220014508 ) ) ;
#13555=CARTESIAN_POINT ( 'NONE',  ( 124.3692356341887830, 2.211163780387002564, -9.774729780252799927 ) ) ;
#13593=TOROIDAL_SURFACE ( 'NONE', #44185, 5.952500000000000568, 0.9525000000000000133 ) ;
#13635=CARTESIAN_POINT ( 'NONE',  ( 122.3132204359119868, 1.345710702986147034, -13.97328579221134426 ) ) ;
#13642=CARTESIAN_POINT ( 'NONE',  ( 121.4103298109119748, -7.200787124940443817, -17.81845355600750835 ) ) ;
#13643=CARTESIAN_POINT ( 'NONE',  ( 121.3408766859119794, -9.033780868592240054, -16.85052413769862056 ) ) ;
#13653=LINE ( 'NONE', #34376, #25721 ) ;
#13677=CARTESIAN_POINT ( 'NONE',  ( 120.5074391859119913, -8.844754642576884152, -8.592115655440050404 ) ) ;
#13684=EDGE_CURVE ( 'NONE', #43772, #11695, #40231, .T. ) ;
#13693=CARTESIAN_POINT ( 'NONE',  ( 123.5633766859119618, -0.06289925094098414160, -9.412459353600670653 ) ) ;
#13714=CARTESIAN_POINT ( 'NONE',  ( 122.3132204359119868, 1.345710702986147034, -13.97328579221134426 ) ) ;
#13744=ORIENTED_EDGE ( 'NONE', *, *, #39832, .F. ) ;
#13750=CARTESIAN_POINT ( 'NONE',  ( 120.0875454359120056, -10.25250061710389282, -12.88985647778275911 ) ) ;
#13765=CARTESIAN_POINT ( 'NONE',  ( 120.4379860609119675, -3.387241619883791355, -18.17469012370385073 ) ) ;
#13769=EDGE_LOOP ( 'NONE', ( #26499, #44506, #39321, #12219 ) ) ;
#13775=CARTESIAN_POINT ( 'NONE',  ( 120.5074391859119913, -8.844754642576884152, -8.592115655440050404 ) ) ;
#13778=CARTESIAN_POINT ( 'NONE',  ( 125.2512653913870082, 2.257127252030525000, -11.96997911676347393 ) ) ;
#13819=ORIENTED_EDGE ( 'NONE', *, *, #22778, .T. ) ;
#13823=ORIENTED_EDGE ( 'NONE', *, *, #35289, .T. ) ;
#13830=CARTESIAN_POINT ( 'NONE',  ( 121.4136688928271184, -8.278628333885235335, -17.13983228602121045 ) ) ;
#13839=VERTEX_POINT ( 'NONE', #18785 ) ;
#13884=EDGE_CURVE ( 'NONE', #27644, #17793, #38070, .T. ) ;
#13885=CARTESIAN_POINT ( 'NONE',  ( 125.4584548109119737, -9.722663502801697888, -19.87444018218530317 ) ) ;
#13895=CARTESIAN_POINT ( 'NONE',  ( 123.0772048109119652, -7.554583864224885481, -18.48844787311982785 ) ) ;
#13902=CARTESIAN_POINT ( 'NONE',  ( 123.0385396737536752, -8.611453504372539314, -17.77011218421760574 ) ) ;
#13911=CARTESIAN_POINT ( 'NONE',  ( 124.1975102976252003, -8.580000213326620440, -17.71054824844518905 ) ) ;
#13912=EDGE_CURVE ( 'NONE', #27644, #42758, #11051, .T. ) ;
#13924=ORIENTED_EDGE ( 'NONE', *, *, #26138, .F. ) ;
#13929=VERTEX_POINT ( 'NONE', #27149 ) ;
#13931=CARTESIAN_POINT ( 'NONE',  ( 123.5633766859119760, -0.06289925094097943703, -9.412459353600674206 ) ) ;
#13945=CARTESIAN_POINT ( 'NONE',  ( 123.9584548109119737, -11.97804492312075553, -17.05249760251923163 ) ) ;
#13956=AXIS2_PLACEMENT_3D ( 'NONE', #20588, #34466, #19671 ) ;
#13967=CARTESIAN_POINT ( 'NONE',  ( 119.5350954359119839, 0.5291689781388270175, -13.89700978578772705 ) ) ;
#13986=EDGE_CURVE ( 'NONE', #30218, #43475, #43608, .T. ) ;
#13993=CARTESIAN_POINT ( 'NONE',  ( 123.8411891859119862, -1.406689858478933353, -17.56299727309130887 ) ) ;
#13996=CARTESIAN_POINT ( 'NONE',  ( 124.8633137343397692, -2.383538422968402237, -6.106049506750366618 ) ) ;
#14007=CIRCLE ( 'NONE', #9749, 1.587499999999998579 ) ;
#14075=CARTESIAN_POINT ( 'NONE',  ( 123.0077516859119839, -9.665098340737509730, -17.37397104707595474 ) ) ;
#14159=ADVANCED_FACE ( 'NONE', ( #3851 ), #885, .F. ) ;
#14168=ADVANCED_FACE ( 'NONE', ( #8637 ), #23794, .F. ) ;
#14214=CARTESIAN_POINT ( 'NONE',  ( 124.5837840600787274, -9.794985466449714906, -14.24011022619069600 ) ) ;
#14215=CARTESIAN_POINT ( 'NONE',  ( 121.4103298109119748, -2.173413727453600508, -8.297982527556802879 ) ) ;
#14221=B_SPLINE_CURVE_WITH_KNOTS ( 'NONE', 3,
 ( #27352, #34168, #27794, #41706, #10031, #10472, #24373, #34824, #28020, #31420 ),
 .UNSPECIFIED., .F., .F.,
 ( 4, 2, 2, 2, 4 ),
 ( 0.000000000000000000, 0.2500000000000000000, 0.5000000000000000000, 0.7500000000000000000, 1.000000000000000000 ),
 .UNSPECIFIED. ) ;
#14225=CARTESIAN_POINT ( 'NONE',  ( 125.4210411930764337, -6.901805073872763430, -19.97202117700874524 ) ) ;
#14251=DIRECTION ( 'NONE',  ( -1.000000000000000000, 0.000000000000000000, -0.000000000000000000 ) ) ;
#14285=CARTESIAN_POINT ( 'NONE',  ( 121.9272896737536911, -8.611453504372539314, -17.77011218421760574 ) ) ;
#14297=CARTESIAN_POINT ( 'NONE',  ( 120.0907204359119760, 1.345710702986147034, -13.97328579221134426 ) ) ;
#14322=CARTESIAN_POINT ( 'NONE',  ( 119.8129079359119942, -5.444069387712269226, -19.60292469916370450 ) ) ;
#14334=CARTESIAN_POINT ( 'NONE',  ( 124.9063227527182534, -11.00801412892373854, -8.806701716868159835 ) ) ;
#14336=CARTESIAN_POINT ( 'NONE',  ( 123.9800954359119771, -11.07370829466463569, -12.81314460846529002 ) ) ;
#14340=EDGE_LOOP ( 'NONE', ( #37810, #26958, #29429, #7958 ) ) ;
#14354=CARTESIAN_POINT ( 'NONE',  ( 120.4952766009169238, -8.403782945130243931, -17.37684090985457885 ) ) ;
#14396=CARTESIAN_POINT ( 'NONE',  ( 125.4584548109119737, -6.456500312860584678, -19.12873567962219568 ) ) ;
#14438=CARTESIAN_POINT ( 'NONE',  ( 124.5950401870421445, -9.726016666192203175, -14.57860129224645540 ) ) ;
#14439=CARTESIAN_POINT ( 'NONE',  ( 121.2019704359119743, 1.345710702986147034, -13.97328579221134426 ) ) ;
#14442=CARTESIAN_POINT ( 'NONE',  ( 124.3741441133359160, 0.01270242874617801519, -7.107006293821772402 ) ) ;
#14494=CYLINDRICAL_SURFACE ( 'NONE', #14966, 8.000000000000001776 ) ;
#14521=CARTESIAN_POINT ( 'NONE',  ( 122.1048610609119720, -3.163656168406935087, -18.89861972220014508 ) ) ;
#14543=CARTESIAN_POINT ( 'NONE',  ( 121.6881423109119709, -9.959231468620755479, -10.70263013195267199 ) ) ;
#14556=CARTESIAN_POINT ( 'NONE',  ( 125.1589444732352234, -10.92313641483920250, -9.146039627217522394 ) ) ;
#14610=EDGE_CURVE ( 'NONE', #8725, #33098, #31313, .T. ) ;
#14631=CARTESIAN_POINT ( 'NONE',  ( 119.7821199480702603, -6.365377317481695663, -18.95617363400926081 ) ) ;
#14649=CARTESIAN_POINT ( 'NONE',  ( 123.7717360609119623, -3.387241619883791355, -18.17469012370385073 ) ) ;
#14662=CARTESIAN_POINT ( 'NONE',  ( 124.5550616865675693, -9.865623858367307264, -13.39908528032752955 ) ) ;
#14663=CARTESIAN_POINT ( 'NONE',  ( 120.8547048109119686, -7.554583864224885481, -18.48844787311982785 ) ) ;
#14666=CARTESIAN_POINT ( 'NONE',  ( 125.3563494635854880, -1.799223464854087018, -7.045947544758777603 ) ) ;
#14674=ORIENTED_EDGE ( 'NONE', *, *, #39803, .T. ) ;
#14749=CARTESIAN_POINT ( 'NONE',  ( 123.0772048109119652, -7.554583864224885481, -18.48844787311982785 ) ) ;
#14769=CARTESIAN_POINT ( 'NONE',  ( 121.0630641859119976, -0.8832429491016019485, -18.19431474523657855 ) ) ;
#14771=CARTESIAN_POINT ( 'NONE',  ( 124.1884548109119777, -7.554583864224885481, -18.48844787311982785 ) ) ;
#14785=CARTESIAN_POINT ( 'NONE',  ( 123.9584548109119737, -11.17722486020181627, -8.479644537342501565 ) ) ;
#14803=CARTESIAN_POINT ( 'NONE',  ( 120.9936110609119737, -3.163656168406935087, -18.89861972220014508 ) ) ;
#14876=CARTESIAN_POINT ( 'NONE',  ( 122.5910329359119970, -5.367793381288652910, -18.78638297431638904 ) ) ;
#14891=CARTESIAN_POINT ( 'NONE',  ( 123.2161110609119561, -3.163656168406935087, -18.89861972220014508 ) ) ;
#14894=CARTESIAN_POINT ( 'NONE',  ( 124.4646854081442626, -2.418452363927385385, -5.864561580288276232 ) ) ;
#14896=ADVANCED_FACE ( 'NONE', ( #45005 ), #30827, .F. ) ;
#14966=AXIS2_PLACEMENT_3D ( 'NONE', #34556, #21107, #45069 ) ;
#14971=CARTESIAN_POINT ( 'NONE',  ( 123.7717360609119623, -6.564341423271550902, -7.887810678476487425 ) ) ;
#14989=CARTESIAN_POINT ( 'NONE',  ( 121.2019704359119743, 1.345710702986147034, -13.97328579221134426 ) ) ;
#14993=CARTESIAN_POINT ( 'NONE',  ( 119.2572829359120021, -5.367793381288652910, -18.78638297431638904 ) ) ;
#15008=CARTESIAN_POINT ( 'NONE',  ( 124.8633137343444446, -12.15116448942433713, -10.91275482746690706 ) ) ;
#15023=CARTESIAN_POINT ( 'NONE',  ( 120.3685329359119862, -4.283928203966213211, -7.183505701512924446 ) ) ;
#15039=DIRECTION ( 'NONE',  ( -1.000000000000000000, 0.000000000000000000, -0.000000000000000000 ) ) ;
#15043=EDGE_LOOP ( 'NONE', ( #3717, #42836, #40307, #33289, #6255, #20225, #16914, #16002, #7150, #24443, #32494, #36937, #6024, #13541, #37183, #28177, #32770, #40042, #7834, #33763, #3150, #3152 ) ) ;
#15099=CARTESIAN_POINT ( 'NONE',  ( 120.9936110609119737, -3.163656168406935087, -18.89861972220014508 ) ) ;
#15115=CARTESIAN_POINT ( 'NONE',  ( 123.0772048109119652, -7.554583864224885481, -18.48844787311982785 ) ) ;
#15120=CIRCLE ( 'NONE', #6410, 1.587499999999998579 ) ;
#15194=CARTESIAN_POINT ( 'NONE',  ( 123.8411891859119862, -8.844754642576884152, -8.592115655440050404 ) ) ;
#15216=CARTESIAN_POINT ( 'NONE',  ( 120.8547048109119686, -2.527210466738041728, -8.967976844669124148 ) ) ;
#15228=CARTESIAN_POINT ( 'NONE',  ( 124.1188183746285887, -11.97333064901767763, -17.04775611777621336 ) ) ;
#15242=CARTESIAN_POINT ( 'NONE',  ( 120.7157985609119635, -10.36940331770106916, -15.09355782777062061 ) ) ;
#15247=CARTESIAN_POINT ( 'NONE',  ( 120.2296266859119953, -0.06289925094097943703, -9.412459353600674206 ) ) ;
#15248=CARTESIAN_POINT ( 'NONE',  ( 120.4379860609119675, -6.564341423271550902, -7.887810678476487425 ) ) ;
#15266=EDGE_CURVE ( 'NONE', #37005, #33098, #26342, .T. ) ;
#15279=CARTESIAN_POINT ( 'NONE',  ( 123.0204673576684797, -6.302457937304696500, -18.83702152638931082 ) ) ;
#15285=CARTESIAN_POINT ( 'NONE',  ( 120.4379860609119675, -3.387241619883791355, -18.17469012370385073 ) ) ;
#15302=DIRECTION ( 'NONE',  ( 0.000000000000000000, 0.4669533266896293000, 0.8842819633428516957 ) ) ;
#15318=CARTESIAN_POINT ( 'NONE',  ( 124.6051735609119646, -9.645473719204776586, -14.86997237629376656 ) ) ;
#15320=CARTESIAN_POINT ( 'NONE',  ( 119.7434548109119703, 2.768327990826033425, -17.42353644532102308 ) ) ;
#15367=CARTESIAN_POINT ( 'NONE',  ( 122.0046199480702569, -6.365377317481695663, -18.95617363400926081 ) ) ;
#15388=CARTESIAN_POINT ( 'NONE',  ( 125.0660727672596408, -6.058182552637899398, -5.977212348642386708 ) ) ;
#15421=CARTESIAN_POINT ( 'NONE',  ( 120.0212673109119805, -9.289237151508434209, -11.05642687123711276 ) ) ;
#15444=CARTESIAN_POINT ( 'NONE',  ( 119.6740016859119748, -0.6942167230862511529, -9.935906262978006609 ) ) ;
#15453=CARTESIAN_POINT ( 'NONE',  ( 124.5316694066389971, -9.821485997248675659, -12.73715838876115036 ) ) ;
#15457=CARTESIAN_POINT ( 'NONE',  ( 125.3535861756261482, -11.55705830787929678, -15.61165832305779944 ) ) ;
#15476=CARTESIAN_POINT ( 'NONE',  ( 121.5492360609119800, -6.564341423271550902, -7.887810678476487425 ) ) ;
#15477=CARTESIAN_POINT ( 'NONE',  ( 123.9800954359119771, -11.07370829466463569, -12.81314460846529002 ) ) ;
#15498=ORIENTED_EDGE ( 'NONE', *, *, #24246, .T. ) ;
#15507=CARTESIAN_POINT ( 'NONE',  ( 124.8714078922225497, -3.772723311433941795, -21.00617493672336167 ) ) ;
#15512=CARTESIAN_POINT ( 'NONE',  ( 123.9584548109119737, -7.429215134363809092, -20.97079166887802160 ) ) ;
#15542=CARTESIAN_POINT ( 'NONE',  ( 124.0495485609119584, -0.08252387247370887580, -11.91645802438286417 ) ) ;
#15585=ADVANCED_FACE ( 'NONE', ( #26517 ), #2328, .T. ) ;
#15608=CARTESIAN_POINT ( 'NONE',  ( 124.7472578386067283, -5.916068793159596773, -5.684620300579358521 ) ) ;
#15613=CIRCLE ( 'NONE', #28025, 5.000000000000000000 ) ;
#15641=CARTESIAN_POINT ( 'NONE',  ( 124.3692356341941974, 2.697552217974573896, -15.83745505781797647 ) ) ;
#15644=CARTESIAN_POINT ( 'NONE',  ( 120.3439060953690642, -6.001247023715329476, -18.26661038929047720 ) ) ;
#15645=CARTESIAN_POINT ( 'NONE',  ( 122.6009548109119720, 0.04957186715663641774, -7.079989135975798931 ) ) ;
#15659=VECTOR ( 'NONE', #31257, 1000.000000000000000 ) ;
#15681=CARTESIAN_POINT ( 'NONE',  ( 121.2019704359119885, 1.345710702986149920, -13.97328579221134071 ) ) ;
#15684=CARTESIAN_POINT ( 'NONE',  ( 125.2723929556167661, -11.93466551383809815, -14.87328830137684221 ) ) ;
#15704=CARTESIAN_POINT ( 'NONE',  ( 124.0495485609119584, -10.36940331770106916, -15.09355782777062061 ) ) ;
#15705=CARTESIAN_POINT ( 'NONE',  ( 119.8129079359119942, -5.444069387712269226, -19.60292469916370450 ) ) ;
#15721=( LENGTH_UNIT ( ) NAMED_UNIT ( * ) SI_UNIT ( .MILLI., .METRE. ) );
#15736=CARTESIAN_POINT ( 'NONE',  ( 124.7156075856321991, -3.817466558032057478, -21.12005900094969491 ) ) ;
#15755=CARTESIAN_POINT ( 'NONE',  ( 124.8842416685201471, -9.531938938847675402, -19.51325999086594720 ) ) ;
#15772=CARTESIAN_POINT ( 'NONE',  ( 121.9659548109119811, -7.554583864224885481, -18.48844787311982785 ) ) ;
#15807=CARTESIAN_POINT ( 'NONE',  ( 123.9584548109119737, 2.753894863294152007, -15.83610205775420177 ) ) ;
#15813=EDGE_CURVE ( 'NONE', #29158, #2916, #35192, .T. ) ;
#15863=ORIENTED_EDGE ( 'NONE', *, *, #44553, .F. ) ;
#15869=CARTESIAN_POINT ( 'NONE',  ( 124.1685108350173010, 2.742570392492192255, -15.83608568264068062 ) ) ;
#15883=VERTEX_POINT ( 'NONE', #14396 ) ;
#15900=CARTESIAN_POINT ( 'NONE',  ( 121.3408766859119794, -9.033780868592240054, -16.85052413769862056 ) ) ;
#15903=CARTESIAN_POINT ( 'NONE',  ( 125.0211000582878711, 1.959868932401269470, -10.14215219406585256 ) ) ;
#15909=DIRECTION ( 'NONE',  ( 0.000000000000000000, -0.4669533266896290225, -0.8842819633428516957 ) ) ;
#15913=CARTESIAN_POINT ( 'NONE',  ( 124.7774606721202986, -11.80897325920537888, -16.84910625859622968 ) ) ;
#15933=CARTESIAN_POINT ( 'NONE',  ( 119.8823610609119754, -6.340755971794695078, -8.611740276972781771 ) ) ;
#15934=CARTESIAN_POINT ( 'NONE',  ( 120.0907204359119760, 1.345710702986147034, -13.97328579221134426 ) ) ;
#15963=CARTESIAN_POINT ( 'NONE',  ( 125.3031471548959814, -3.285148677421780405, -20.38179746482967758 ) ) ;
#15966=CARTESIAN_POINT ( 'NONE',  ( 123.6328298109119714, -7.200787124940443817, -17.81845355600750835 ) ) ;
#15979=ORIENTED_EDGE ( 'NONE', *, *, #13684, .T. ) ;
#15981=CARTESIAN_POINT ( 'NONE',  ( 123.9106423109119675, -0.4387604401700495593, -15.73000352943951263 ) ) ;
#16002=ORIENTED_EDGE ( 'NONE', *, *, #28641, .F. ) ;
#16003=CARTESIAN_POINT ( 'NONE',  ( 119.8823610609119754, -3.163656168406935087, -18.89861972220014508 ) ) ;
#16012=CARTESIAN_POINT ( 'NONE',  ( 124.5966688623432219, -9.713577380183913590, -14.62808432448665563 ) ) ;
#16065=CARTESIAN_POINT ( 'NONE',  ( 120.9241579359119925, -4.360204210389833968, -8.000047426360245240 ) ) ;
#16068=CIRCLE ( 'NONE', #3695, 1.587500000000000799 ) ;
#16089=CARTESIAN_POINT ( 'NONE',  ( 124.9063227527188928, 1.280016537245024066, -17.97972868380785627 ) ) ;
#16122=CARTESIAN_POINT ( 'NONE',  ( 121.8270485609119760, -0.08252387247370887580, -11.91645802438286417 ) ) ;
#16127=CARTESIAN_POINT ( 'NONE',  ( 122.1743141859119817, -0.8832429491016114964, -18.19431474523657499 ) ) ;
#16135=CARTESIAN_POINT ( 'NONE',  ( 125.3368646685608923, -11.73513648066642290, -15.14777030654274803 ) ) ;
#16136=CARTESIAN_POINT ( 'NONE',  ( 123.7054579359119941, -5.367357518394499927, -18.78171702160300782 ) ) ;
#16138=DIRECTION ( 'NONE',  ( -1.000000000000000000, 0.000000000000000000, -0.000000000000000000 ) ) ;
#16158=CARTESIAN_POINT ( 'NONE',  ( 119.8129079359119942, -4.360204210389833968, -8.000047426360245240 ) ) ;
#16159=CARTESIAN_POINT ( 'NONE',  ( 121.3408766859119794, -0.06289925094097943703, -9.412459353600674206 ) ) ;
#16176=( NAMED_UNIT ( * ) SI_UNIT ( $, .STERADIAN. ) SOLID_ANGLE_UNIT ( ) );
#16194=CARTESIAN_POINT ( 'NONE',  ( 122.4521266859119635, -9.033780868592240054, -16.85052413769862056 ) ) ;
#16235=CARTESIAN_POINT ( 'NONE',  ( 122.5215798109119874, -7.200787124940443817, -17.81845355600750835 ) ) ;
#16241=VERTEX_POINT ( 'NONE', #3135 ) ;
#16255=CYLINDRICAL_SURFACE ( 'NONE', #23470, 8.000000000000001776 ) ;
#16257=CARTESIAN_POINT ( 'NONE',  ( 120.8160396737536928, -8.611453504372539314, -17.77011218421760574 ) ) ;
#16271=CARTESIAN_POINT ( 'NONE',  ( 120.9241579359119925, -4.360204210389833968, -8.000047426360245240 ) ) ;
#16322=CARTESIAN_POINT ( 'NONE',  ( 125.0211000582883685, 2.260053046519062026, -15.91956964709736333 ) ) ;
#16348=AXIS2_PLACEMENT_3D ( 'NONE', #32374, #688, #29411 ) ;
#16349=CARTESIAN_POINT ( 'NONE',  ( 122.7299391859119737, -1.406689858478933353, -17.56299727309130887 ) ) ;
#16351=CYLINDRICAL_SURFACE ( 'NONE', #1451, 8.000000000000001776 ) ;
#16357=CARTESIAN_POINT ( 'NONE',  ( 121.1325173109119788, 0.2312338769422696283, -16.08380026872395874 ) ) ;
#16359=DIRECTION ( 'NONE',  ( -1.000000000000000000, 0.000000000000000000, -0.000000000000000000 ) ) ;
#16360=CARTESIAN_POINT ( 'NONE',  ( 124.3305360609119816, -6.339478340643663223, -8.615877017535705562 ) ) ;
#16362=CARTESIAN_POINT ( 'NONE',  ( 119.7434548109119561, 0.4099171239737569583, -13.35943364252451460 ) ) ;
#16381=CARTESIAN_POINT ( 'NONE',  ( 123.5633766859119760, -0.06289925094097943703, -9.412459353600674206 ) ) ;
#16382=CARTESIAN_POINT ( 'NONE',  ( 120.9936110609119737, -6.340755971794695078, -8.611740276972781771 ) ) ;
#16423=CARTESIAN_POINT ( 'NONE',  ( 120.0212673109119805, 0.2312338769422704887, -16.08380026872395874 ) ) ;
#16439=CARTESIAN_POINT ( 'NONE',  ( 123.4939235609119663, 0.6414057260225851653, -11.69287257290601723 ) ) ;
#16455=CARTESIAN_POINT ( 'NONE',  ( 122.6604860609119640, -6.564341423271550902, -7.887810678476487425 ) ) ;
#16459=CARTESIAN_POINT ( 'NONE',  ( 121.1325173109119788, -9.289237151508434209, -11.05642687123711276 ) ) ;
#16464=ORIENTED_EDGE ( 'NONE', *, *, #20284, .F. ) ;
#16469=EDGE_CURVE ( 'NONE', #7750, #39662, #38998, .T. ) ;
#16484=CARTESIAN_POINT ( 'NONE',  ( 120.9590811593281785, -8.517053830703083861, -17.59134500557228620 ) ) ;
#16499=CARTESIAN_POINT ( 'NONE',  ( 124.6894688159050872, -8.253847584685239269, -17.09290432062678278 ) ) ;
#16518=ORIENTED_EDGE ( 'NONE', *, *, #24251, .F. ) ;
#16526=CARTESIAN_POINT ( 'NONE',  ( 122.6604860609119640, -3.387241619883791355, -18.17469012370385073 ) ) ;
#16531=AXIS2_PLACEMENT_3D ( 'NONE', #17123, #26923, #38290 ) ;
#16581=CARTESIAN_POINT ( 'NONE',  ( 121.9659548109119811, -2.527210466738041728, -8.967976844669124148 ) ) ;
#16595=CARTESIAN_POINT ( 'NONE',  ( 124.4694423109119725, -9.285408612553634811, -11.05844856689041755 ) ) ;
#16597=CARTESIAN_POINT ( 'NONE',  ( 119.7434548109119703, 0.4041035117704004365, -14.01369669089266168 ) ) ;
#16615=CARTESIAN_POINT ( 'NONE',  ( 121.2019704359119743, -10.25716656981731489, -12.88942061488890545 ) ) ;
#16616=CARTESIAN_POINT ( 'NONE',  ( 122.1743141859119817, -8.321307733199551748, -9.223433127585318303 ) ) ;
#16648=CARTESIAN_POINT ( 'NONE',  ( 120.3685329359119862, -4.283928203966213211, -7.183505701512925334 ) ) ;
#16655=EDGE_CURVE ( 'NONE', #25324, #13081, #2620, .T. ) ;
#16668=CARTESIAN_POINT ( 'NONE',  ( 124.2928311593281876, -8.517053830703071426, -17.59134500557229330 ) ) ;
#16683=CARTESIAN_POINT ( 'NONE',  ( 123.0772048109119652, -7.554583864224885481, -18.48844787311982785 ) ) ;
#16687=CARTESIAN_POINT ( 'NONE',  ( 121.5492360609119800, -3.387241619883791355, -18.17469012370385073 ) ) ;
#16710=ORIENTED_EDGE ( 'NONE', *, *, #1152, .F. ) ;
#16726=CARTESIAN_POINT ( 'NONE',  ( 125.4584548109119737, -9.722663502801697888, -19.87444018218530317 ) ) ;
#16753=CARTESIAN_POINT ( 'NONE',  ( 124.1190016859119680, -0.6942167230862511529, -9.935906262978006609 ) ) ;
#16779=EDGE_CURVE ( 'NONE', #17122, #33790, #3522, .T. ) ;
#16802=EDGE_CURVE ( 'NONE', #7584, #2526, #1653, .T. ) ;
#16816=CARTESIAN_POINT ( 'NONE',  ( 122.0046199480702569, -6.365377317481695663, -18.95617363400926081 ) ) ;
#16845=CARTESIAN_POINT ( 'NONE',  ( 123.2855641859119942, -8.321307733199551748, -9.223433127585318303 ) ) ;
#16846=CARTESIAN_POINT ( 'NONE',  ( 121.6186891859119896, -1.406689858478933353, -17.56299727309130887 ) ) ;
#16865=CARTESIAN_POINT ( 'NONE',  ( 120.6463454359119822, -11.07370829466463569, -12.81314460846529002 ) ) ;
#16879=CARTESIAN_POINT ( 'NONE',  ( 122.8688454359119646, -11.07370829466463569, -12.81314460846529002 ) ) ;
#16896=CARTESIAN_POINT ( 'NONE',  ( 123.1158699480702410, -6.365377317481717867, -18.95617363400926081 ) ) ;
#16914=ORIENTED_EDGE ( 'NONE', *, *, #18985, .F. ) ;
#16915=CARTESIAN_POINT ( 'NONE',  ( 123.7717360609119623, -3.387241619883791355, -18.17469012370385073 ) ) ;
#16927=CARTESIAN_POINT ( 'NONE',  ( 123.9584548109119737, -4.863998795839242995, -13.39321520033831447 ) ) ;
#16951=CARTESIAN_POINT ( 'NONE',  ( 119.3235610609119846, -3.388519251035092328, -18.17055338314101220 ) ) ;
#16953=CARTESIAN_POINT ( 'NONE',  ( 122.5215798109119874, -7.200787124940443817, -17.81845355600750835 ) ) ;
#16965=VERTEX_POINT ( 'NONE', #30897 ) ;
#16980=CARTESIAN_POINT ( 'NONE',  ( 120.0212673109119805, 0.2312338769422704887, -16.08380026872395874 ) ) ;
#17040=CARTESIAN_POINT ( 'NONE',  ( 122.9868014478796425, -9.877548923986811502, -16.68609415519377137 ) ) ;
#17041=CARTESIAN_POINT ( 'NONE',  ( 121.8363908503701509, -8.552676153439012552, -17.65880394779906837 ) ) ;
#17046=CARTESIAN_POINT ( 'NONE',  ( 122.8688454359119646, 0.5291689781388270175, -13.89700978578772705 ) ) ;
#17048=CARTESIAN_POINT ( 'NONE',  ( 124.5357204359119834, -10.25716656981734332, -12.88942061488921098 ) ) ;
#17063=CARTESIAN_POINT ( 'NONE',  ( 119.9518141859119851, -0.8832429491016019485, -18.19431474523657855 ) ) ;
#17070=CARTESIAN_POINT ( 'NONE',  ( 119.4656423109119743, -0.4387604401700512802, -15.73000352943951619 ) ) ;
#17088=CARTESIAN_POINT ( 'NONE',  ( 121.4797829359119987, -4.283928203966213211, -7.183505701512925334 ) ) ;
#17102=CARTESIAN_POINT ( 'NONE',  ( 124.1884548109119777, -7.554583864224885481, -18.48844787311982785 ) ) ;
#17113=CARTESIAN_POINT ( 'NONE',  ( 121.6186891859119754, -1.406689858478935573, -17.56299727309130887 ) ) ;
#17122=VERTEX_POINT ( 'NONE', #21303 ) ;
#17123=CARTESIAN_POINT ( 'NONE',  ( 125.4584548109119737, -13.11073630560948722, -15.94021774473354114 ) ) ;
#17131=( BOUNDED_SURFACE ( )  B_SPLINE_SURFACE ( 1, 2, ( 
 ( #35568, #18261, #15285, #29192, #11874, #32157, #28754, #42659, #39685, #11430, #8450, #36247, #26457, #13229, #5460, #27130, #6149, #2043, #19604, #2266, #40359, #43556, #23027, #30542, #2722, #44014, #9348, #12776, #41054, #12550, #20069, #16194, #33488, #8898, #30098, #44464, #26224, #26901, #9811, #26678, #34176, #2494, #36690, #2952, #40589, #23720, #37379, #23257, #15966, #19380, #40822, #43785, #9123, #40133, #13003, #36914, #22796, #37141, #5915, #5685, #29870, #33268, #33955, #19837, #9577 ),
 ( #33724, #23493, #37610, #20292, #16423, #12324, #6384, #30319, #44245, #16648, #29642, #13677, #41280, #35052, #34831, #3835, #7048, #24163, #37827, #21400, #6833, #44696, #13456, #6605, #3616, #20738, #20518, #17534, #17755, #10256, #38055, #20959, #10040, #34618, #31652, #3405, #24821, #420, #24602, #17322, #38712, #28028, #27360, #31429, #35280, #16879, #31212, #30994, #13895, #30770, #34398, #45136, #27801, #38485, #21177, #196, #38267, #23947, #7260, #41936, #44920, #14336, #7481, #3179, #17102 ) ),
 .UNSPECIFIED., .F., .F., .T. ) 
 B_SPLINE_SURFACE_WITH_KNOTS ( ( 2, 2 ),
 ( 3, 2, 2, 2, 2, 2, 2, 2, 2, 2, 2, 2, 2, 2, 2, 2, 2, 2, 2, 2, 2, 2, 2, 2, 2, 2, 2, 2, 2, 2, 2, 2, 3 ),
 ( 0.000000000000000000, 1.000000000000000000 ),
 ( 0.000000000000000000, 0.03125000000000000000, 0.06250000000000000000, 0.09375000000000000000, 0.1250000000000000000, 0.1562500000000000000, 0.1875000000000000000, 0.2187500000000000000, 0.2500000000000000000, 0.2812500000000000000, 0.3125000000000000000, 0.3437500000000000000, 0.3750000000000000000, 0.4062500000000000000, 0.4375000000000000000, 0.4687500000000000000, 0.5000000000000000000, 0.5312500000000000000, 0.5625000000000000000, 0.5937500000000000000, 0.6250000000000000000, 0.6562500000000000000, 0.6875000000000000000, 0.7187500000000000000, 0.7500000000000000000, 0.7812500000000000000, 0.8125000000000000000, 0.8437500000000000000, 0.8750000000000000000, 0.9062500000000000000, 0.9375000000000000000, 0.9687500000000000000, 1.000000000000000000 ),
 .UNSPECIFIED. ) 
 GEOMETRIC_REPRESENTATION_ITEM ( )  RATIONAL_B_SPLINE_SURFACE ( (
 ( 1.000000000000000000, 0.9238795325112869605, 1.000000000000000000, 0.9238795325112869605, 1.000000000000000000, 0.9238795325112869605, 1.000000000000000000, 0.9238795325112869605, 1.000000000000000000, 0.9238795325112869605, 1.000000000000000000, 0.9238795325112869605, 1.000000000000000000, 0.9238795325112869605, 1.000000000000000000, 0.9238795325112869605, 1.000000000000000000, 0.9238795325112869605, 1.000000000000000000, 0.9238795325112869605, 1.000000000000000000, 0.9238795325112869605, 1.000000000000000000, 0.9238795325112869605, 1.000000000000000000, 0.9238795325112869605, 1.000000000000000000, 0.9238795325112869605, 1.000000000000000000, 0.9238795325112869605, 1.000000000000000000, 0.9238795325112869605, 1.000000000000000000, 0.9238795325112869605, 1.000000000000000000, 0.9238795325112869605, 1.000000000000000000, 0.9238795325112869605, 1.000000000000000000, 0.9238795325112869605, 1.000000000000000000, 0.9238795325112869605, 1.000000000000000000, 0.9238795325112869605, 1.000000000000000000, 0.9238795325112869605, 1.000000000000000000, 0.9238795325112869605, 1.000000000000000000, 0.9238795325112869605, 1.000000000000000000, 0.9238795325112869605, 1.000000000000000000, 0.9238795325112869605, 1.000000000000000000, 0.9238795325112869605, 1.000000000000000000, 0.9238795325112869605, 1.000000000000000000, 0.9238795325112869605, 1.000000000000000000, 0.9238795325112869605, 1.000000000000000000, 0.9238795325112869605, 1.000000000000000000),
 ( 1.000000000000000000, 0.9238795325112869605, 1.000000000000000000, 0.9238795325112869605, 1.000000000000000000, 0.9238795325112869605, 1.000000000000000000, 0.9238795325112869605, 1.000000000000000000, 0.9238795325112869605, 1.000000000000000000, 0.9238795325112869605, 1.000000000000000000, 0.9238795325112869605, 1.000000000000000000, 0.9238795325112869605, 1.000000000000000000, 0.9238795325112869605, 1.000000000000000000, 0.9238795325112869605, 1.000000000000000000, 0.9238795325112869605, 1.000000000000000000, 0.9238795325112869605, 1.000000000000000000, 0.9238795325112869605, 1.000000000000000000, 0.9238795325112869605, 1.000000000000000000, 0.9238795325112869605, 1.000000000000000000, 0.9238795325112869605, 1.000000000000000000, 0.9238795325112869605, 1.000000000000000000, 0.9238795325112869605, 1.000000000000000000, 0.9238795325112869605, 1.000000000000000000, 0.9238795325112869605, 1.000000000000000000, 0.9238795325112869605, 1.000000000000000000, 0.9238795325112869605, 1.000000000000000000, 0.9238795325112869605, 1.000000000000000000, 0.9238795325112869605, 1.000000000000000000, 0.9238795325112869605, 1.000000000000000000, 0.9238795325112869605, 1.000000000000000000, 0.9238795325112869605, 1.000000000000000000, 0.9238795325112869605, 1.000000000000000000, 0.9238795325112869605, 1.000000000000000000, 0.9238795325112869605, 1.000000000000000000, 0.9238795325112869605, 1.000000000000000000, 0.9238795325112869605, 1.000000000000000000) ) ) 
 REPRESENTATION_ITEM ( '' )  SURFACE ( )  );
#17133=ORIENTED_EDGE ( 'NONE', *, *, #39109, .T. ) ;
#17139=CARTESIAN_POINT ( 'NONE',  ( 124.1190016859119680, -9.665098340737509730, -17.37397104707595474 ) ) ;
#17174=CARTESIAN_POINT ( 'NONE',  ( 119.6708266859119760, -0.6978242514985085743, -9.938897388174442682 ) ) ;
#17199=CARTESIAN_POINT ( 'NONE',  ( 122.3826735609119680, -9.645473719204776586, -14.86997237629376656 ) ) ;
#17225=EDGE_CURVE ( 'NONE', #13929, #34025, #27614, .T. ) ;
#17253=ORIENTED_EDGE ( 'NONE', *, *, #13986, .T. ) ;
#17273=CARTESIAN_POINT ( 'NONE',  ( 123.1158699480702552, -6.365377317481717867, -18.95617363400926081 ) ) ;
#17283=CARTESIAN_POINT ( 'NONE',  ( 120.1601735609119856, 0.6414057260225851653, -11.69287257290600657 ) ) ;
#17297=SURFACE_STYLE_USAGE ( .BOTH. , #42135 ) ;
#17298=CARTESIAN_POINT ( 'NONE',  ( 120.2518633482210504, -8.245769691054972483, -17.07760699810916094 ) ) ;
#17310=ORIENTED_EDGE ( 'NONE', *, *, #18985, .T. ) ;
#17322=CARTESIAN_POINT ( 'NONE',  ( 122.4521266859119635, -0.06289925094097943703, -9.412459353600674206 ) ) ;
#17358=CARTESIAN_POINT ( 'NONE',  ( 121.8270485609119760, -10.36940331770106916, -15.09355782777062061 ) ) ;
#17416=CARTESIAN_POINT ( 'NONE',  ( 123.3550173109119612, -9.289237151508434209, -11.05642687123711276 ) ) ;
#17419=CARTESIAN_POINT ( 'NONE',  ( 119.7434548109119703, -2.613043214085062793, -8.928554074455437473 ) ) ;
#17425=ORIENTED_EDGE ( 'NONE', *, *, #11666, .F. ) ;
#17428=CARTESIAN_POINT ( 'NONE',  ( 119.7434548109119703, -2.832009000835249868, -18.56602343984135572 ) ) ;
#17470=CARTESIAN_POINT ( 'NONE',  ( 124.6110072661092119, -9.586796501237937917, -15.06922472696892967 ) ) ;
#17480=CARTESIAN_POINT ( 'NONE',  ( 122.0703311593281768, -8.517053830703083861, -17.59134500557228620 ) ) ;
#17491=CARTESIAN_POINT ( 'NONE',  ( 121.4797829359119987, -4.283928203966213211, -7.183505701512925334 ) ) ;
#17505=SHAPE_REPRESENTATION_RELATIONSHIP ( 'NONE' , 'NONE' ,  #38750, #6345 ) ;
#17514=EDGE_CURVE ( 'NONE', #7179, #10924, #24303, .T. ) ;
#17515=CARTESIAN_POINT ( 'NONE',  ( 120.9936110609119737, -3.163656168406935087, -18.89861972220014508 ) ) ;
#17530=CARTESIAN_POINT ( 'NONE',  ( 125.3563494635812958, -11.21126645141554512, -10.32843986934705605 ) ) ;
#17534=CARTESIAN_POINT ( 'NONE',  ( 121.6186891859119896, -8.844754642576884152, -8.592115655440050404 ) ) ;
#17573=VECTOR ( 'NONE', #17890, 1000.000000000000000 ) ;
#17585=DIRECTION ( 'NONE',  ( 1.000000000000000000, 0.000000000000000000, 0.000000000000000000 ) ) ;
#17611=CARTESIAN_POINT ( 'NONE',  ( 119.3930141859119942, -1.409680983675372534, -17.55938974467904856 ) ) ;
#17625=CARTESIAN_POINT ( 'NONE',  ( 120.9241579359119925, -4.360204210389833968, -8.000047426360245240 ) ) ;
#17629=CARTESIAN_POINT ( 'NONE',  ( 125.4584548109119737, -13.11073630560948722, -15.94021774473354114 ) ) ;
#17636=CARTESIAN_POINT ( 'NONE',  ( 123.2855641859119942, -0.8832429491016019485, -18.19431474523657855 ) ) ;
#17639=CARTESIAN_POINT ( 'NONE',  ( 124.7472578386042272, -0.1571248981867441608, -7.198489643910104263 ) ) ;
#17645=CARTESIAN_POINT ( 'NONE',  ( 125.4584548109119737, -6.811592368434140177, -19.80118297172327857 ) ) ;
#17653=ADVANCED_FACE ( 'NONE', ( #21865 ), #1387, .F. ) ;
#17724=CARTESIAN_POINT ( 'NONE',  ( 121.4797829359119987, -5.367793381288652910, -18.78638297431638904 ) ) ;
#17750=CARTESIAN_POINT ( 'NONE',  ( 125.4584548109119737, -4.863998795839242995, -13.39321520033831447 ) ) ;
#17753=CARTESIAN_POINT ( 'NONE',  ( 124.6565730087442887, -12.30134031792964855, -10.93904118205077935 ) ) ;
#17755=CARTESIAN_POINT ( 'NONE',  ( 121.6881423109119709, -9.959231468620755479, -10.70263013195267199 ) ) ;
#17763=CARTESIAN_POINT ( 'NONE',  ( 119.7434548109119703, -9.675291321254654520, -19.78473021908636298 ) ) ;
#17765=CARTESIAN_POINT ( 'NONE',  ( 121.6881423109119709, -0.4387604401700521684, -15.73000352943951974 ) ) ;
#17793=VERTEX_POINT ( 'NONE', #3148 ) ;
#17808=CARTESIAN_POINT ( 'NONE',  ( 122.7419882662982786, -6.118135741080345191, -18.48796566952144005 ) ) ;
#17834=AXIS2_PLACEMENT_3D ( 'NONE', #13885, #26891, #23712 ) ;
#17854=ORIENTED_EDGE ( 'NONE', *, *, #26771, .T. ) ;
#17859=CARTESIAN_POINT ( 'NONE',  ( 124.5857744023975471, -9.784663199447079407, -14.29957148619841334 ) ) ;
#17869=CARTESIAN_POINT ( 'NONE',  ( 125.4584548109119737, -6.717659058379802595, -19.62329895828877468 ) ) ;
#17890=DIRECTION ( 'NONE',  ( 1.000000000000000000, 0.000000000000000000, 0.000000000000000000 ) ) ;
#17916=CARTESIAN_POINT ( 'NONE',  ( 119.7434548109119703, -7.429215134363809092, -20.97079166887802160 ) ) ;
#17929=ORIENTED_EDGE ( 'NONE', *, *, #39135, .T. ) ;
#17942=CARTESIAN_POINT ( 'NONE',  ( 120.3685329359119862, -4.283928203966213211, -7.183505701512925334 ) ) ;
#17949=VERTEX_POINT ( 'NONE', #44492 ) ;
#17964=CARTESIAN_POINT ( 'NONE',  ( 119.8129079359119942, -4.360204210389833968, -8.000047426360245240 ) ) ;
#17989=CARTESIAN_POINT ( 'NONE',  ( 121.9659548109119811, -2.527210466738039951, -8.967976844669125924 ) ) ;
#17994=CARTESIAN_POINT ( 'NONE',  ( 120.0212673109119805, 0.2312338769422704887, -16.08380026872395874 ) ) ;
#17995=DIRECTION ( 'NONE',  ( 0.000000000000000000, -0.4669533266896287449, -0.8842819633428518067 ) ) ;
#18020=ORIENTED_EDGE ( 'NONE', *, *, #23916, .F. ) ;
#18069=CARTESIAN_POINT ( 'NONE',  ( 120.3685329359119862, -5.367793381288652910, -18.78638297431638904 ) ) ;
#18082=CARTESIAN_POINT ( 'NONE',  ( 124.5529552597880638, -9.864862387977231251, -13.33873797166363318 ) ) ;
#18084=CARTESIAN_POINT ( 'NONE',  ( 121.7575954359119805, -11.07370829466463569, -12.81314460846529002 ) ) ;
#18087=CARTESIAN_POINT ( 'NONE',  ( 124.9542645564587247, -2.361164406680991146, -6.193652130325402183 ) ) ;
#18142=DIRECTION ( 'NONE',  ( 0.000000000000000000, -0.4669533266896288004, -0.8842819633428519177 ) ) ;
#18165=CARTESIAN_POINT ( 'NONE',  ( 121.9659548109119811, -2.527210466738041728, -8.967976844669124148 ) ) ;
#18173=ORIENTED_EDGE ( 'NONE', *, *, #34453, .F. ) ;
#18184=CARTESIAN_POINT ( 'NONE',  ( 121.5492360609119800, -6.564341423271550902, -7.887810678476487425 ) ) ;
#18188=CARTESIAN_POINT ( 'NONE',  ( 123.8411891859119862, -8.844754642576884152, -8.592115655440050404 ) ) ;
#18222=CARTESIAN_POINT ( 'NONE',  ( 120.2990798109119766, -2.173413727453600508, -8.297982527556802879 ) ) ;
#18261=CARTESIAN_POINT ( 'NONE',  ( 120.3685329359119862, -5.367793381288652910, -18.78638297431638904 ) ) ;
#18266=ORIENTED_EDGE ( 'NONE', *, *, #26730, .F. ) ;
#18283=ORIENTED_EDGE ( 'NONE', *, *, #18686, .F. ) ;
#18293=CARTESIAN_POINT ( 'NONE',  ( 123.4244704359119709, -10.25716656981731489, -12.88942061488890545 ) ) ;
#18309=CARTESIAN_POINT ( 'NONE',  ( 124.0495485609119584, -10.36940331770106916, -15.09355782777062061 ) ) ;
#18312=CARTESIAN_POINT ( 'NONE',  ( 119.7434548109119987, -2.601528322103975999, -8.933709204980601726 ) ) ;
#18379=CARTESIAN_POINT ( 'NONE',  ( 123.2855641859119800, -8.321307733199551748, -9.223433127585318303 ) ) ;
#18398=CARTESIAN_POINT ( 'NONE',  ( 122.1048610609119720, -6.340755971794695078, -8.611740276972781771 ) ) ;
#18419=CARTESIAN_POINT ( 'NONE',  ( 120.2990798109119766, -2.173413727453600508, -8.297982527556802879 ) ) ;
#18423=CARTESIAN_POINT ( 'NONE',  ( 120.5768923109119868, -0.4387604401700512802, -15.73000352943951619 ) ) ;
#18430=CYLINDRICAL_SURFACE ( 'NONE', #20091, 8.000000000000001776 ) ;
#18443=LINE ( 'NONE', #10922, #38001 ) ;
#18448=LINE ( 'NONE', #24829, #2976 ) ;
#18451=CARTESIAN_POINT ( 'NONE',  ( 119.8338581739443072, -4.756192495830076084, -19.39047411591439385 ) ) ;
#18455=CARTESIAN_POINT ( 'NONE',  ( 120.1601735609119856, 0.6414057260225851653, -11.69287257290600657 ) ) ;
#18470=EDGE_CURVE ( 'NONE', #1411, #30218, #19358, .T. ) ;
#18521=CARTESIAN_POINT ( 'NONE',  ( 123.5633766859119760, -9.033780868592240054, -16.85052413769862056 ) ) ;
#18578=ORIENTED_EDGE ( 'NONE', *, *, #35388, .F. ) ;
#18584=AXIS2_PLACEMENT_3D ( 'NONE', #15320, #11683, #25589 ) ;
#18617=CARTESIAN_POINT ( 'NONE',  ( 119.3267360609119692, -3.387241619883791355, -18.17469012370385073 ) ) ;
#18619=EDGE_CURVE ( 'NONE', #24335, #31497, #36543, .T. ) ;
#18638=CARTESIAN_POINT ( 'NONE',  ( 120.4379860609119675, -6.564341423271550902, -7.887810678476487425 ) ) ;
#18641=CARTESIAN_POINT ( 'NONE',  ( 124.1190016859119680, -9.665098340737509730, -17.37397104707595474 ) ) ;
#18657=CARTESIAN_POINT ( 'NONE',  ( 125.2958570204316118, -11.52802372718165103, -16.06387753721113754 ) ) ;
#18669=CARTESIAN_POINT ( 'NONE',  ( 120.0907204359119760, 1.345710702986149920, -13.97328579221134071 ) ) ;
#18674=CARTESIAN_POINT ( 'NONE',  ( 121.6881423109119709, -9.959231468620755479, -10.70263013195267199 ) ) ;
#18675=CARTESIAN_POINT ( 'NONE',  ( 123.2161110609119561, -3.163656168406935087, -18.89861972220014508 ) ) ;
#18685=LINE ( 'NONE', #8196, #13302 ) ;
#18686=EDGE_CURVE ( 'NONE', #16965, #10924, #27435, .T. ) ;
#18702=CARTESIAN_POINT ( 'NONE',  ( 124.5059548109119731, -4.863998795839242995, -13.39321520033831447 ) ) ;
#18716=ADVANCED_FACE ( 'NONE', ( #44538 ), #7513, .F. ) ;
#18745=CARTESIAN_POINT ( 'NONE',  ( 120.6463454359119822, -11.07370829466463569, -12.81314460846529002 ) ) ;
#18749=CARTESIAN_POINT ( 'NONE',  ( 120.2990798109119766, -7.200787124940443817, -17.81845355600750835 ) ) ;
#18758=CARTESIAN_POINT ( 'NONE',  ( 124.5444919965972161, -9.856391046268592859, -13.09751618074382584 ) ) ;
#18785=CARTESIAN_POINT ( 'NONE',  ( 123.5880035264548837, -8.247323210606174015, -17.08054893949881858 ) ) ;
#18835=CARTESIAN_POINT ( 'NONE',  ( 119.8129079359119942, -4.360204210389833968, -8.000047426360245240 ) ) ;
#18856=CARTESIAN_POINT ( 'NONE',  ( 123.6794958213048261, -6.000051279993413367, -18.26434597752674094 ) ) ;
#18858=CARTESIAN_POINT ( 'NONE',  ( 119.4656423109119743, -0.4387604401700512802, -15.73000352943951619 ) ) ;
#18866=CARTESIAN_POINT ( 'NONE',  ( 124.5295211713731049, -9.813149682921396888, -12.67736657363807851 ) ) ;
#18872=CARTESIAN_POINT ( 'NONE',  ( 125.3390168672558218, -11.72568323628656906, -15.16441118647451169 ) ) ;
#18886=CARTESIAN_POINT ( 'NONE',  ( 120.7643014478796459, -9.877548923986811502, -16.68609415519376427 ) ) ;
#18888=ORIENTED_EDGE ( 'NONE', *, *, #14610, .F. ) ;
#18892=CARTESIAN_POINT ( 'NONE',  ( 123.7022829359119811, -4.283928203966213211, -7.183505701512925334 ) ) ;
#18928=CARTESIAN_POINT ( 'NONE',  ( 124.9511461828809473, -3.739606423682455993, -20.93492623671060926 ) ) ;
#18961=ORIENTED_EDGE ( 'NONE', *, *, #11674, .T. ) ;
#18962=CARTESIAN_POINT ( 'NONE',  ( 122.7993923109119692, -0.4387604401700512802, -15.73000352943951619 ) ) ;
#18967=AXIS2_PLACEMENT_3D ( 'NONE', #41986, #3454, #3004 ) ;
#18968=CARTESIAN_POINT ( 'NONE',  ( 120.3685329359119862, -5.367793381288652910, -18.78638297431638904 ) ) ;
#18985=EDGE_CURVE ( 'NONE', #38956, #23418, #14007, .T. ) ;
#19029=CARTESIAN_POINT ( 'NONE',  ( 120.2990798109119766, -7.200787124940443817, -17.81845355600750835 ) ) ;
#19085=CARTESIAN_POINT ( 'NONE',  ( 121.6881423109119709, -0.4387604401700512802, -15.73000352943951619 ) ) ;
#19093=CARTESIAN_POINT ( 'NONE',  ( 124.5155214467870479, -9.741323495560987311, -12.29181226416380390 ) ) ;
#19097=CARTESIAN_POINT ( 'NONE',  ( 125.3096478272239835, -11.83614581139350541, -14.99072624410023202 ) ) ;
#19120=CARTESIAN_POINT ( 'NONE',  ( 121.8965016859119856, -9.665098340737509730, -17.37397104707595474 ) ) ;
#19121=CARTESIAN_POINT ( 'NONE',  ( 120.9936110609119737, -3.163656168406935087, -18.89861972220014508 ) ) ;
#19154=CARTESIAN_POINT ( 'NONE',  ( 124.8979611532368494, -3.762709360267329828, -20.98360247027872916 ) ) ;
#19194=CARTESIAN_POINT ( 'NONE',  ( 123.9800954359119771, 0.5291689781388270175, -13.89700978578772705 ) ) ;
#19199=CARTESIAN_POINT ( 'NONE',  ( 120.6463454359119822, 0.5291689781388270175, -13.89700978578772705 ) ) ;
#19234=CARTESIAN_POINT ( 'NONE',  ( 120.8933699480702586, -6.365377317481695663, -18.95617363400926081 ) ) ;
#19259=CARTESIAN_POINT ( 'NONE',  ( 125.2512653913849476, -6.287234879411991884, -6.272089152466438833 ) ) ;
#19278=CARTESIAN_POINT ( 'NONE',  ( 122.5249188928271167, -8.278628333885240664, -17.13983228602120690 ) ) ;
#19289=CARTESIAN_POINT ( 'NONE',  ( 124.7442371152574196, 2.518403514258475528, -15.85449577716609859 ) ) ;
#19318=CARTESIAN_POINT ( 'NONE',  ( 123.9584548109119737, 2.250047331442289966, -9.733932798157443500 ) ) ;
#19327=FACE_OUTER_BOUND ( 'NONE', #35620, .T. ) ;
#19328=CARTESIAN_POINT ( 'NONE',  ( 123.8443641859119992, -1.409680983675146049, -17.55938974467885672 ) ) ;
#19347=CARTESIAN_POINT ( 'NONE',  ( 119.3267360609119692, -3.387241619883791355, -18.17469012370385073 ) ) ;
#19348=CARTESIAN_POINT ( 'NONE',  ( 120.3685329359119862, -4.283928203966213211, -7.183505701512925334 ) ) ;
#19358=B_SPLINE_CURVE_WITH_KNOTS ( 'NONE', 3,
 ( #36985, #43402, #5986, #19674, #26975, #13077, #19452, #43625, #33562, #33796 ),
 .UNSPECIFIED., .F., .F.,
 ( 4, 3, 3, 4 ),
 ( 5.553824967135429714E-18, 0.0002476486541971044722, 0.0004952973025691070419, 0.0009610892161188180861 ),
 .UNSPECIFIED. ) ;
#19376=CARTESIAN_POINT ( 'NONE',  ( 125.3521822035780815, -2.963544489311753516, -20.18754802458934705 ) ) ;
#19380=CARTESIAN_POINT ( 'NONE',  ( 123.7022829359119811, -5.367793381288652910, -18.78638297431638904 ) ) ;
#19393=CARTESIAN_POINT ( 'NONE',  ( 124.1593615891115547, -9.675291321254654520, -19.78473021908635943 ) ) ;
#19412=CARTESIAN_POINT ( 'NONE',  ( 122.3826735609119680, 0.6414057260225851653, -11.69287257290600657 ) ) ;
#19417=CARTESIAN_POINT ( 'NONE',  ( 119.8129079359119942, -5.444069387712269226, -19.60292469916370450 ) ) ;
#19422=ORIENTED_EDGE ( 'NONE', *, *, #44066, .F. ) ;
#19452=CARTESIAN_POINT ( 'NONE',  ( 123.3883748871816266, -6.188980713775695364, -18.62212668298318619 ) ) ;
#19478=CARTESIAN_POINT ( 'NONE',  ( 124.9801526047680227, -8.159936295607842283, -6.546456203805208318 ) ) ;
#19499=CARTESIAN_POINT ( 'NONE',  ( 119.7434548109119703, -13.11073630560948722, -15.94021774473354114 ) ) ;
#19510=CARTESIAN_POINT ( 'NONE',  ( 125.0532895624267837, 1.228647770399326156, -17.81034849661567065 ) ) ;
#19540=CARTESIAN_POINT ( 'NONE',  ( 122.8688454359119646, 0.5291689781388270175, -13.89700978578772705 ) ) ;
#19549=CARTESIAN_POINT ( 'NONE',  ( 125.3570663707213839, -11.61100471653260513, -15.41365316013039255 ) ) ;
#19552=CARTESIAN_POINT ( 'NONE',  ( 119.7434548109119845, -1.456678546396870333, -17.70209537461181526 ) ) ;
#19570=CARTESIAN_POINT ( 'NONE',  ( 123.8411891859119862, -8.844754642576884152, -8.592115655440050404 ) ) ;
#19571=CARTESIAN_POINT ( 'NONE',  ( 120.7852516859119731, -9.665098340737509730, -17.37397104707595474 ) ) ;
#19594=DIRECTION ( 'NONE',  ( 0.000000000000000000, -0.4669533266896289114, -0.8842819633428518067 ) ) ;
#19596=CARTESIAN_POINT ( 'NONE',  ( 124.7061593007352371, -1.353583375765361696, -20.37564943805809747 ) ) ;
#19601=CARTESIAN_POINT ( 'NONE',  ( 124.2773744744968951, -3.869742919590428265, -21.30530514842164536 ) ) ;
#19604=CARTESIAN_POINT ( 'NONE',  ( 121.5492360609119800, -3.387241619883791355, -18.17469012370385073 ) ) ;
#19617=CARTESIAN_POINT ( 'NONE',  ( 125.4213865762419999, -9.147205927423879501, -18.78468083046782056 ) ) ;
#19626=DIRECTION ( 'NONE',  ( 0.000000000000000000, 0.4669533266896288559, 0.8842819633428518067 ) ) ;
#19640=CARTESIAN_POINT ( 'NONE',  ( 120.0212673109119805, 0.2312338769422704887, -16.08380026872395874 ) ) ;
#19644=EDGE_LOOP ( 'NONE', ( #37679, #42244, #38657, #26043 ) ) ;
#19671=DIRECTION ( 'NONE',  ( 0.000000000000000000, -0.4669533266896289114, -0.8842819633428518067 ) ) ;
#19674=CARTESIAN_POINT ( 'NONE',  ( 123.5330849628857237, -6.095137211460710525, -18.44441274085890115 ) ) ;
#19677=CARTESIAN_POINT ( 'NONE',  ( 123.4939235609119663, 0.6414057260225851653, -11.69287257290600657 ) ) ;
#19678=ORIENTED_EDGE ( 'NONE', *, *, #12758, .F. ) ;
#19697=CARTESIAN_POINT ( 'NONE',  ( 120.3925890224331710, -4.681800857092175860, -18.57451437749315559 ) ) ;
#19750=AXIS2_PLACEMENT_3D ( 'NONE', #38509, #7286, #24405 ) ;
#19755=AXIS2_PLACEMENT_3D ( 'NONE', #21892, #685, #31697 ) ;
#19756=EDGE_CURVE ( 'NONE', #22801, #24842, #18685, .T. ) ;
#19763=CARTESIAN_POINT ( 'NONE',  ( 123.9832704359119759, 0.5245030254254422486, -13.89657392289357141 ) ) ;
#19765=VERTEX_POINT ( 'NONE', #39434 ) ;
#19766=CARTESIAN_POINT ( 'NONE',  ( 122.6604860609119640, -3.387241619883791355, -18.17469012370385073 ) ) ;
#19768=DIRECTION ( 'NONE',  ( 0.000000000000000000, 0.4669533266896289669, 0.8842819633428518067 ) ) ;
#19770=CARTESIAN_POINT ( 'NONE',  ( 122.7993923109119692, -9.959231468620748373, -10.70263013195265955 ) ) ;
#19775=CARTESIAN_POINT ( 'NONE',  ( 122.6604860609119640, -3.387241619883791355, -18.17469012370385073 ) ) ;
#19778=CARTESIAN_POINT ( 'NONE',  ( 123.9138173109119663, -0.4425889791248522331, -15.72798183378621140 ) ) ;
#19780=CARTESIAN_POINT ( 'NONE',  ( 119.7434548109119845, -1.978546973019726263, -18.09349220968092098 ) ) ;
#19791=CARTESIAN_POINT ( 'NONE',  ( 124.6127514966337060, -12.64971312686726712, -14.42062521576453626 ) ) ;
#19797=FACE_OUTER_BOUND ( 'NONE', #13285, .T. ) ;
#19799=CARTESIAN_POINT ( 'NONE',  ( 120.7852516859119731, -0.6942167230862511529, -9.935906262978006609 ) ) ;
#19800=CARTESIAN_POINT ( 'NONE',  ( 119.3961891859119930, -1.406689858478933353, -17.56299727309130887 ) ) ;
#19801=ORIENTED_EDGE ( 'NONE', *, *, #25156, .T. ) ;
#19826=CARTESIAN_POINT ( 'NONE',  ( 119.7434548109119703, -2.613043214085062793, -8.928554074455437473 ) ) ;
#19827=FACE_OUTER_BOUND ( 'NONE', #34707, .T. ) ;
#19834=CARTESIAN_POINT ( 'NONE',  ( 125.1986466278897154, -1.893713009889057552, -20.10971988540413236 ) ) ;
#19837=CARTESIAN_POINT ( 'NONE',  ( 124.6746266859119743, -9.033780868592240054, -16.85052413769862056 ) ) ;
#19847=CARTESIAN_POINT ( 'NONE',  ( 122.6009548109119720, -2.421111938423274879, -5.775321541204940345 ) ) ;
#19870=CARTESIAN_POINT ( 'NONE',  ( 122.7993923109119692, -9.959231468620755479, -10.70263013195267199 ) ) ;
#19875=CARTESIAN_POINT ( 'NONE',  ( 124.6051735609119646, -9.645473719204776586, -14.86997237629376656 ) ) ;
#19938=CARTESIAN_POINT ( 'NONE',  ( 121.6186891859119896, -1.406689858478933353, -17.56299727309130887 ) ) ;
#19963=DIRECTION ( 'NONE',  ( 0.000000000000000000, -0.4669533266896281343, -0.8842819633428521398 ) ) ;
#19993=B_SPLINE_CURVE_WITH_KNOTS ( 'NONE', 3,
 ( #8048, #21279, #31536, #38587, #14894, #979, #28134, #13996, #28805, #18087, #24482, #4395, #24699, #42714, #744, #31980, #21506, #14666, #27913, #42490, #7365, #28582, #3719, #31310, #35394, #24927, #3941, #34932, #11251, #35164, #11481, #17639, #3502, #14442, #34718, #41824 ),
 .UNSPECIFIED., .F., .F.,
 ( 4, 2, 2, 2, 2, 1, 2, 2, 2, 2, 2, 2, 2, 1, 2, 2, 2, 2, 4 ),
 ( 0.000000000000000000, 0.06249999999998848144, 0.1249999999999769629, 0.1874999999999654443, 0.2187499999999629463, 0.2343749999999588385, 0.2421874999999513445, 0.2499999999999438505, 0.3749999999999300004, 0.4999999999999161782, 0.6249999999999023004, 0.6874999999998954170, 0.7187499999998919753, 0.7343749999998853140, 0.7421874999998818723, 0.7499999999998784306, 0.8124999999999107381, 0.8749999999999430456, 1.000000000000000000 ),
 .UNSPECIFIED. ) ;
#19995=CARTESIAN_POINT ( 'NONE',  ( 123.6328298109119714, -7.200787124940443817, -17.81845355600750835 ) ) ;
#20000=CARTESIAN_POINT ( 'NONE',  ( 123.0385396737536752, -8.611453504372539314, -17.77011218421760574 ) ) ;
#20022=AXIS2_PLACEMENT_3D ( 'NONE', #20564, #10087, #40869 ) ;
#20027=EDGE_LOOP ( 'NONE', ( #36927, #319, #7616, #10978 ) ) ;
#20031=CARTESIAN_POINT ( 'NONE',  ( 124.1190016859119680, -9.665098340737509730, -17.37397104707595474 ) ) ;
#20032=CARTESIAN_POINT ( 'NONE',  ( 121.4103298109119748, -7.200787124940443817, -17.81845355600750835 ) ) ;
#20069=CARTESIAN_POINT ( 'NONE',  ( 122.3826735609119680, -9.645473719204776586, -14.86997237629376656 ) ) ;
#20091=AXIS2_PLACEMENT_3D ( 'NONE', #1087, #27795, #3825 ) ;
#20107=CARTESIAN_POINT ( 'NONE',  ( 122.8688454359119646, 0.5291689781388270175, -13.89700978578772705 ) ) ;
#20139=( BOUNDED_CURVE ( )  B_SPLINE_CURVE ( 2, ( #24072, #3305, #30679, #45043, #44823, #2853, #37276, #37740, #44148 ),
 .UNSPECIFIED., .F., .T. ) 
 B_SPLINE_CURVE_WITH_KNOTS ( ( 3, 2, 2, 2, 3 ),
 ( 0.1250000000000000000, 0.1562500000000000000, 0.1875000000000000000, 0.2187500000000000000, 0.2397292404589490000 ),
 .UNSPECIFIED. ) 
 CURVE ( )  GEOMETRIC_REPRESENTATION_ITEM ( )  RATIONAL_B_SPLINE_CURVE ( ( 1.000000000000000000, 0.9238795325112869605, 1.000000000000000000, 0.9238795325112869605, 1.000000000000000000, 0.9238795325112869605, 1.000000000000000000, 0.9488976130786129781, 0.9664089390052280626 ) ) 
 REPRESENTATION_ITEM ( '' )  );
#20168=CARTESIAN_POINT ( 'NONE',  ( 121.3655035264548872, -8.247323210606168686, -17.08054893949881148 ) ) ;
#20174=CARTESIAN_POINT ( 'NONE',  ( 124.5357204359119550, -10.25716656981731489, -12.88942061488890545 ) ) ;
#20177=CARTESIAN_POINT ( 'NONE',  ( 125.1589444732338308, 2.423665151342216273, -12.11196455044497000 ) ) ;
#20225=ORIENTED_EDGE ( 'NONE', *, *, #39803, .F. ) ;
#20259=CARTESIAN_POINT ( 'NONE',  ( 121.5492360609119800, -3.387241619883791355, -18.17469012370385073 ) ) ;
#20260=CARTESIAN_POINT ( 'NONE',  ( 120.3685329359119862, -5.367793381288652910, -18.78638297431638904 ) ) ;
#20284=EDGE_CURVE ( 'NONE', #31497, #32564, #3565, .T. ) ;
#20292=CARTESIAN_POINT ( 'NONE',  ( 119.9518141859119851, -0.8832429491016019485, -18.19431474523657855 ) ) ;
#20300=EDGE_CURVE ( 'NONE', #2526, #19765, #13653, .T. ) ;
#20330=EDGE_CURVE ( 'NONE', #37005, #42142, #13208, .T. ) ;
#20331=CARTESIAN_POINT ( 'NONE',  ( 121.3408766859119794, -9.033780868592240054, -16.85052413769862056 ) ) ;
#20368=CARTESIAN_POINT ( 'NONE',  ( 119.8791860609119624, -6.339478340643393217, -8.615877017535622073 ) ) ;
#20390=CARTESIAN_POINT ( 'NONE',  ( 120.5074391859119913, -1.406689858478935573, -17.56299727309130887 ) ) ;
#20398=CARTESIAN_POINT ( 'NONE',  ( 119.8129079359119942, -5.444069387712269226, -19.60292469916370450 ) ) ;
#20401=CARTESIAN_POINT ( 'NONE',  ( 124.6565730087419581, 2.130358918975589599, -9.869583666609218042 ) ) ;
#20463=CYLINDRICAL_SURFACE ( 'NONE', #28864, 1.587500000000000355 ) ;
#20480=CARTESIAN_POINT ( 'NONE',  ( 120.7852516859119731, -9.665098340737509730, -17.37397104707595474 ) ) ;
#20487=CARTESIAN_POINT ( 'NONE',  ( 121.8965016859119856, -0.6942167230862511529, -9.935906262978006609 ) ) ;
#20488=CARTESIAN_POINT ( 'NONE',  ( 121.1325173109119788, -9.289237151508434209, -11.05642687123711276 ) ) ;
#20495=CARTESIAN_POINT ( 'NONE',  ( 120.2521385739447908, -8.245948579112495125, -17.07794576319270163 ) ) ;
#20505=CARTESIAN_POINT ( 'NONE',  ( 121.0630641859119976, -0.8832429491016019485, -18.19431474523657855 ) ) ;
#20518=CARTESIAN_POINT ( 'NONE',  ( 121.5492360609119800, -6.564341423271550902, -7.887810678476487425 ) ) ;
#20552=VERTEX_POINT ( 'NONE', #29891 ) ;
#20553=CARTESIAN_POINT ( 'NONE',  ( 123.2855641859119942, -0.8832429491016019485, -18.19431474523657855 ) ) ;
#20561=AXIS2_PLACEMENT_3D ( 'NONE', #13062, #33549, #40882 ) ;
#20564=CARTESIAN_POINT ( 'NONE',  ( 125.4584548109119737, -4.863998795839242995, -13.39321520033831447 ) ) ;
#20588=CARTESIAN_POINT ( 'NONE',  ( 119.7434548109119703, -4.863998795839242995, -13.39321520033831447 ) ) ;
#20593=CARTESIAN_POINT ( 'NONE',  ( 119.6045485609119794, -0.08252387247370887580, -11.91645802438286417 ) ) ;
#20599=CARTESIAN_POINT ( 'NONE',  ( 123.9584548109119737, 3.074545301078819737, -12.40350937470759973 ) ) ;
#20620=CARTESIAN_POINT ( 'NONE',  ( 120.3685329359119862, -4.283928203966213211, -7.183505701512925334 ) ) ;
#20653=DIRECTION ( 'NONE',  ( 0.000000000000000000, -0.4669533266896290225, -0.8842819633428516957 ) ) ;
#20687=DIRECTION ( 'NONE',  ( 0.000000000000000000, 0.4669533266896289669, 0.8842819633428516957 ) ) ;
#20703=CARTESIAN_POINT ( 'NONE',  ( 121.3408766859119794, -0.06289925094097943703, -9.412459353600674206 ) ) ;
#20708=CARTESIAN_POINT ( 'NONE',  ( 122.6604860609119640, -3.387241619883791355, -18.17469012370385073 ) ) ;
#20724=CARTESIAN_POINT ( 'NONE',  ( 121.6186891859119896, -8.844754642576884152, -8.592115655440050404 ) ) ;
#20726=EDGE_LOOP ( 'NONE', ( #11504, #35481, #3880, #27732, #25141 ) ) ;
#20731=CYLINDRICAL_SURFACE ( 'NONE', #3984, 1.587500000000000355 ) ;
#20733=DIRECTION ( 'NONE',  ( -1.000000000000000000, 0.000000000000000000, -0.000000000000000000 ) ) ;
#20738=CARTESIAN_POINT ( 'NONE',  ( 121.4797829359119987, -4.283928203966213211, -7.183505701512925334 ) ) ;
#20755=CARTESIAN_POINT ( 'NONE',  ( 123.9800954359119913, -11.07370829466463391, -12.81314460846528469 ) ) ;
#20809=CARTESIAN_POINT ( 'NONE',  ( 120.1569985609119726, -9.641336978641936284, -14.86869474514246647 ) ) ;
#20824=CARTESIAN_POINT ( 'NONE',  ( 120.7852516859119731, -0.6942167230862511529, -9.935906262978006609 ) ) ;
#20836=CARTESIAN_POINT ( 'NONE',  ( 122.5215798109119874, -7.200787124940443817, -17.81845355600750835 ) ) ;
#20839=CARTESIAN_POINT ( 'NONE',  ( 124.9063227527192765, 2.723630896063975015, -12.29189508076541415 ) ) ;
#20864=AXIS2_PLACEMENT_3D ( 'NONE', #30315, #37376, #44693 ) ;
#20886=EDGE_CURVE ( 'NONE', #32403, #11067, #946, .T. ) ;
#20908=CARTESIAN_POINT ( 'NONE',  ( 124.6051735609119646, -9.645473719204691321, -14.86997237629403301 ) ) ;
#20922=VECTOR ( 'NONE', #26324, 1000.000000000000000 ) ;
#20953=EDGE_CURVE ( 'NONE', #43475, #7179, #24262, .T. ) ;
#20959=CARTESIAN_POINT ( 'NONE',  ( 121.8965016859119856, -9.665098340737509730, -17.37397104707595474 ) ) ;
#20968=CARTESIAN_POINT ( 'NONE',  ( 121.5038390224331835, -4.681800857092175860, -18.57451437749315559 ) ) ;
#21027=CARTESIAN_POINT ( 'NONE',  ( 120.2296266859119953, -9.033780868592240054, -16.85052413769862056 ) ) ;
#21052=CARTESIAN_POINT ( 'NONE',  ( 122.7299391859119737, -8.844754642576884152, -8.592115655440050404 ) ) ;
#21053=EDGE_LOOP ( 'NONE', ( #25788, #33986, #2476, #24003 ) ) ;
#21063=CARTESIAN_POINT ( 'NONE',  ( 119.7434548109119703, -5.696008164919469152, -19.01495265173020499 ) ) ;
#21104=AXIS2_PLACEMENT_3D ( 'NONE', #7620, #28833, #7392 ) ;
#21107=DIRECTION ( 'NONE',  ( -1.000000000000000000, 0.000000000000000000, -0.000000000000000000 ) ) ;
#21142=CARTESIAN_POINT ( 'NONE',  ( 123.6328298109119714, -7.200787124940443817, -17.81845355600750835 ) ) ;
#21151=CIRCLE ( 'NONE', #1472, 8.000000000000001776 ) ;
#21177=CARTESIAN_POINT ( 'NONE',  ( 123.4939235609119663, 0.6414057260225851653, -11.69287257290600657 ) ) ;
#21191=CARTESIAN_POINT ( 'NONE',  ( 125.3666772207509865, -8.500505272813764890, -17.56000656032637153 ) ) ;
#21216=PRODUCT_DEFINITION_SHAPE ( 'NONE', 'NONE',  #12711 ) ;
#21227=CARTESIAN_POINT ( 'NONE',  ( 123.1158699480702552, -6.365377317481717867, -18.95617363400926081 ) ) ;
#21276=CARTESIAN_POINT ( 'NONE',  ( 124.5487329937728873, -9.861982936719853043, -13.21808400482192880 ) ) ;
#21277=CARTESIAN_POINT ( 'NONE',  ( 122.1048610609119720, -3.163656168406935087, -18.89861972220014508 ) ) ;
#21279=CARTESIAN_POINT ( 'NONE',  ( 124.0650380271176800, -2.421111565351928618, -5.775362573634398089 ) ) ;
#21303=CARTESIAN_POINT ( 'NONE',  ( 123.9584548109119737, -1.204716393658298523, -20.50726132761981901 ) ) ;
#21306=CARTESIAN_POINT ( 'NONE',  ( 121.8139395652850538, -6.239497348973043422, -18.71779138178828106 ) ) ;
#21360=CARTESIAN_POINT ( 'NONE',  ( 121.1325173109119788, 0.2312338769422704887, -16.08380026872395874 ) ) ;
#21382=CARTESIAN_POINT ( 'NONE',  ( 123.2855641859119942, -0.8832429491016019485, -18.19431474523657855 ) ) ;
#21398=CARTESIAN_POINT ( 'NONE',  ( 123.9584548109119737, -12.48189245497263755, -10.95032834292243074 ) ) ;
#21400=CARTESIAN_POINT ( 'NONE',  ( 121.0630641859119976, -0.8832429491016019485, -18.19431474523657855 ) ) ;
#21473=CARTESIAN_POINT ( 'NONE',  ( 120.1028830209070293, -6.157706758239399392, -18.56290235964623392 ) ) ;
#21479=ORIENTED_EDGE ( 'NONE', *, *, #31983, .T. ) ;
#21502=CARTESIAN_POINT ( 'NONE',  ( 124.5476740651314884, -9.860788299936581680, -13.18793303030140329 ) ) ;
#21503=CARTESIAN_POINT ( 'NONE',  ( 122.9382985609119743, -10.36940331770106916, -15.09355782777062061 ) ) ;
#21506=CARTESIAN_POINT ( 'NONE',  ( 125.3296504289734798, -1.968006290854414697, -6.888848368006928347 ) ) ;
#21530=CARTESIAN_POINT ( 'NONE',  ( 121.7663437114597258, -6.208002839291213881, -18.65814938918611077 ) ) ;
#21539=DIRECTION ( 'NONE',  ( 0.000000000000000000, 0.4669533266896289669, 0.8842819633428516957 ) ) ;
#21566=CARTESIAN_POINT ( 'NONE',  ( 123.4244704359119709, -10.25716656981731489, -12.88942061488890545 ) ) ;
#21586=CARTESIAN_POINT ( 'NONE',  ( 120.4379860609119675, -3.387241619883791355, -18.17469012370385073 ) ) ;
#21605=CARTESIAN_POINT ( 'NONE',  ( 122.5910329359119970, -4.283928203966213211, -7.183505701512925334 ) ) ;
#21610=CARTESIAN_POINT ( 'NONE',  ( 121.8965016859119856, -9.665098340737509730, -17.37397104707595474 ) ) ;
#21632=AXIS2_PLACEMENT_3D ( 'NONE', #5406, #1982, #15909 ) ;
#21635=CARTESIAN_POINT ( 'NONE',  ( 123.5880035264548837, -8.247323210606174015, -17.08054893949881858 ) ) ;
#21649=DIRECTION ( 'NONE',  ( 0.000000000000000000, 0.000000000000000000, 1.000000000000000000 ) ) ;
#21657=MANIFOLD_SOLID_BREP ( 'NONE', #3933 ) ;
#21680=FACE_OUTER_BOUND ( 'NONE', #10375, .T. ) ;
#21717=CARTESIAN_POINT ( 'NONE',  ( 123.2161110609119703, -6.340755971794695078, -8.611740276972781771 ) ) ;
#21730=CARTESIAN_POINT ( 'NONE',  ( 124.5402294140156698, -9.847276183098475855, -12.97714367041513839 ) ) ;
#21731=CARTESIAN_POINT ( 'NONE',  ( 122.4521266859119635, -0.06289925094097943703, -9.412459353600674206 ) ) ;
#21757=CARTESIAN_POINT ( 'NONE',  ( 121.4551560953690483, -6.001247023715324147, -18.26661038929047010 ) ) ;
#21809=CARTESIAN_POINT ( 'NONE',  ( 119.7434548109119703, -2.527210466738041728, -8.967976844669124148 ) ) ;
#21829=CARTESIAN_POINT ( 'NONE',  ( 122.3826735609119680, 0.6414057260225851653, -11.69287257290600657 ) ) ;
#21830=CARTESIAN_POINT ( 'NONE',  ( 119.7434548109119703, -9.722663502801697888, -19.87444018218530317 ) ) ;
#21833=CARTESIAN_POINT ( 'NONE',  ( 122.3826735609119680, 0.6414057260225851653, -11.69287257290600657 ) ) ;
#21846=CARTESIAN_POINT ( 'NONE',  ( 124.1685108350158515, -12.47056798417068180, -10.95034471803594833 ) ) ;
#21865=FACE_OUTER_BOUND ( 'NONE', #40, .T. ) ;
#21892=CARTESIAN_POINT ( 'NONE',  ( 123.9584548109119737, -4.863998795839242995, -13.39321520033831447 ) ) ;
#21935=CARTESIAN_POINT ( 'NONE',  ( 124.6746266859119743, -9.033780868592240054, -16.85052413769862056 ) ) ;
#21944=ORIENTED_EDGE ( 'NONE', *, *, #16655, .F. ) ;
#21949=CARTESIAN_POINT ( 'NONE',  ( 124.5787747700264276, -9.818244482720213995, -14.09103721618573601 ) ) ;
#21950=CARTESIAN_POINT ( 'NONE',  ( 120.9241579359119925, -5.444069387712269226, -19.60292469916370450 ) ) ;
#21951=ORIENTED_EDGE ( 'NONE', *, *, #18619, .F. ) ;
#21997=VERTEX_POINT ( 'NONE', #34600 ) ;
#22017=CARTESIAN_POINT ( 'NONE',  ( 123.0385396737536752, -8.611453504372539314, -17.77011218421760574 ) ) ;
#22030=CARTESIAN_POINT ( 'NONE',  ( 124.0650380271193995, 2.753853830864835484, -15.83610243082555691 ) ) ;
#22036=CARTESIAN_POINT ( 'NONE',  ( 121.8270485609119760, -0.08252387247370887580, -11.91645802438286417 ) ) ;
#22057=CARTESIAN_POINT ( 'NONE',  ( 122.7993923109119692, -9.959231468620755479, -10.70263013195267199 ) ) ;
#22061=CARTESIAN_POINT ( 'NONE',  ( 122.7299391859119737, -8.844754642576884152, -8.592115655440050404 ) ) ;
#22070=CARTESIAN_POINT ( 'NONE',  ( 124.5079745746482871, -9.690323912439273712, -12.08684339900582749 ) ) ;
#22077=CARTESIAN_POINT ( 'NONE',  ( 124.3692356341927336, -12.42554980965305766, -10.94897534285865426 ) ) ;
#22096=CARTESIAN_POINT ( 'NONE',  ( 122.9382985609119743, -10.36940331770106916, -15.09355782777062061 ) ) ;
#22108=( GEOMETRIC_REPRESENTATION_CONTEXT ( 3 ) GLOBAL_UNCERTAINTY_ASSIGNED_CONTEXT ( ( #38801 ) ) GLOBAL_UNIT_ASSIGNED_CONTEXT ( ( #15721, #33251, #16176 ) ) REPRESENTATION_CONTEXT ( 'NONE', 'WORKASPACE' ) );
#22118=ORIENTED_EDGE ( 'NONE', *, *, #5344, .T. ) ;
#22122=CARTESIAN_POINT ( 'NONE',  ( 124.1546421904525346, -1.211725351588312183, -20.50025038867522653 ) ) ;
#22123=FACE_OUTER_BOUND ( 'NONE', #26230, .T. ) ;
#22146=CARTESIAN_POINT ( 'NONE',  ( 119.9638582044368320, -6.247802574075781656, -18.73351920797576042 ) ) ;
#22147=CARTESIAN_POINT ( 'NONE',  ( 125.4584548109119737, -12.49632558250451986, -9.362893955355607645 ) ) ;
#22160=ORIENTED_EDGE ( 'NONE', *, *, #33064, .F. ) ;
#22161=CARTESIAN_POINT ( 'NONE',  ( 120.1601735609119856, 0.6414057260225851653, -11.69287257290600657 ) ) ;
#22173=CARTESIAN_POINT ( 'NONE',  ( 124.5933994731490202, -9.737703366526362814, -14.52892336661181005 ) ) ;
#22203=CARTESIAN_POINT ( 'NONE',  ( 121.7187960087704113, -6.176492496456559955, -18.59847741292036716 ) ) ;
#22223=LINE ( 'NONE', #8099, #20922 ) ;
#22251=CARTESIAN_POINT ( 'NONE',  ( 125.1433143116076394, 2.106814825465578522, -15.97349185543337668 ) ) ;
#22258=CARTESIAN_POINT ( 'NONE',  ( 121.2019704359119743, -10.25716656981731489, -12.88942061488890545 ) ) ;
#22278=EDGE_CURVE ( 'NONE', #2517, #1411, #10053, .T. ) ;
#22285=CARTESIAN_POINT ( 'NONE',  ( 121.7575954359119805, -11.07370829466463569, -12.81314460846529002 ) ) ;
#22288=CARTESIAN_POINT ( 'NONE',  ( 122.5664060953690466, -6.001247023715324147, -18.26661038929047010 ) ) ;
#22293=CARTESIAN_POINT ( 'NONE',  ( 124.5262951945957042, -9.799039402788389808, -12.58795091330891580 ) ) ;
#22297=CARTESIAN_POINT ( 'NONE',  ( 125.2382274389888295, -12.00999942234432538, -14.79627280731742012 ) ) ;
#22318=CARTESIAN_POINT ( 'NONE',  ( 123.7717360609119623, -6.564341423271550902, -7.887810678476487425 ) ) ;
#22336=EDGE_CURVE ( 'NONE', #13270, #24335, #4497, .T. ) ;
#22350=CARTESIAN_POINT ( 'NONE',  ( 125.3086838498437317, -2.252769241038413472, -20.05322569067225658 ) ) ;
#22384=CARTESIAN_POINT ( 'NONE',  ( 122.2437673109119629, -9.289237151508434209, -11.05642687123711276 ) ) ;
#22422=B_SPLINE_CURVE_WITH_KNOTS ( 'NONE', 3,
 ( #30095, #33035, #1810, #29639, #44011, #26220, #34173, #41714, #10478, #6602 ),
 .UNSPECIFIED., .F., .F.,
 ( 4, 3, 3, 4 ),
 ( 8.545274078289149956E-18, 0.0002476486541971030086, 0.0004952973025691040062, 0.0009610892161188130988 ),
 .UNSPECIFIED. ) ;
#22446=CARTESIAN_POINT ( 'NONE',  ( 124.6574308310800916, -5.898449491513396481, -5.630628696673196210 ) ) ;
#22489=ORIENTED_EDGE ( 'NONE', *, *, #16802, .F. ) ;
#22496=EDGE_CURVE ( 'NONE', #19765, #45054, #961, .T. ) ;
#22515=CARTESIAN_POINT ( 'NONE',  ( 125.3282169345246189, -11.52192247331090158, -15.89464684586357279 ) ) ;
#22537=CARTESIAN_POINT ( 'NONE',  ( 123.1466579359119891, -5.444069387712269226, -19.60292469916370450 ) ) ;
#22538=CARTESIAN_POINT ( 'NONE',  ( 120.2990798109119766, -2.173413727453600508, -8.297982527556802879 ) ) ;
#22568=CARTESIAN_POINT ( 'NONE',  ( 125.2180320564445282, -1.939873832223439898, -20.09786755395826674 ) ) ;
#22591=CARTESIAN_POINT ( 'NONE',  ( 119.7434548109119703, -13.11073630560948722, -15.94021774473354114 ) ) ;
#22605=CARTESIAN_POINT ( 'NONE',  ( 120.8547048109119686, -7.554583864224885481, -18.48844787311982785 ) ) ;
#22606=CIRCLE ( 'NONE', #33521, 8.000000000000001776 ) ;
#22649=ORIENTED_EDGE ( 'NONE', *, *, #2480, .T. ) ;
#22663=VECTOR ( 'NONE', #23738, 1000.000000000000000 ) ;
#22670=CARTESIAN_POINT ( 'NONE',  ( 125.0532895624264569, -6.048765590996615593, -5.961678590775178144 ) ) ;
#22673=CARTESIAN_POINT ( 'NONE',  ( 120.7157985609119635, -0.08252387247370887580, -11.91645802438286417 ) ) ;
#22697=( BOUNDED_CURVE ( )  B_SPLINE_CURVE ( 2, ( #42152, #38705, #7472, #31644, #3608, #31422, #187 ),
 .UNSPECIFIED., .F., .F. ) 
 B_SPLINE_CURVE_WITH_KNOTS ( ( 3, 2, 2, 3 ),
 ( 0.4999999999999819589, 0.6249999999999900080, 0.7500000000000000000, 0.7837465698629629829 ),
 .UNSPECIFIED. ) 
 CURVE ( )  GEOMETRIC_REPRESENTATION_ITEM ( )  RATIONAL_B_SPLINE_CURVE ( ( 1.000000000000000000, 0.9238795325112759693, 1.000000000000000000, 0.9238795325112869605, 1.000000000000000000, 0.9794495626071260119, 0.9699952335533410519 ) ) 
 REPRESENTATION_ITEM ( '' )  );
#22700=CARTESIAN_POINT ( 'NONE',  ( 125.0849378844218478, 1.217985041202279461, -17.76587250167452936 ) ) ;
#22711=CARTESIAN_POINT ( 'NONE',  ( 124.5203963484541703, -8.366382308237135135, -17.30601432669995532 ) ) ;
#22725=DIRECTION ( 'NONE',  ( 0.000000000000000000, -0.4669533266896290225, -0.8842819633428516957 ) ) ;
#22729=CARTESIAN_POINT ( 'NONE',  ( 124.3741441133336991, 3.029370655639220367, -12.39654276031037305 ) ) ;
#22734=CARTESIAN_POINT ( 'NONE',  ( 121.8755514478796442, -9.877548923986811502, -16.68609415519376427 ) ) ;
#22736=CARTESIAN_POINT ( 'NONE',  ( 125.3159867104938456, -11.52188856829479491, -15.97039513045710102 ) ) ;
#22757=CARTESIAN_POINT ( 'NONE',  ( 122.0354079359119908, -5.444069387712269226, -19.60292469916370450 ) ) ;
#22758=CARTESIAN_POINT ( 'NONE',  ( 123.4939235609119663, 0.6414057260225851653, -11.69287257290600657 ) ) ;
#22773=( BOUNDED_CURVE ( )  B_SPLINE_CURVE ( 2, ( #26547, #19697, #6246, #20390, #23351, #6009, #12878, #29965, #30865, #26778, #40687, #23589, #9671, #33357, #44788, #13546, #20168 ),
 .UNSPECIFIED., .F., .T. ) 
 B_SPLINE_CURVE_WITH_KNOTS ( ( 3, 2, 2, 2, 2, 2, 2, 2, 3 ),
 ( 0.2602707595410510000, 0.2812500000000000000, 0.3125000000000000000, 0.3437500000000000000, 0.3750000000000000000, 0.4062500000000000000, 0.4375000000000000000, 0.4687500000000000000, 0.4897292404589490000 ),
 .UNSPECIFIED. ) 
 CURVE ( )  GEOMETRIC_REPRESENTATION_ITEM ( )  RATIONAL_B_SPLINE_CURVE ( ( 0.9664089390052280626, 0.9488976130786129781, 1.000000000000000000, 0.9238795325112869605, 1.000000000000000000, 0.9238795325112869605, 1.000000000000000000, 0.9238795325112869605, 1.000000000000000000, 0.9238795325112869605, 1.000000000000000000, 0.9238795325112869605, 1.000000000000000000, 0.9238795325112869605, 1.000000000000000000, 0.9488976130786129781, 0.9664089390052280626 ) ) 
 REPRESENTATION_ITEM ( '' )  );
#22778=EDGE_CURVE ( 'NONE', #23986, #37731, #4224, .T. ) ;
#22793=CARTESIAN_POINT ( 'NONE',  ( 125.2222176290895845, -1.950389891022559663, -20.09533972395541568 ) ) ;
#22796=CARTESIAN_POINT ( 'NONE',  ( 124.1884548109119777, -2.527210466738041728, -8.967976844669124148 ) ) ;
#22801=VERTEX_POINT ( 'NONE', #27970 ) ;
#22810=CARTESIAN_POINT ( 'NONE',  ( 125.2714945850566863, -9.321016064732583928, -19.11382972112425804 ) ) ;
#22811=CARTESIAN_POINT ( 'NONE',  ( 124.3273610609119686, -6.340755971794695078, -8.611740276972781771 ) ) ;
#22815=B_SPLINE_CURVE_WITH_KNOTS ( 'NONE', 3,
 ( #14285, #9984, #28204, #17480, #38440, #7210, #37554, #41447, #3781, #42111 ),
 .UNSPECIFIED., .F., .F.,
 ( 4, 3, 3, 4 ),
 ( 3.127317220692749988E-18, 0.0002476486808869860054, 0.0004952973797228679611, 0.0009539399846111490172 ),
 .UNSPECIFIED. ) ;
#22837=CARTESIAN_POINT ( 'NONE',  ( 124.5357204359119550, -10.25716656981731489, -12.88942061488890545 ) ) ;
#22871=CARTESIAN_POINT ( 'NONE',  ( 125.4584548109119737, -8.245233026025740486, -17.07659070123625611 ) ) ;
#22894=CARTESIAN_POINT ( 'NONE',  ( 124.0650380271182200, -8.523251919909833774, -6.279197823564533820 ) ) ;
#22899=CARTESIAN_POINT ( 'NONE',  ( 120.5768923109119868, -0.4387604401700512802, -15.73000352943951619 ) ) ;
#22959=CARTESIAN_POINT ( 'NONE',  ( 125.0480389746925738, 2.573808657167731440, -12.21219197517087096 ) ) ;
#22965=CARTESIAN_POINT ( 'NONE',  ( 120.9936110609119737, -3.163656168406939528, -18.89861972220014152 ) ) ;
#22968=CARTESIAN_POINT ( 'NONE',  ( 125.2909043387969490, -11.52983536252548546, -16.08521104921829448 ) ) ;
#22972=LINE ( 'NONE', #3511, #33513 ) ;
#22988=EDGE_LOOP ( 'NONE', ( #17133, #39952, #14674, #6521 ) ) ;
#22990=CARTESIAN_POINT ( 'NONE',  ( 120.4379860609119675, -3.387241619883791355, -18.17469012370385073 ) ) ;
#22991=CARTESIAN_POINT ( 'NONE',  ( 122.2437673109119629, 0.2312338769422704887, -16.08380026872395874 ) ) ;
#22993=CARTESIAN_POINT ( 'NONE',  ( 123.8290266009169045, -8.403782945130243931, -17.37684090985457885 ) ) ;
#23012=ORIENTED_EDGE ( 'NONE', *, *, #24771, .F. ) ;
#23016=CARTESIAN_POINT ( 'NONE',  ( 119.8115785246182412, -4.413224050718078217, -8.020953925612355206 ) ) ;
#23017=CARTESIAN_POINT ( 'NONE',  ( 124.4330791887808516, -1.261433387662844297, -20.45354594542311588 ) ) ;
#23020=B_SPLINE_CURVE_WITH_KNOTS ( 'NONE', 3,
 ( #44632, #13830, #13396, #38210, #3995, #31592, #37769, #6542, #17041, #31367 ),
 .UNSPECIFIED., .F., .F.,
 ( 4, 3, 3, 4 ),
 ( 6.254634441385499976E-18, 0.0002476486541971024665, 0.0004952973025691019462, 0.0009610892161188130988 ),
 .UNSPECIFIED. ) ;
#23022=CARTESIAN_POINT ( 'NONE',  ( 125.0921134857867827, -3.652124968999053145, -20.77843945995303088 ) ) ;
#23027=CARTESIAN_POINT ( 'NONE',  ( 121.8270485609119760, -0.08252387247370887580, -11.91645802438286417 ) ) ;
#23052=CARTESIAN_POINT ( 'NONE',  ( 124.5059548109119731, -9.675232987814487373, -12.03232374619203249 ) ) ;
#23067=CARTESIAN_POINT ( 'NONE',  ( 124.7440798109119697, -7.200787124940443817, -17.81845355600750835 ) ) ;
#23078=AXIS2_PLACEMENT_3D ( 'NONE', #44002, #4782, #38046 ) ;
#23109=CARTESIAN_POINT ( 'NONE',  ( 119.6045485609119794, -0.08252387247370887580, -11.91645802438286417 ) ) ;
#23136=CARTESIAN_POINT ( 'NONE',  ( 121.2019704359119743, -10.25716656981731489, -12.88942061488890545 ) ) ;
#23139=EDGE_CURVE ( 'NONE', #11067, #1412, #33923, .T. ) ;
#23161=CARTESIAN_POINT ( 'NONE',  ( 125.2183010572640853, 1.181151835247190141, -17.51410646645848956 ) ) ;
#23177=ORIENTED_EDGE ( 'NONE', *, *, #17225, .F. ) ;
#23191=CARTESIAN_POINT ( 'NONE',  ( 122.0354079359119908, -4.360204210389833968, -8.000047426360245240 ) ) ;
#23196=CARTESIAN_POINT ( 'NONE',  ( 122.2437673109119629, 0.2312338769422687679, -16.08380026872396229 ) ) ;
#23205=CARTESIAN_POINT ( 'NONE',  ( 119.7434548109119845, 0.1464806637125226352, -15.28762191210849153 ) ) ;
#23224=CARTESIAN_POINT ( 'NONE',  ( 121.9659548109119811, -7.554583864224885481, -18.48844787311982785 ) ) ;
#23225=CARTESIAN_POINT ( 'NONE',  ( 120.8547048109119686, -2.527210466738041728, -8.967976844669124148 ) ) ;
#23254=CARTESIAN_POINT ( 'NONE',  ( 125.1861822135562079, -1.866968678097731260, -20.11746626182562991 ) ) ;
#23257=CARTESIAN_POINT ( 'NONE',  ( 123.5633766859119760, -9.033780868592240054, -16.85052413769862056 ) ) ;
#23270=EDGE_LOOP ( 'NONE', ( #18173, #463, #37489, #27019, #11115 ) ) ;
#23293=CARTESIAN_POINT ( 'NONE',  ( 123.5633766859119760, -9.033780868592240054, -16.85052413769862056 ) ) ;
#23351=CARTESIAN_POINT ( 'NONE',  ( 120.5768923109119868, -0.4387604401700512802, -15.73000352943951619 ) ) ;
#23416=CARTESIAN_POINT ( 'NONE',  ( 123.7749110609119754, -3.388519251034822766, -18.17055338314092694 ) ) ;
#23418=VERTEX_POINT ( 'NONE', #11487 ) ;
#23433=CARTESIAN_POINT ( 'NONE',  ( 123.7022829359119953, -5.367793381288350041, -18.78638297431641391 ) ) ;
#23435=CARTESIAN_POINT ( 'NONE',  ( 119.7434548109119845, -6.180136000736347945, -18.94341591693292415 ) ) ;
#23449=B_SPLINE_CURVE_WITH_KNOTS ( 'NONE', 3,
 ( #26396, #23435, #5632, #21063, #40999, #23664, #6323, #34127, #33894, #34941, #95, #17428, #30264, #3728, #27923, #19780, #36862, #19552, #33430, #2209, #37319, #30039, #9517, #33662, #43956, #9297, #23205, #2439, #2664, #6090, #16597, #16362, #44190, #12952, #26848, #30490, #40761, #25168, #7374, #42723, #4178, #42054, #752, #28815 ),
 .UNSPECIFIED., .F., .F.,
 ( 4, 2, 2, 2, 2, 2, 2, 2, 2, 2, 2, 2, 2, 2, 2, 2, 2, 2, 2, 2, 2, 4 ),
 ( 0.000000000000000000, 0.03124999999999984041, 0.06249999999999968081, 0.1249999999999993616, 0.1874999999999988898, 0.2187499999999985567, 0.2499999999999982236, 0.2812499999999978906, 0.3124999999999975575, 0.3749999999999973355, 0.4374999999999970579, 0.4687499999999972244, 0.4999999999999973910, 0.5312499999999975575, 0.5624999999999976685, 0.6249999999999980016, 0.6874999999999983347, 0.7499999999999986677, 0.8124999999999991118, 0.8749999999999994449, 0.9374999999999997780, 1.000000000000000000 ),
 .UNSPECIFIED. ) ;
#23451=ORIENTED_EDGE ( 'NONE', *, *, #44066, .T. ) ;
#23455=CARTESIAN_POINT ( 'NONE',  ( 123.4939235609119663, 0.6414057260225851653, -11.69287257290600657 ) ) ;
#23456=CARTESIAN_POINT ( 'NONE',  ( 119.9518141859119851, -8.321307733199551748, -9.223433127585318303 ) ) ;
#23470=AXIS2_PLACEMENT_3D ( 'NONE', #29932, #40881, #35054 ) ;
#23493=CARTESIAN_POINT ( 'NONE',  ( 119.8129079359119942, -5.444069387712269226, -19.60292469916370450 ) ) ;
#23498=ORIENTED_EDGE ( 'NONE', *, *, #16469, .T. ) ;
#23507=CARTESIAN_POINT ( 'NONE',  ( 125.4584548109119453, -9.057393577726255529, -18.61460078952223895 ) ) ;
#23510=CARTESIAN_POINT ( 'NONE',  ( 124.1497896737536877, -8.611453504372539314, -17.77011218421760574 ) ) ;
#23526=CARTESIAN_POINT ( 'NONE',  ( 123.2855641859119942, -0.8832429491016019485, -18.19431474523657855 ) ) ;
#23532=CARTESIAN_POINT ( 'NONE',  ( 123.8411891859119862, -1.406689858478933353, -17.56299727309130887 ) ) ;
#23535=COLOUR_RGB ( '',0.7921568627450980005, 0.8196078431372548767, 0.9333333333333333481 ) ;
#23539=CIRCLE ( 'NONE', #36619, 8.000000000000001776 ) ;
#23543=B_SPLINE_CURVE_WITH_KNOTS ( 'NONE', 3,
 ( #32118, #25068, #38961, #8188, #35071, #14354, #28494, #4072, #4302, #28941 ),
 .UNSPECIFIED., .F., .F.,
 ( 4, 3, 3, 4 ),
 ( 5.356661003234389743E-18, 0.0002476486541971049601, 0.0004952973025691059577, 0.0009610892161188140746 ),
 .UNSPECIFIED. ) ;
#23570=CARTESIAN_POINT ( 'NONE',  ( 119.3267360609119692, -3.387241619883791355, -18.17469012370385073 ) ) ;
#23573=CARTESIAN_POINT ( 'NONE',  ( 123.0772048109119652, -2.527210466738041728, -8.967976844669124148 ) ) ;
#23589=CARTESIAN_POINT ( 'NONE',  ( 121.0630641859119976, -8.321307733199551748, -9.223433127585318303 ) ) ;
#23595=CARTESIAN_POINT ( 'NONE',  ( 123.9800954359119771, 0.5291689781388270175, -13.89700978578772705 ) ) ;
#23600=CARTESIAN_POINT ( 'NONE',  ( 122.6009548109119720, 2.250047331442289966, -9.733932798157443500 ) ) ;
#23604=ORIENTED_EDGE ( 'NONE', *, *, #37614, .F. ) ;
#23619=CARTESIAN_POINT ( 'NONE',  ( 123.9584548109119737, -4.863998795839242995, -13.39321520033831447 ) ) ;
#23625=CARTESIAN_POINT ( 'NONE',  ( 119.7434548109119703, -11.97804492312076086, -17.05249760251924229 ) ) ;
#23648=AXIS2_PLACEMENT_3D ( 'NONE', #17750, #20733, #34613 ) ;
#23653=CARTESIAN_POINT ( 'NONE',  ( 122.5215798109119874, -2.173413727453597843, -8.297982527556802879 ) ) ;
#23662=CARTESIAN_POINT ( 'NONE',  ( 124.1221766859119811, -0.6978242514987066381, -9.938897388174217085 ) ) ;
#23664=CARTESIAN_POINT ( 'NONE',  ( 119.7434548109119561, -5.045040375314679082, -19.05184332167395667 ) ) ;
#23685=CARTESIAN_POINT ( 'NONE',  ( 123.2161110609119703, -6.340755971794695078, -8.611740276972781771 ) ) ;
#23686=CARTESIAN_POINT ( 'NONE',  ( 119.2572829359120021, -5.367793381288652910, -18.78638297431638904 ) ) ;
#23697=CARTESIAN_POINT ( 'NONE',  ( 122.6009548109119720, 3.074545301078819737, -12.40350937470759973 ) ) ;
#23705=CARTESIAN_POINT ( 'NONE',  ( 120.5074391859119913, -8.844754642576884152, -8.592115655440050404 ) ) ;
#23712=DIRECTION ( 'NONE',  ( 0.000000000000000000, 0.4669533266896290225, 0.8842819633428516957 ) ) ;
#23720=CARTESIAN_POINT ( 'NONE',  ( 123.4244704359119709, -10.25716656981731489, -12.88942061488890545 ) ) ;
#23725=ORIENTED_EDGE ( 'NONE', *, *, #40662, .T. ) ;
#23738=DIRECTION ( 'NONE',  ( -1.000000000000000000, 0.000000000000000000, -0.000000000000000000 ) ) ;
#23758=CARTESIAN_POINT ( 'NONE',  ( 122.3132204359119868, -10.25716656981731489, -12.88942061488890545 ) ) ;
#23794=( BOUNDED_SURFACE ( )  B_SPLINE_SURFACE ( 1, 2, ( 
 ( #43976, #15705, #25744, #43295, #12065, #15934, #43068, #29833, #22538, #19348, #15248, #40098, #25967, #43750, #8857, #19571, #29155, #4980, #19121, #12517, #5202, #26415, #1779, #16159, #4754, #8187, #33005, #11836, #30063, #5431, #33235, #40325, #36658, #12291, #2230, #9089, #22991, #39872, #12740, #36881, #29383, #5651, #2008, #33450, #26642, #29607, #22096, #35983, #26189, #36435, #18675, #32567, #39650, #1555, #22758, #1334, #8413, #18892, #22318, #36213, #32783, #15477, #30284, #9774, #33685 ),
 ( #2460, #23686, #37575, #19800, #17070, #6346, #3149, #27328, #27098, #30962, #41245, #23456, #10004, #23913, #44210, #37795, #2685, #20260, #26868, #44886, #34146, #5879, #27552, #41020, #23225, #6570, #16382, #13424, #20488, #2915, #12972, #13643, #20032, #41464, #37104, #16846, #40783, #37341, #9541, #6113, #33914, #34367, #30738, #16616, #10223, #40556, #9316, #30509, #44430, #13198, #44661, #12430, #1918, #26330, #32920, #26787, #32700, #1471, #9006, #8551, #29742, #11978, #2139, #8771, #43654 ) ),
 .UNSPECIFIED., .F., .F., .T. ) 
 B_SPLINE_SURFACE_WITH_KNOTS ( ( 2, 2 ),
 ( 3, 2, 2, 2, 2, 2, 2, 2, 2, 2, 2, 2, 2, 2, 2, 2, 2, 2, 2, 2, 2, 2, 2, 2, 2, 2, 2, 2, 2, 2, 2, 2, 3 ),
 ( 0.000000000000000000, 1.000000000000000000 ),
 ( 0.000000000000000000, 0.03125000000000000000, 0.06250000000000000000, 0.09375000000000000000, 0.1250000000000000000, 0.1562500000000000000, 0.1875000000000000000, 0.2187500000000000000, 0.2500000000000000000, 0.2812500000000000000, 0.3125000000000000000, 0.3437500000000000000, 0.3750000000000000000, 0.4062500000000000000, 0.4375000000000000000, 0.4687500000000000000, 0.5000000000000000000, 0.5312500000000000000, 0.5625000000000000000, 0.5937500000000000000, 0.6250000000000000000, 0.6562500000000000000, 0.6875000000000000000, 0.7187500000000000000, 0.7500000000000000000, 0.7812500000000000000, 0.8125000000000000000, 0.8437500000000000000, 0.8750000000000000000, 0.9062500000000000000, 0.9375000000000000000, 0.9687500000000000000, 1.000000000000000000 ),
 .UNSPECIFIED. ) 
 GEOMETRIC_REPRESENTATION_ITEM ( )  RATIONAL_B_SPLINE_SURFACE ( (
 ( 1.000000000000000000, 0.9238795325112869605, 1.000000000000000000, 0.9238795325112869605, 1.000000000000000000, 0.9238795325112869605, 1.000000000000000000, 0.9238795325112869605, 1.000000000000000000, 0.9238795325112869605, 1.000000000000000000, 0.9238795325112869605, 1.000000000000000000, 0.9238795325112869605, 1.000000000000000000, 0.9238795325112869605, 1.000000000000000000, 0.9238795325112869605, 1.000000000000000000, 0.9238795325112869605, 1.000000000000000000, 0.9238795325112869605, 1.000000000000000000, 0.9238795325112869605, 1.000000000000000000, 0.9238795325112869605, 1.000000000000000000, 0.9238795325112869605, 1.000000000000000000, 0.9238795325112869605, 1.000000000000000000, 0.9238795325112869605, 1.000000000000000000, 0.9238795325112869605, 1.000000000000000000, 0.9238795325112869605, 1.000000000000000000, 0.9238795325112869605, 1.000000000000000000, 0.9238795325112869605, 1.000000000000000000, 0.9238795325112869605, 1.000000000000000000, 0.9238795325112869605, 1.000000000000000000, 0.9238795325112869605, 1.000000000000000000, 0.9238795325112869605, 1.000000000000000000, 0.9238795325112869605, 1.000000000000000000, 0.9238795325112869605, 1.000000000000000000, 0.9238795325112869605, 1.000000000000000000, 0.9238795325112869605, 1.000000000000000000, 0.9238795325112869605, 1.000000000000000000, 0.9238795325112869605, 1.000000000000000000, 0.9238795325112869605, 1.000000000000000000, 0.9238795325112869605, 1.000000000000000000),
 ( 1.000000000000000000, 0.9238795325112869605, 1.000000000000000000, 0.9238795325112869605, 1.000000000000000000, 0.9238795325112869605, 1.000000000000000000, 0.9238795325112869605, 1.000000000000000000, 0.9238795325112869605, 1.000000000000000000, 0.9238795325112869605, 1.000000000000000000, 0.9238795325112869605, 1.000000000000000000, 0.9238795325112869605, 1.000000000000000000, 0.9238795325112869605, 1.000000000000000000, 0.9238795325112869605, 1.000000000000000000, 0.9238795325112869605, 1.000000000000000000, 0.9238795325112869605, 1.000000000000000000, 0.9238795325112869605, 1.000000000000000000, 0.9238795325112869605, 1.000000000000000000, 0.9238795325112869605, 1.000000000000000000, 0.9238795325112869605, 1.000000000000000000, 0.9238795325112869605, 1.000000000000000000, 0.9238795325112869605, 1.000000000000000000, 0.9238795325112869605, 1.000000000000000000, 0.9238795325112869605, 1.000000000000000000, 0.9238795325112869605, 1.000000000000000000, 0.9238795325112869605, 1.000000000000000000, 0.9238795325112869605, 1.000000000000000000, 0.9238795325112869605, 1.000000000000000000, 0.9238795325112869605, 1.000000000000000000, 0.9238795325112869605, 1.000000000000000000, 0.9238795325112869605, 1.000000000000000000, 0.9238795325112869605, 1.000000000000000000, 0.9238795325112869605, 1.000000000000000000, 0.9238795325112869605, 1.000000000000000000, 0.9238795325112869605, 1.000000000000000000, 0.9238795325112869605, 1.000000000000000000) ) ) 
 REPRESENTATION_ITEM ( '' )  SURFACE ( )  );
#23796=CARTESIAN_POINT ( 'NONE',  ( 119.7402798109119715, -2.529232162391097383, -8.971805383624054997 ) ) ;
#23798=CARTESIAN_POINT ( 'NONE',  ( 122.7993923109119692, -0.4387604401700512802, -15.73000352943951619 ) ) ;
#23826=CARTESIAN_POINT ( 'NONE',  ( 121.4797829359119987, -5.367793381288652910, -18.78638297431638904 ) ) ;
#23829=CARTESIAN_POINT ( 'NONE',  ( 125.2231329858083910, 1.832718407601616750, -10.45069729728725605 ) ) ;
#23872=ORIENTED_EDGE ( 'NONE', *, *, #34917, .F. ) ;
#23885=CARTESIAN_POINT ( 'NONE',  ( 124.6336743332493313, -9.305111785269604141, -15.72189022787271284 ) ) ;
#23889=CARTESIAN_POINT ( 'NONE',  ( 122.7993923109119692, -0.4387604401700486711, -15.73000352943951263 ) ) ;
#23905=CARTESIAN_POINT ( 'NONE',  ( 124.1190016859119680, -0.6942167230862511529, -9.935906262978004833 ) ) ;
#23906=CARTESIAN_POINT ( 'NONE',  ( 119.7434548109119703, -7.554583864224885481, -18.48844787311982785 ) ) ;
#23913=CARTESIAN_POINT ( 'NONE',  ( 120.0907204359119760, -10.25716656981731489, -12.88942061488890545 ) ) ;
#23916=EDGE_CURVE ( 'NONE', #20552, #7363, #43708, .T. ) ;
#23922=DIRECTION ( 'NONE',  ( 1.000000000000000000, 0.000000000000000000, 0.000000000000000000 ) ) ;
#23930=ORIENTED_EDGE ( 'NONE', *, *, #17514, .F. ) ;
#23932=CARTESIAN_POINT ( 'NONE',  ( 120.9241579359119925, -5.444069387712269226, -19.60292469916370450 ) ) ;
#23947=CARTESIAN_POINT ( 'NONE',  ( 123.7022829359119811, -4.283928203966213211, -7.183505701512925334 ) ) ;
#23980=CARTESIAN_POINT ( 'NONE',  ( 121.6881423109119709, -9.959231468620755479, -10.70263013195267199 ) ) ;
#23986=VERTEX_POINT ( 'NONE', #44628 ) ;
#24003=ORIENTED_EDGE ( 'NONE', *, *, #13050, .T. ) ;
#24019=CARTESIAN_POINT ( 'NONE',  ( 123.0077516859119839, -0.6942167230862511529, -9.935906262978006609 ) ) ;
#24032=CARTESIAN_POINT ( 'NONE',  ( 121.2019704359119743, -10.25716656981731489, -12.88942061488890545 ) ) ;
#24037=CARTESIAN_POINT ( 'NONE',  ( 125.4584548109119737, -4.863998795839242995, -13.39321520033831447 ) ) ;
#24043=CARTESIAN_POINT ( 'NONE',  ( 120.2296266859119953, -0.06289925094097943703, -9.412459353600674206 ) ) ;
#24048=ADVANCED_FACE ( 'NONE', ( #6076 ), #16351, .T. ) ;
#24072=CARTESIAN_POINT ( 'NONE',  ( 119.7434548109119703, -2.527210466738042172, -8.967976844669124148 ) ) ;
#24096=VECTOR ( 'NONE', #2166, 1000.000000000000000 ) ;
#24125=CARTESIAN_POINT ( 'NONE',  ( 120.4379860609119675, -6.564341423271550902, -7.887810678476487425 ) ) ;
#24163=CARTESIAN_POINT ( 'NONE',  ( 120.9241579359119925, -5.444069387712269226, -19.60292469916370450 ) ) ;
#24181=CARTESIAN_POINT ( 'NONE',  ( 123.9584548109119737, -4.863998795839242995, -13.39321520033831447 ) ) ;
#24199=CARTESIAN_POINT ( 'NONE',  ( 124.1884548109119777, -7.554583864224885481, -18.48844787311982785 ) ) ;
#24246=EDGE_CURVE ( 'NONE', #7134, #19765, #26199, .T. ) ;
#24251=EDGE_CURVE ( 'NONE', #39662, #17122, #30591, .T. ) ;
#24254=CARTESIAN_POINT ( 'NONE',  ( 121.7575954359119805, 0.5291689781388270175, -13.89700978578772705 ) ) ;
#24262=B_SPLINE_CURVE_WITH_KNOTS ( 'NONE', 3,
 ( #6405, #13911, #24399, #16668, #9831, #34197, #1731, #22711, #38503, #36609 ),
 .UNSPECIFIED., .F., .F.,
 ( 4, 3, 3, 4 ),
 ( 1.226634733346699927E-18, 0.0002476486808869855175, 0.0004952973797228700211, 0.0009368823381787680761 ),
 .UNSPECIFIED. ) ;
#24265=CARTESIAN_POINT ( 'NONE',  ( 123.5633766859119760, -9.033780868592240054, -16.85052413769862056 ) ) ;
#24303=B_SPLINE_CURVE_WITH_KNOTS ( 'NONE', 3,
 ( #16499, #30399, #38499, #7276, #21191, #33564, #26757, #2341 ),
 .UNSPECIFIED., .F., .F.,
 ( 4, 2, 2, 4 ),
 ( 0.000000000000000000, 0.5000000000000193179, 0.7500000000000096589, 1.000000000000000000 ),
 .UNSPECIFIED. ) ;
#24317=CARTESIAN_POINT ( 'NONE',  ( 123.7295344654666991, -4.681376030475591143, -18.56985183333092237 ) ) ;
#24335=VERTEX_POINT ( 'NONE', #34771 ) ;
#24346=CARTESIAN_POINT ( 'NONE',  ( 122.5910329359119970, -4.283928203966213211, -7.183505701512925334 ) ) ;
#24366=CARTESIAN_POINT ( 'NONE',  ( 119.7434548109119703, -7.554583864224885481, -18.48844787311982785 ) ) ;
#24373=CARTESIAN_POINT ( 'NONE',  ( 124.9928017464362426, -6.058968105182603203, -18.37591834006149938 ) ) ;
#24390=CARTESIAN_POINT ( 'NONE',  ( 123.2768159103642063, -8.454079026182057532, -17.47208793939445215 ) ) ;
#24396=DIRECTION ( 'NONE',  ( 0.000000000000000000, -0.4669533266896289669, -0.8842819633428519177 ) ) ;
#24399=CARTESIAN_POINT ( 'NONE',  ( 124.2451922641554489, -8.548534124195539263, -17.65096007659765220 ) ) ;
#24405=DIRECTION ( 'NONE',  ( 0.000000000000000000, 0.4669533266896289669, 0.8842819633428518067 ) ) ;
#24443=ORIENTED_EDGE ( 'NONE', *, *, #22496, .F. ) ;
#24482=CARTESIAN_POINT ( 'NONE',  ( 124.9801526047678664, -2.353188836694182218, -6.221245728286003640 ) ) ;
#24509=AXIS2_PLACEMENT_3D ( 'NONE', #37547, #13173, #20687 ) ;
#24526=( BOUNDED_SURFACE ( )  B_SPLINE_SURFACE ( 1, 2, ( 
 ( #18749, #18968, #32856, #5281, #12136, #19199, #33076, #36730, #2762, #5722, #2305, #30361, #16459, #30809, #37418, #20331, #33764, #5496, #16687, #41091, #13038, #44285, #26495, #33993, #30580, #12364, #2532, #40400, #9163, #23758, #44501, #13264, #16235, #27170, #9849, #26937, #33303, #20107, #34216, #37648, #26717, #40860, #26264, #43825, #40626, #9383, #9613, #23293, #2989, #12591, #16915, #23532, #6422, #37178, #30138, #44052, #40171, #8935, #2079, #5951, #12817, #22837, #19875, #6187, #23067 ),
 ( #36951, #19417, #16003, #29911, #19640, #33526, #31026, #35949, #18419, #11346, #18638, #31246, #41535, #3439, #25483, #42813, #38090, #10078, #11575, #14769, #34434, #14989, #34654, #39387, #25258, #42585, #18184, #39155, #23980, #7920, #17358, #6645, #8153, #4496, #28903, #847, #4265, #13714, #21829, #32311, #44733, #21605, #27621, #10296, #22057, #35723, #1077, #18, #4721, #13492, #28682, #20553, #27397, #41319, #37867, #13931, #35493, #3213, #44957, #27840, #41753, #32079, #10513, #17139, #24199 ) ),
 .UNSPECIFIED., .F., .F., .T. ) 
 B_SPLINE_SURFACE_WITH_KNOTS ( ( 2, 2 ),
 ( 3, 2, 2, 2, 2, 2, 2, 2, 2, 2, 2, 2, 2, 2, 2, 2, 2, 2, 2, 2, 2, 2, 2, 2, 2, 2, 2, 2, 2, 2, 2, 2, 3 ),
 ( 0.000000000000000000, 1.000000000000000000 ),
 ( 0.000000000000000000, 0.03125000000000000000, 0.06250000000000000000, 0.09375000000000000000, 0.1250000000000000000, 0.1562500000000000000, 0.1875000000000000000, 0.2187500000000000000, 0.2500000000000000000, 0.2812500000000000000, 0.3125000000000000000, 0.3437500000000000000, 0.3750000000000000000, 0.4062500000000000000, 0.4375000000000000000, 0.4687500000000000000, 0.5000000000000000000, 0.5312500000000000000, 0.5625000000000000000, 0.5937500000000000000, 0.6250000000000000000, 0.6562500000000000000, 0.6875000000000000000, 0.7187500000000000000, 0.7500000000000000000, 0.7812500000000000000, 0.8125000000000000000, 0.8437500000000000000, 0.8750000000000000000, 0.9062500000000000000, 0.9375000000000000000, 0.9687500000000000000, 1.000000000000000000 ),
 .UNSPECIFIED. ) 
 GEOMETRIC_REPRESENTATION_ITEM ( )  RATIONAL_B_SPLINE_SURFACE ( (
 ( 1.000000000000000000, 0.9238795325112869605, 1.000000000000000000, 0.9238795325112869605, 1.000000000000000000, 0.9238795325112869605, 1.000000000000000000, 0.9238795325112869605, 1.000000000000000000, 0.9238795325112869605, 1.000000000000000000, 0.9238795325112869605, 1.000000000000000000, 0.9238795325112869605, 1.000000000000000000, 0.9238795325112869605, 1.000000000000000000, 0.9238795325112869605, 1.000000000000000000, 0.9238795325112869605, 1.000000000000000000, 0.9238795325112869605, 1.000000000000000000, 0.9238795325112869605, 1.000000000000000000, 0.9238795325112869605, 1.000000000000000000, 0.9238795325112869605, 1.000000000000000000, 0.9238795325112869605, 1.000000000000000000, 0.9238795325112869605, 1.000000000000000000, 0.9238795325112869605, 1.000000000000000000, 0.9238795325112869605, 1.000000000000000000, 0.9238795325112869605, 1.000000000000000000, 0.9238795325112869605, 1.000000000000000000, 0.9238795325112869605, 1.000000000000000000, 0.9238795325112869605, 1.000000000000000000, 0.9238795325112869605, 1.000000000000000000, 0.9238795325112869605, 1.000000000000000000, 0.9238795325112869605, 1.000000000000000000, 0.9238795325112869605, 1.000000000000000000, 0.9238795325112869605, 1.000000000000000000, 0.9238795325112869605, 1.000000000000000000, 0.9238795325112869605, 1.000000000000000000, 0.9238795325112869605, 1.000000000000000000, 0.9238795325112869605, 1.000000000000000000, 0.9238795325112869605, 1.000000000000000000),
 ( 1.000000000000000000, 0.9238795325112869605, 1.000000000000000000, 0.9238795325112869605, 1.000000000000000000, 0.9238795325112869605, 1.000000000000000000, 0.9238795325112869605, 1.000000000000000000, 0.9238795325112869605, 1.000000000000000000, 0.9238795325112869605, 1.000000000000000000, 0.9238795325112869605, 1.000000000000000000, 0.9238795325112869605, 1.000000000000000000, 0.9238795325112869605, 1.000000000000000000, 0.9238795325112869605, 1.000000000000000000, 0.9238795325112869605, 1.000000000000000000, 0.9238795325112869605, 1.000000000000000000, 0.9238795325112869605, 1.000000000000000000, 0.9238795325112869605, 1.000000000000000000, 0.9238795325112869605, 1.000000000000000000, 0.9238795325112869605, 1.000000000000000000, 0.9238795325112869605, 1.000000000000000000, 0.9238795325112869605, 1.000000000000000000, 0.9238795325112869605, 1.000000000000000000, 0.9238795325112869605, 1.000000000000000000, 0.9238795325112869605, 1.000000000000000000, 0.9238795325112869605, 1.000000000000000000, 0.9238795325112869605, 1.000000000000000000, 0.9238795325112869605, 1.000000000000000000, 0.9238795325112869605, 1.000000000000000000, 0.9238795325112869605, 1.000000000000000000, 0.9238795325112869605, 1.000000000000000000, 0.9238795325112869605, 1.000000000000000000, 0.9238795325112869605, 1.000000000000000000, 0.9238795325112869605, 1.000000000000000000, 0.9238795325112869605, 1.000000000000000000, 0.9238795325112869605, 1.000000000000000000) ) ) 
 REPRESENTATION_ITEM ( '' )  SURFACE ( )  );
#24554=EDGE_CURVE ( 'NONE', #30137, #37005, #8772, .T. ) ;
#24565=CARTESIAN_POINT ( 'NONE',  ( 121.5492360609119800, -6.564341423271550902, -7.887810678476487425 ) ) ;
#24572=CARTESIAN_POINT ( 'NONE',  ( 122.4521266859119635, -9.033780868592240054, -16.85052413769862056 ) ) ;
#24602=CARTESIAN_POINT ( 'NONE',  ( 122.3826735609119680, 0.6414057260225851653, -11.69287257290600657 ) ) ;
#24648=CARTESIAN_POINT ( 'NONE',  ( 122.9728284624957553, -6.270977643812233104, -18.77740645536396258 ) ) ;
#24683=ORIENTED_EDGE ( 'NONE', *, *, #22336, .T. ) ;
#24695=CARTESIAN_POINT ( 'NONE',  ( 124.5613353876793639, -9.862207337050596934, -13.58011646024242403 ) ) ;
#24699=CARTESIAN_POINT ( 'NONE',  ( 125.0211000582876721, -2.337644349080307826, -6.269163357979471662 ) ) ;
#24755=CARTESIAN_POINT ( 'NONE',  ( 124.6736757622208671, -8.623525442416562825, -16.74998043996585650 ) ) ;
#24762=CARTESIAN_POINT ( 'NONE',  ( 124.3273610609119828, -6.340755971794960644, -8.611740276972867036 ) ) ;
#24771=EDGE_CURVE ( 'NONE', #42142, #7750, #21151, .T. ) ;
#24781=CARTESIAN_POINT ( 'NONE',  ( 121.2019704359119743, 1.345710702986147034, -13.97328579221134426 ) ) ;
#24783=( BOUNDED_CURVE ( )  B_SPLINE_CURVE ( 2, ( #16816, #9288, #43945, #16127, #23196, #30031, #30480, #12712, #23653, #6770, #3115, #37075, #19770, #2429, #2887, #17040, #20000 ),
 .UNSPECIFIED., .F., .T. ) 
 B_SPLINE_CURVE_WITH_KNOTS ( ( 3, 2, 2, 2, 2, 2, 2, 2, 3 ),
 ( 0.5089135524044680059, 0.5312500000000000000, 0.5625000000000000000, 0.5937500000000000000, 0.6250000000000000000, 0.6562500000000000000, 0.6875000000000000000, 0.7187500000000000000, 0.7410864475955319941 ),
 .UNSPECIFIED. ) 
 CURVE ( )  GEOMETRIC_REPRESENTATION_ITEM ( )  RATIONAL_B_SPLINE_CURVE ( ( 0.9689618144536780164, 0.9455916533437099813, 1.000000000000000000, 0.9238795325112869605, 1.000000000000000000, 0.9238795325112869605, 1.000000000000000000, 0.9238795325112869605, 1.000000000000000000, 0.9238795325112869605, 1.000000000000000000, 0.9238795325112869605, 1.000000000000000000, 0.9238795325112869605, 1.000000000000000000, 0.9455916533437099813, 0.9689618144536780164 ) ) 
 REPRESENTATION_ITEM ( '' )  );
#24805=CARTESIAN_POINT ( 'NONE',  ( 122.9382985609119743, -10.36940331770106916, -15.09355782777062061 ) ) ;
#24807=ORIENTED_EDGE ( 'NONE', *, *, #28670, .T. ) ;
#24818=CARTESIAN_POINT ( 'NONE',  ( 125.1028739313169496, -10.94014759239619039, -9.048497972336113193 ) ) ;
#24821=CARTESIAN_POINT ( 'NONE',  ( 122.2437673109119629, 0.2312338769422704887, -16.08380026872395874 ) ) ;
#24823=CARTESIAN_POINT ( 'NONE',  ( 122.6009548109119720, -11.97804492312076086, -17.05249760251924229 ) ) ;
#24829=CARTESIAN_POINT ( 'NONE',  ( 122.6009548109119720, -11.17722486020181627, -8.479644537342501565 ) ) ;
#24833=ORIENTED_EDGE ( 'NONE', *, *, #44062, .F. ) ;
#24842=VERTEX_POINT ( 'NONE', #6436 ) ;
#24924=CARTESIAN_POINT ( 'NONE',  ( 122.5910329359119970, -4.283928203966213211, -7.183505701512925334 ) ) ;
#24927=CARTESIAN_POINT ( 'NONE',  ( 125.0849378844200714, -0.4913414945001060574, -7.311231363296191610 ) ) ;
#24953=DIRECTION ( 'NONE',  ( 1.000000000000000000, 0.000000000000000000, 0.000000000000000000 ) ) ;
#24994=ORIENTED_EDGE ( 'NONE', *, *, #6377, .F. ) ;
#25007=CARTESIAN_POINT ( 'NONE',  ( 121.5492360609119800, -3.387241619883791355, -18.17469012370385073 ) ) ;
#25031=CARTESIAN_POINT ( 'NONE',  ( 120.0212673109119805, -9.289237151508434209, -11.05642687123711276 ) ) ;
#25046=CARTESIAN_POINT ( 'NONE',  ( 124.4646854081411504, -12.39265241589126987, -10.94766876842672332 ) ) ;
#25068=CARTESIAN_POINT ( 'NONE',  ( 120.3024188928271059, -8.278628333885235335, -17.13983228602121045 ) ) ;
#25084=CARTESIAN_POINT ( 'NONE',  ( 119.7434548109119703, 3.382738713931011443, -10.84621265594315176 ) ) ;
#25089=B_SPLINE_CURVE_WITH_KNOTS ( 'NONE', 3,
 ( #11539, #19278, #29755, #1482, #43667, #12442, #26343, #25446, #39348, #22017 ),
 .UNSPECIFIED., .F., .F.,
 ( 4, 3, 3, 4 ),
 ( 2.168404344971010024E-18, 0.0002476486541971039844, 0.0004952973025691040062, 0.0009610892161188170019 ),
 .UNSPECIFIED. ) ;
#25120=ORIENTED_EDGE ( 'NONE', *, *, #38675, .F. ) ;
#25141=ORIENTED_EDGE ( 'NONE', *, *, #37359, .T. ) ;
#25143=CARTESIAN_POINT ( 'NONE',  ( 124.7440798109119697, -7.200787124940443817, -17.81845355600750835 ) ) ;
#25156=EDGE_CURVE ( 'NONE', #30218, #20552, #12621, .T. ) ;
#25157=CARTESIAN_POINT ( 'NONE',  ( 123.4939235609119663, 0.6414057260225851653, -11.69287257290600657 ) ) ;
#25168=CARTESIAN_POINT ( 'NONE',  ( 119.7434548109119845, -0.5379176930699823833, -10.61813817059959142 ) ) ;
#25213=CARTESIAN_POINT ( 'NONE',  ( 119.7434548109119703, -7.476587315910852460, -21.06050163197695824 ) ) ;
#25238=CARTESIAN_POINT ( 'NONE',  ( 123.6328298109119714, -2.173413727453600508, -8.297982527556802879 ) ) ;
#25258=CARTESIAN_POINT ( 'NONE',  ( 121.4103298109119748, -2.173413727453600508, -8.297982527556802879 ) ) ;
#25262=CARTESIAN_POINT ( 'NONE',  ( 120.4379860609119675, -3.387241619883791355, -18.17469012370385073 ) ) ;
#25270=CARTESIAN_POINT ( 'NONE',  ( 124.5241427111123755, -9.788830010355399125, -12.52847583010056098 ) ) ;
#25272=CARTESIAN_POINT ( 'NONE',  ( 125.4584548109119737, -6.717659058379802595, -19.62329895828877468 ) ) ;
#25274=CARTESIAN_POINT ( 'NONE',  ( 124.0650380271183906, -12.48185142254331836, -10.95032796985108270 ) ) ;
#25294=CARTESIAN_POINT ( 'NONE',  ( 121.6186891859119896, -8.844754642576884152, -8.592115655440050404 ) ) ;
#25312=DIRECTION ( 'NONE',  ( 0.000000000000000000, -0.2950959089608191088, 0.9554676365605421218 ) ) ;
#25324=VERTEX_POINT ( 'NONE', #12094 ) ;
#25351=CARTESIAN_POINT ( 'NONE',  ( 120.0546248871816317, -6.188980713775695364, -18.62212668298318619 ) ) ;
#25367=CARTESIAN_POINT ( 'NONE',  ( 124.1884548109119777, -2.527210466738041728, -8.967976844669124148 ) ) ;
#25371=APPLICATION_CONTEXT ( 'automotive_design' ) ;
#25387=CARTESIAN_POINT ( 'NONE',  ( 119.7434548109119703, -2.590033228374110763, -8.938908788042002840 ) ) ;
#25446=CARTESIAN_POINT ( 'NONE',  ( 122.8568014173871177, -8.493878760966627084, -17.54745775818410536 ) ) ;
#25464=CARTESIAN_POINT ( 'NONE',  ( 122.3132204359119868, -10.25716656981731489, -12.88942061488890545 ) ) ;
#25483=CARTESIAN_POINT ( 'NONE',  ( 120.7157985609119635, -10.36940331770106916, -15.09355782777062061 ) ) ;
#25484=CARTESIAN_POINT ( 'NONE',  ( 123.6776560953690591, -6.001247023715324147, -18.26661038929047010 ) ) ;
#25487=CARTESIAN_POINT ( 'NONE',  ( 123.4244704359119709, 1.345710702986147034, -13.97328579221134426 ) ) ;
#25518=CARTESIAN_POINT ( 'NONE',  ( 119.7434548109119703, -7.554583864224885481, -18.48844787311982785 ) ) ;
#25588=CARTESIAN_POINT ( 'NONE',  ( 120.2296266859119953, -0.06289925094097943703, -9.412459353600674206 ) ) ;
#25589=DIRECTION ( 'NONE',  ( 0.000000000000000000, 0.4669533266896288004, 0.8842819633428518067 ) ) ;
#25602=CARTESIAN_POINT ( 'NONE',  ( 124.5706358376855860, -9.845282878008639216, -13.85115115540643593 ) ) ;
#25621=B_SPLINE_CURVE_WITH_KNOTS ( 'NONE', 3,
 ( #28993, #39700, #7559, #11662, #1386, #21473, #25351, #22146, #35585, #14631 ),
 .UNSPECIFIED., .F., .F.,
 ( 4, 3, 3, 4 ),
 ( 5.421010862427519859E-18, 0.0002476486541971024665, 0.0004952973025691049819, 0.0009610892161188130988 ),
 .UNSPECIFIED. ) ;
#25646=VERTEX_POINT ( 'NONE', #5255 ) ;
#25654=CARTESIAN_POINT ( 'NONE',  ( 124.1685108350155957, -8.515285166876527256, -6.287188262108023729 ) ) ;
#25686=CARTESIAN_POINT ( 'NONE',  ( 120.7852516859119731, -0.6942167230862511529, -9.935906262978006609 ) ) ;
#25700=SHAPE_DEFINITION_REPRESENTATION ( #21216, #38750 ) ;
#25710=CARTESIAN_POINT ( 'NONE',  ( 123.5633766859119760, -0.06289925094097943703, -9.412459353600674206 ) ) ;
#25721=VECTOR ( 'NONE', #44670, 1000.000000000000000 ) ;
#25723=CARTESIAN_POINT ( 'NONE',  ( 125.3574654937850426, -11.58588033818513097, -15.49098285581515455 ) ) ;
#25739=CARTESIAN_POINT ( 'NONE',  ( 120.1601735609119856, 0.6414057260225851653, -11.69287257290600657 ) ) ;
#25744=CARTESIAN_POINT ( 'NONE',  ( 119.8823610609119754, -3.163656168406935087, -18.89861972220014508 ) ) ;
#25745=CARTESIAN_POINT ( 'NONE',  ( 123.5880035264548837, -8.247323210606174015, -17.08054893949881858 ) ) ;
#25771=CARTESIAN_POINT ( 'NONE',  ( 119.7434548109119703, 3.074545301078819737, -12.40350937470759973 ) ) ;
#25775=CARTESIAN_POINT ( 'NONE',  ( 124.5779955726312949, -3.841352728425414753, -21.19493817005371383 ) ) ;
#25788=ORIENTED_EDGE ( 'NONE', *, *, #16802, .T. ) ;
#25807=CARTESIAN_POINT ( 'NONE',  ( 124.5357204359119550, -10.25716656981731489, -12.88942061488890545 ) ) ;
#25820=EDGE_CURVE ( 'NONE', #1411, #36318, #32279, .T. ) ;
#25871=CARTESIAN_POINT ( 'NONE',  ( 124.8633137343399113, -8.262852723283208078, -6.486460572651194134 ) ) ;
#25902=CARTESIAN_POINT ( 'NONE',  ( 123.9584548109119737, 1.449227268523328505, -18.30678586333412738 ) ) ;
#25908=CARTESIAN_POINT ( 'NONE',  ( 123.9106423109119675, -9.959231468620755479, -10.70263013195267199 ) ) ;
#25930=DIRECTION ( 'NONE',  ( 0.000000000000000000, -0.4669533266896290225, -0.8842819633428516957 ) ) ;
#25946=CARTESIAN_POINT ( 'NONE',  ( 124.5035785706779876, -11.90564393026358481, -16.97396928258573112 ) ) ;
#25966=CARTESIAN_POINT ( 'NONE',  ( 122.5910329359119970, -4.283928203966213211, -7.183505701512925334 ) ) ;
#25967=CARTESIAN_POINT ( 'NONE',  ( 120.5768923109119868, -9.959231468620755479, -10.70263013195267199 ) ) ;
#25968=CARTESIAN_POINT ( 'NONE',  ( 123.6361688928271150, -8.278628333885240664, -17.13983228602120690 ) ) ;
#26001=CARTESIAN_POINT ( 'NONE',  ( 125.3135537922313034, -3.242854772516403639, -20.35017254681205046 ) ) ;
#26034=CARTESIAN_POINT ( 'NONE',  ( 124.1190016859119680, -0.6942167230862511529, -9.935906262978006609 ) ) ;
#26043=ORIENTED_EDGE ( 'NONE', *, *, #15813, .F. ) ;
#26094=CARTESIAN_POINT ( 'NONE',  ( 125.2183010572602768, -6.224655641565995268, -6.204738036994054795 ) ) ;
#26097=CARTESIAN_POINT ( 'NONE',  ( 120.4379860609119675, -3.387241619883791355, -18.17469012370385073 ) ) ;
#26124=CARTESIAN_POINT ( 'NONE',  ( 125.3566265649659357, 1.247438245257331157, -16.90339198053782610 ) ) ;
#26138=EDGE_CURVE ( 'NONE', #26479, #2604, #12457, .T. ) ;
#26157=CARTESIAN_POINT ( 'NONE',  ( 124.0650380271158042, 2.250018580934641577, -9.733962076267653529 ) ) ;
#26168=DIRECTION ( 'NONE',  ( 0.000000000000000000, -0.4669533266896290225, -0.8842819633428516957 ) ) ;
#26176=CARTESIAN_POINT ( 'NONE',  ( 119.7434548109119703, 0.04957186715663641774, -7.079989135975798931 ) ) ;
#26184=CARTESIAN_POINT ( 'NONE',  ( 120.8160396737536928, -8.611453504372539314, -17.77011218421760574 ) ) ;
#26188=CARTESIAN_POINT ( 'NONE',  ( 122.5215798109119874, -2.173413727453600508, -8.297982527556802879 ) ) ;
#26189=CARTESIAN_POINT ( 'NONE',  ( 123.0772048109119652, -7.554583864224885481, -18.48844787311982785 ) ) ;
#26199=CIRCLE ( 'NONE', #5094, 1.587500000000001021 ) ;
#26211=ORIENTED_EDGE ( 'NONE', *, *, #27392, .T. ) ;
#26220=CARTESIAN_POINT ( 'NONE',  ( 121.2141330209070276, -6.157706758239399392, -18.56290235964623392 ) ) ;
#26224=CARTESIAN_POINT ( 'NONE',  ( 122.7993923109119692, -0.4387604401700512802, -15.73000352943951619 ) ) ;
#26230=EDGE_LOOP ( 'NONE', ( #37890, #19678, #23498, #41593 ) ) ;
#26257=CARTESIAN_POINT ( 'NONE',  ( 121.6186891859119896, -8.844754642576884152, -8.592115655440050404 ) ) ;
#26264=CARTESIAN_POINT ( 'NONE',  ( 123.2161110609119703, -6.340755971794695078, -8.611740276972781771 ) ) ;
#26324=DIRECTION ( 'NONE',  ( 1.000000000000000000, 0.000000000000000000, 0.000000000000000000 ) ) ;
#26330=CARTESIAN_POINT ( 'NONE',  ( 122.8688454359119646, 0.5291689781388270175, -13.89700978578772705 ) ) ;
#26342=CIRCLE ( 'NONE', #6702, 1.587500000000000355 ) ;
#26343=CARTESIAN_POINT ( 'NONE',  ( 122.7660347346423180, -8.435056900666539903, -17.43606523319152757 ) ) ;
#26381=CARTESIAN_POINT ( 'NONE',  ( 123.0077516859119839, -0.6942167230862511529, -9.935906262978006609 ) ) ;
#26396=CARTESIAN_POINT ( 'NONE',  ( 119.7434548109119703, -6.339884145921025116, -18.90789653539788517 ) ) ;
#26397=VERTEX_POINT ( 'NONE', #28499 ) ;
#26414=CARTESIAN_POINT ( 'NONE',  ( 119.6740016859119748, -0.6942167230862511529, -9.935906262978006609 ) ) ;
#26415=CARTESIAN_POINT ( 'NONE',  ( 121.2019704359119743, 1.345710702986147034, -13.97328579221134426 ) ) ;
#26438=AXIS2_PLACEMENT_3D ( 'NONE', #24181, #13476, #38287 ) ;
#26445=CARTESIAN_POINT ( 'NONE',  ( 119.8791860609119624, -6.339478340643393217, -8.615877017535622073 ) ) ;
#26457=CARTESIAN_POINT ( 'NONE',  ( 121.1325173109119788, -9.289237151508434209, -11.05642687123711276 ) ) ;
#26479=VERTEX_POINT ( 'NONE', #26176 ) ;
#26490=CARTESIAN_POINT ( 'NONE',  ( 122.5910329359119970, -4.283928203966213211, -7.183505701512925334 ) ) ;
#26495=CARTESIAN_POINT ( 'NONE',  ( 121.8270485609119760, -0.08252387247370887580, -11.91645802438286417 ) ) ;
#26499=ORIENTED_EDGE ( 'NONE', *, *, #29512, .T. ) ;
#26517=FACE_OUTER_BOUND ( 'NONE', #768, .T. ) ;
#26547=CARTESIAN_POINT ( 'NONE',  ( 120.3439060953690642, -6.001247023715329476, -18.26661038929047720 ) ) ;
#26578=CARTESIAN_POINT ( 'NONE',  ( 125.2512653913891114, 1.177777608218840255, -17.42223183254473184 ) ) ;
#26607=CARTESIAN_POINT ( 'NONE',  ( 121.7575954359119805, 0.5291689781388270175, -13.89700978578772705 ) ) ;
#26615=B_SPLINE_CURVE_WITH_KNOTS ( 'NONE', 3,
 ( #15367, #38612, #42956, #7617, #21306, #21530, #22203, #4870, #42288, #21757 ),
 .UNSPECIFIED., .F., .F.,
 ( 4, 3, 3, 4 ),
 ( 3.127317220692749988E-18, 0.0002476486808869839996, 0.0004952973797228660095, 0.0009539399846111540045 ),
 .UNSPECIFIED. ) ;
#26619=CARTESIAN_POINT ( 'NONE',  ( 125.2473467947029206, -11.99112074166402842, -14.81453580268809134 ) ) ;
#26641=CARTESIAN_POINT ( 'NONE',  ( 123.9106423109119675, -9.959231468620755479, -10.70263013195267199 ) ) ;
#26642=CARTESIAN_POINT ( 'NONE',  ( 122.7993923109119692, -9.959231468620755479, -10.70263013195267199 ) ) ;
#26644=CARTESIAN_POINT ( 'NONE',  ( 123.9680514173871018, -8.493878760966627084, -17.54745775818410536 ) ) ;
#26674=CARTESIAN_POINT ( 'NONE',  ( 124.1207852356725709, -3.874282071529665750, -21.33170422639506469 ) ) ;
#26678=CARTESIAN_POINT ( 'NONE',  ( 123.0077516859119839, -0.6942167230862511529, -9.935906262978006609 ) ) ;
#26712=EDGE_CURVE ( 'NONE', #21997, #26397, #38572, .T. ) ;
#26713=CARTESIAN_POINT ( 'NONE',  ( 121.4797829359119987, -4.283928203966213211, -7.183505701512925334 ) ) ;
#26717=CARTESIAN_POINT ( 'NONE',  ( 123.0772048109119652, -2.527210466738041728, -8.967976844669124148 ) ) ;
#26730=EDGE_CURVE ( 'NONE', #43772, #23418, #35193, .T. ) ;
#26757=CARTESIAN_POINT ( 'NONE',  ( 125.4584548109120021, -8.650253244288707677, -17.84358828606593050 ) ) ;
#26771=EDGE_CURVE ( 'NONE', #7134, #21997, #42518, .T. ) ;
#26778=CARTESIAN_POINT ( 'NONE',  ( 120.9241579359119925, -4.360204210389833968, -8.000047426360245240 ) ) ;
#26787=CARTESIAN_POINT ( 'NONE',  ( 123.0077516859119839, -0.6942167230862511529, -9.935906262978006609 ) ) ;
#26806=DIRECTION ( 'NONE',  ( -1.000000000000000000, 0.000000000000000000, -0.000000000000000000 ) ) ;
#26812=DIRECTION ( 'NONE',  ( 0.000000000000000000, -0.8842819633428466997, 0.4669533266896385149 ) ) ;
#26835=CARTESIAN_POINT ( 'NONE',  ( 122.5215798109119874, -7.200787124940443817, -17.81845355600750835 ) ) ;
#26845=DIRECTION ( 'NONE',  ( 0.000000000000000000, 0.4669533266896288004, 0.8842819633428518067 ) ) ;
#26848=CARTESIAN_POINT ( 'NONE',  ( 119.7434548109119703, 0.1812605887601431154, -12.07667898593298617 ) ) ;
#26867=CARTESIAN_POINT ( 'NONE',  ( 119.7434548109119703, -2.527210466738041728, -8.967976844669124148 ) ) ;
#26868=CARTESIAN_POINT ( 'NONE',  ( 120.4379860609119675, -3.387241619883791355, -18.17469012370385073 ) ) ;
#26891=DIRECTION ( 'NONE',  ( 0.000000000000000000, -0.8842819633428518067, 0.4669533266896290780 ) ) ;
#26901=CARTESIAN_POINT ( 'NONE',  ( 122.8688454359119646, 0.5291689781388270175, -13.89700978578772705 ) ) ;
#26918=CARTESIAN_POINT ( 'NONE',  ( 124.0980514478796408, -9.877548923986811502, -16.68609415519377137 ) ) ;
#26923=DIRECTION ( 'NONE',  ( -1.000000000000000000, 0.000000000000000000, -0.000000000000000000 ) ) ;
#26937=CARTESIAN_POINT ( 'NONE',  ( 122.7299391859119737, -1.406689858478933353, -17.56299727309130887 ) ) ;
#26958=ORIENTED_EDGE ( 'NONE', *, *, #6666, .T. ) ;
#26975=CARTESIAN_POINT ( 'NONE',  ( 123.4848705389825199, -6.126425863531494542, -18.50366489541501380 ) ) ;
#27005=CARTESIAN_POINT ( 'NONE',  ( 122.1048610609119720, -6.340755971794695078, -8.611740276972781771 ) ) ;
#27019=ORIENTED_EDGE ( 'NONE', *, *, #11844, .T. ) ;
#27076=CARTESIAN_POINT ( 'NONE',  ( 123.9106423109119817, -0.4387604401699203294, -15.73000352943926927 ) ) ;
#27097=CARTESIAN_POINT ( 'NONE',  ( 123.0077516859119839, -0.6942167230862511529, -9.935906262978006609 ) ) ;
#27098=CARTESIAN_POINT ( 'NONE',  ( 119.7434548109119703, -2.527210466738041728, -8.967976844669124148 ) ) ;
#27107=CARTESIAN_POINT ( 'NONE',  ( 120.2526890279447116, -8.246306354371270686, -17.07862329173823568 ) ) ;
#27130=CARTESIAN_POINT ( 'NONE',  ( 121.3408766859119794, -9.033780868592240054, -16.85052413769862056 ) ) ;
#27146=LINE ( 'NONE', #40836, #3411 ) ;
#27149=CARTESIAN_POINT ( 'NONE',  ( 120.8933699480702586, -6.365377317481695663, -18.95617363400926081 ) ) ;
#27165=CARTESIAN_POINT ( 'NONE',  ( 123.8411891859119862, -8.844754642576884152, -8.592115655440050404 ) ) ;
#27170=CARTESIAN_POINT ( 'NONE',  ( 122.5910329359119970, -5.367793381288652910, -18.78638297431638904 ) ) ;
#27223=ORIENTED_EDGE ( 'NONE', *, *, #27392, .F. ) ;
#27237=CARTESIAN_POINT ( 'NONE',  ( 122.2437673109119629, -9.289237151508434209, -11.05642687123711276 ) ) ;
#27248=DIRECTION ( 'NONE',  ( 0.000000000000000000, 0.9554676365605390131, 0.2950959089608289343 ) ) ;
#27263=EDGE_CURVE ( 'NONE', #2604, #8725, #35012, .T. ) ;
#27296=DIRECTION ( 'NONE',  ( -1.000000000000000000, 0.000000000000000000, -0.000000000000000000 ) ) ;
#27303=CARTESIAN_POINT ( 'NONE',  ( 122.7299391859119737, -1.406689858478935573, -17.56299727309130887 ) ) ;
#27305=CARTESIAN_POINT ( 'NONE',  ( 124.1190016859119822, -0.6942167230864397798, -9.935906262977766801 ) ) ;
#27328=CARTESIAN_POINT ( 'NONE',  ( 119.6740016859119748, -0.6942167230862511529, -9.935906262978006609 ) ) ;
#27346=CARTESIAN_POINT ( 'NONE',  ( 121.2714235609119697, 0.6414057260225851653, -11.69287257290600657 ) ) ;
#27352=CARTESIAN_POINT ( 'NONE',  ( 125.4584548109119737, -6.456500312860584678, -19.12873567962219568 ) ) ;
#27360=CARTESIAN_POINT ( 'NONE',  ( 122.6604860609119640, -6.564341423271550902, -7.887810678476487425 ) ) ;
#27392=EDGE_CURVE ( 'NONE', #7972, #31497, #1122, .T. ) ;
#27397=CARTESIAN_POINT ( 'NONE',  ( 123.3550173109119612, 0.2312338769422704887, -16.08380026872395874 ) ) ;
#27402=B_SPLINE_CURVE_WITH_KNOTS ( 'NONE', 3,
 ( #8912, #23507, #19617, #22810, #5473, #15755, #2280, #12338, #19393, #6164 ),
 .UNSPECIFIED., .F., .F.,
 ( 4, 2, 2, 2, 4 ),
 ( 0.000000000000000000, 0.2500000000000000000, 0.5000000000000000000, 0.7500000000000000000, 1.000000000000000000 ),
 .UNSPECIFIED. ) ;
#27435=LINE ( 'NONE', #16726, #31575 ) ;
#27450=CARTESIAN_POINT ( 'NONE',  ( 120.5768923109119868, -0.4387604401700512802, -15.73000352943951619 ) ) ;
#27459=( BOUNDED_SURFACE ( )  B_SPLINE_SURFACE ( 1, 2, ( 
 ( #24366, #14322, #41483, #27570, #34384, #34818, #31413, #44680, #7034, #10465, #27787, #23705, #3601, #16865, #10241, #38252, #30756, #23932, #17515, #20505, #13441, #180, #27346, #41266, #3166, #17088, #28014, #20724, #14543, #22285, #38924, #21610, #1080, #8156, #7694, #7923, #11578, #32315, #21833, #39617, #42368, #1523, #29123, #22061, #29350, #42589, #24805, #38697, #28460, #7464, #4269, #21382, #8378, #25487, #630, #25710, #852, #36178, #35953, #18188, #4944, #4500, #35265, #18641, #14771 ),
 ( #42816, #14993, #4042, #10905, #18858, #32750, #28686, #15444, #11129, #17964, #35726, #31863, #25031, #35497, #4724, #39390, #32083, #11351, #25262, #39158, #18423, #28907, #32533, #1304, #15216, #11802, #43034, #5168, #29574, #43942, #12938, #15900, #1975, #8823, #9284, #5844, #19085, #26607, #16122, #2196, #16581, #23191, #44175, #5399, #33880, #33199, #32971, #37071, #26835, #29800, #19766, #16349, #43264, #19540, #30250, #26381, #6073, #12707, #33647, #43712, #2424, #40748, #9505, #2649, #19995 ) ),
 .UNSPECIFIED., .F., .F., .F. ) 
 B_SPLINE_SURFACE_WITH_KNOTS ( ( 2, 2 ),
 ( 3, 2, 2, 2, 2, 2, 2, 2, 2, 2, 2, 2, 2, 2, 2, 2, 2, 2, 2, 2, 2, 2, 2, 2, 2, 2, 2, 2, 2, 2, 2, 2, 3 ),
 ( 0.000000000000000000, 1.000000000000000000 ),
 ( 0.000000000000000000, 0.03125000000000000000, 0.06250000000000000000, 0.09375000000000000000, 0.1250000000000000000, 0.1562500000000000000, 0.1875000000000000000, 0.2187500000000000000, 0.2500000000000000000, 0.2812500000000000000, 0.3125000000000000000, 0.3437500000000000000, 0.3750000000000000000, 0.4062500000000000000, 0.4375000000000000000, 0.4687500000000000000, 0.5000000000000000000, 0.5312500000000000000, 0.5625000000000000000, 0.5937500000000000000, 0.6250000000000000000, 0.6562500000000000000, 0.6875000000000000000, 0.7187500000000000000, 0.7500000000000000000, 0.7812500000000000000, 0.8125000000000000000, 0.8437500000000000000, 0.8750000000000000000, 0.9062500000000000000, 0.9375000000000000000, 0.9687500000000000000, 1.000000000000000000 ),
 .UNSPECIFIED. ) 
 GEOMETRIC_REPRESENTATION_ITEM ( )  RATIONAL_B_SPLINE_SURFACE ( (
 ( 1.000000000000000000, 0.9238795325112869605, 1.000000000000000000, 0.9238795325112869605, 1.000000000000000000, 0.9238795325112869605, 1.000000000000000000, 0.9238795325112869605, 1.000000000000000000, 0.9238795325112869605, 1.000000000000000000, 0.9238795325112869605, 1.000000000000000000, 0.9238795325112869605, 1.000000000000000000, 0.9238795325112869605, 1.000000000000000000, 0.9238795325112869605, 1.000000000000000000, 0.9238795325112869605, 1.000000000000000000, 0.9238795325112869605, 1.000000000000000000, 0.9238795325112869605, 1.000000000000000000, 0.9238795325112869605, 1.000000000000000000, 0.9238795325112869605, 1.000000000000000000, 0.9238795325112869605, 1.000000000000000000, 0.9238795325112869605, 1.000000000000000000, 0.9238795325112869605, 1.000000000000000000, 0.9238795325112869605, 1.000000000000000000, 0.9238795325112869605, 1.000000000000000000, 0.9238795325112869605, 1.000000000000000000, 0.9238795325112869605, 1.000000000000000000, 0.9238795325112869605, 1.000000000000000000, 0.9238795325112869605, 1.000000000000000000, 0.9238795325112869605, 1.000000000000000000, 0.9238795325112869605, 1.000000000000000000, 0.9238795325112869605, 1.000000000000000000, 0.9238795325112869605, 1.000000000000000000, 0.9238795325112869605, 1.000000000000000000, 0.9238795325112869605, 1.000000000000000000, 0.9238795325112869605, 1.000000000000000000, 0.9238795325112869605, 1.000000000000000000, 0.9238795325112869605, 1.000000000000000000),
 ( 1.000000000000000000, 0.9238795325112869605, 1.000000000000000000, 0.9238795325112869605, 1.000000000000000000, 0.9238795325112869605, 1.000000000000000000, 0.9238795325112869605, 1.000000000000000000, 0.9238795325112869605, 1.000000000000000000, 0.9238795325112869605, 1.000000000000000000, 0.9238795325112869605, 1.000000000000000000, 0.9238795325112869605, 1.000000000000000000, 0.9238795325112869605, 1.000000000000000000, 0.9238795325112869605, 1.000000000000000000, 0.9238795325112869605, 1.000000000000000000, 0.9238795325112869605, 1.000000000000000000, 0.9238795325112869605, 1.000000000000000000, 0.9238795325112869605, 1.000000000000000000, 0.9238795325112869605, 1.000000000000000000, 0.9238795325112869605, 1.000000000000000000, 0.9238795325112869605, 1.000000000000000000, 0.9238795325112869605, 1.000000000000000000, 0.9238795325112869605, 1.000000000000000000, 0.9238795325112869605, 1.000000000000000000, 0.9238795325112869605, 1.000000000000000000, 0.9238795325112869605, 1.000000000000000000, 0.9238795325112869605, 1.000000000000000000, 0.9238795325112869605, 1.000000000000000000, 0.9238795325112869605, 1.000000000000000000, 0.9238795325112869605, 1.000000000000000000, 0.9238795325112869605, 1.000000000000000000, 0.9238795325112869605, 1.000000000000000000, 0.9238795325112869605, 1.000000000000000000, 0.9238795325112869605, 1.000000000000000000, 0.9238795325112869605, 1.000000000000000000, 0.9238795325112869605, 1.000000000000000000) ) ) 
 REPRESENTATION_ITEM ( '' )  SURFACE ( )  );
#27462=CARTESIAN_POINT ( 'NONE',  ( 123.9106423109119675, -0.4387604401700512802, -15.73000352943951619 ) ) ;
#27465=CARTESIAN_POINT ( 'NONE',  ( 124.9774582099998383, 2.655747558278632070, -12.25998410011163031 ) ) ;
#27517=ADVANCED_FACE ( 'NONE', ( #9339 ), #30309, .F. ) ;
#27546=CARTESIAN_POINT ( 'NONE',  ( 121.2714235609119697, 0.6414057260225851653, -11.69287257290600657 ) ) ;
#27551=CARTESIAN_POINT ( 'NONE',  ( 122.1743141859119817, -8.321307733199551748, -9.223433127585318303 ) ) ;
#27552=CARTESIAN_POINT ( 'NONE',  ( 120.7157985609119635, -0.08252387247370887580, -11.91645802438286417 ) ) ;
#27559=CARTESIAN_POINT ( 'NONE',  ( 120.2510376736034345, -8.245233026025740486, -17.07659070123625611 ) ) ;
#27570=CARTESIAN_POINT ( 'NONE',  ( 119.9518141859119851, -0.8832429491016019485, -18.19431474523657855 ) ) ;
#27590=EDGE_CURVE ( 'NONE', #15883, #2745, #14221, .T. ) ;
#27602=CARTESIAN_POINT ( 'NONE',  ( 123.7022829359119811, -4.283928203966204329, -7.183505701512929775 ) ) ;
#27614=B_SPLINE_CURVE_WITH_KNOTS ( 'NONE', 3,
 ( #19234, #32451, #29045, #12631, #36986, #33336, #43859, #39753, #43626, #9199 ),
 .UNSPECIFIED., .F., .F.,
 ( 4, 3, 3, 4 ),
 ( 3.127317220692749988E-18, 0.0002476486808869849754, 0.0004952973797228679611, 0.0009539399846111509687 ),
 .UNSPECIFIED. ) ;
#27621=CARTESIAN_POINT ( 'NONE',  ( 122.6604860609119640, -6.564341423271550902, -7.887810678476487425 ) ) ;
#27632=LINE ( 'NONE', #13502, #15659 ) ;
#27644=VERTEX_POINT ( 'NONE', #34610 ) ;
#27674=CARTESIAN_POINT ( 'NONE',  ( 120.5074391859119913, -1.406689858478933353, -17.56299727309130887 ) ) ;
#27679=ORIENTED_EDGE ( 'NONE', *, *, #14610, .T. ) ;
#27686=CARTESIAN_POINT ( 'NONE',  ( 123.2855641859119942, -8.321307733199551748, -9.223433127585318303 ) ) ;
#27689=CARTESIAN_POINT ( 'NONE',  ( 125.1375072647509228, 2.456438219714048188, -12.13603346852097786 ) ) ;
#27712=DIRECTION ( 'NONE',  ( -1.000000000000000000, 0.000000000000000000, -0.000000000000000000 ) ) ;
#27729=EDGE_CURVE ( 'NONE', #2582, #23986, #12044, .T. ) ;
#27732=ORIENTED_EDGE ( 'NONE', *, *, #43865, .T. ) ;
#27736=CARTESIAN_POINT ( 'NONE',  ( 123.6808719482204992, -5.999156839134923480, -18.26265215102791117 ) ) ;
#27742=CARTESIAN_POINT ( 'NONE',  ( 123.9584548109119737, -4.863998795839242995, -13.39321520033831447 ) ) ;
#27753=DIRECTION ( 'NONE',  ( 0.000000000000000000, -0.4669533266896290225, -0.8842819633428516957 ) ) ;
#27772=CARTESIAN_POINT ( 'NONE',  ( 122.1048610609119720, -6.340755971794695078, -8.611740276972781771 ) ) ;
#27787=CARTESIAN_POINT ( 'NONE',  ( 120.4379860609119675, -6.564341423271550902, -7.887810678476487425 ) ) ;
#27794=CARTESIAN_POINT ( 'NONE',  ( 125.4348241020431800, -6.339323288574539639, -18.90683442488884936 ) ) ;
#27795=DIRECTION ( 'NONE',  ( -1.000000000000000000, 0.000000000000000000, -0.000000000000000000 ) ) ;
#27801=CARTESIAN_POINT ( 'NONE',  ( 123.3550173109119612, 0.2312338769422704887, -16.08380026872395874 ) ) ;
#27811=CARTESIAN_POINT ( 'NONE',  ( 123.4124213555256517, -8.364211927971188842, -17.30190421972978143 ) ) ;
#27838=ORIENTED_EDGE ( 'NONE', *, *, #1500, .T. ) ;
#27839=ADVANCED_FACE ( 'NONE', ( #19797 ), #33682, .F. ) ;
#27840=CARTESIAN_POINT ( 'NONE',  ( 123.8411891859119862, -8.844754642576884152, -8.592115655440050404 ) ) ;
#27900=DIRECTION ( 'NONE',  ( -1.000000000000000000, 0.000000000000000000, -0.000000000000000000 ) ) ;
#27909=CARTESIAN_POINT ( 'NONE',  ( 124.6051735609119646, -9.645473719204776586, -14.86997237629376656 ) ) ;
#27911=VECTOR ( 'NONE', #23922, 1000.000000000000000 ) ;
#27913=CARTESIAN_POINT ( 'NONE',  ( 125.3566265649618288, -1.353822015633321829, -7.281778159245134496 ) ) ;
#27923=CARTESIAN_POINT ( 'NONE',  ( 119.7434548109119703, -2.254126046650808401, -18.26827295101220017 ) ) ;
#27970=CARTESIAN_POINT ( 'NONE',  ( 123.9584548109119737, -12.48189245497263755, -10.95032834292243074 ) ) ;
#28012=ORIENTED_EDGE ( 'NONE', *, *, #19756, .F. ) ;
#28014=CARTESIAN_POINT ( 'NONE',  ( 121.5492360609119800, -6.564341423271550902, -7.887810678476487425 ) ) ;
#28020=CARTESIAN_POINT ( 'NONE',  ( 124.6340697093320387, -5.999156839134622388, -18.26265215102739248 ) ) ;
#28025=AXIS2_PLACEMENT_3D ( 'NONE', #10644, #42104, #34565 ) ;
#28028=CARTESIAN_POINT ( 'NONE',  ( 122.5910329359119970, -4.283928203966213211, -7.183505701512925334 ) ) ;
#28063=ORIENTED_EDGE ( 'NONE', *, *, #39109, .F. ) ;
#28103=CARTESIAN_POINT ( 'NONE',  ( 119.8823610609119754, -6.340755971794695078, -8.611740276972781771 ) ) ;
#28118=CARTESIAN_POINT ( 'NONE',  ( 120.9936110609119737, -6.340755971794695078, -8.611740276972781771 ) ) ;
#28129=CARTESIAN_POINT ( 'NONE',  ( 124.5966688623432219, -9.713577380183913590, -14.62808432448665563 ) ) ;
#28130=AXIS2_PLACEMENT_3D ( 'NONE', #32651, #43602, #5063 ) ;
#28131=CARTESIAN_POINT ( 'NONE',  ( 123.3550173109119612, 0.2312338769422704887, -16.08380026872395874 ) ) ;
#28134=CARTESIAN_POINT ( 'NONE',  ( 124.7442371152527016, -2.402718219011967360, -6.010812890236988615 ) ) ;
#28177=ORIENTED_EDGE ( 'NONE', *, *, #24554, .F. ) ;
#28190=CARTESIAN_POINT ( 'NONE',  ( 124.6894688159050872, -8.253847584685239269, -17.09290432062678278 ) ) ;
#28196=LINE ( 'NONE', #42102, #28231 ) ;
#28204=CARTESIAN_POINT ( 'NONE',  ( 122.0226922641554523, -8.548534124195553474, -17.65096007659764510 ) ) ;
#28231=VECTOR ( 'NONE', #31372, 1000.000000000000000 ) ;
#28270=ORIENTED_EDGE ( 'NONE', *, *, #44062, .T. ) ;
#28347=CARTESIAN_POINT ( 'NONE',  ( 122.5215798109119874, -2.173413727453600508, -8.297982527556802879 ) ) ;
#28350=CARTESIAN_POINT ( 'NONE',  ( 119.7434548109119703, -2.530624428477246113, -8.966368849971939170 ) ) ;
#28365=VECTOR ( 'NONE', #33734, 1000.000000000000000 ) ;
#28406=AXIS2_PLACEMENT_3D ( 'NONE', #22147, #28771, #15302 ) ;
#28416=CARTESIAN_POINT ( 'NONE',  ( 124.7440798109119697, -7.200787124940195127, -17.81845355600763625 ) ) ;
#28421=ORIENTED_EDGE ( 'NONE', *, *, #24251, .T. ) ;
#28434=CARTESIAN_POINT ( 'NONE',  ( 121.8270485609119760, -10.36940331770106916, -15.09355782777062061 ) ) ;
#28448=FILL_AREA_STYLE ('',( #38244 ) ) ;
#28460=CARTESIAN_POINT ( 'NONE',  ( 123.0772048109119652, -7.554583864224885481, -18.48844787311982785 ) ) ;
#28474=CARTESIAN_POINT ( 'NONE',  ( 125.1375072647520881, -10.92929117853784682, -9.105846273144043934 ) ) ;
#28492=CARTESIAN_POINT ( 'NONE',  ( 120.7157985609119635, -10.36940331770106916, -15.09355782777062061 ) ) ;
#28494=CARTESIAN_POINT ( 'NONE',  ( 120.5435347346423072, -8.435056900666539903, -17.43606523319152757 ) ) ;
#28499=CARTESIAN_POINT ( 'NONE',  ( 123.9584548109119737, -2.421111938423274879, -5.775321541204940345 ) ) ;
#28542=ADVANCED_FACE ( 'NONE', ( #44602 ), #30904, .T. ) ;
#28564=CARTESIAN_POINT ( 'NONE',  ( 122.0354079359119908, -4.360204210389833968, -8.000047426360245240 ) ) ;
#28578=CARTESIAN_POINT ( 'NONE',  ( 124.5847809835702691, -9.789958397730165629, -14.26986282893143532 ) ) ;
#28579=CARTESIAN_POINT ( 'NONE',  ( 122.3826735609119680, 0.6414057260225851653, -11.69287257290600657 ) ) ;
#28582=CARTESIAN_POINT ( 'NONE',  ( 125.2183010572584010, -0.7431075297091613852, -7.348064569251269162 ) ) ;
#28617=VERTEX_POINT ( 'NONE', #23625 ) ;
#28641=EDGE_CURVE ( 'NONE', #24842, #38956, #22606, .T. ) ;
#28647=ORIENTED_EDGE ( 'NONE', *, *, #20953, .F. ) ;
#28661=CARTESIAN_POINT ( 'NONE',  ( 119.9518141859119851, -8.321307733199551748, -9.223433127585318303 ) ) ;
#28670=EDGE_CURVE ( 'NONE', #26479, #31784, #16068, .T. ) ;
#28682=CARTESIAN_POINT ( 'NONE',  ( 123.2161110609119561, -3.163656168406935087, -18.89861972220014508 ) ) ;
#28686=CARTESIAN_POINT ( 'NONE',  ( 119.6045485609119794, -0.08252387247370887580, -11.91645802438286417 ) ) ;
#28689=CARTESIAN_POINT ( 'NONE',  ( 122.5182407289968154, -6.032552146994431652, -18.32589373581284775 ) ) ;
#28694=CARTESIAN_POINT ( 'NONE',  ( 124.5074358514838906, -9.686381406722462728, -12.07228238157437694 ) ) ;
#28754=CARTESIAN_POINT ( 'NONE',  ( 120.7157985609119635, -0.08252387247370887580, -11.91645802438286417 ) ) ;
#28771=DIRECTION ( 'NONE',  ( -1.000000000000000000, 0.000000000000000000, -0.000000000000000000 ) ) ;
#28789=CARTESIAN_POINT ( 'NONE',  ( 124.3968141859119783, -8.321307733199551748, -9.223433127585318303 ) ) ;
#28801=CARTESIAN_POINT ( 'NONE',  ( 124.5644539102826513, -9.858463830682730134, -13.67056496101630181 ) ) ;
#28805=CARTESIAN_POINT ( 'NONE',  ( 124.9009360172553897, -2.375710885519020099, -6.139922134414775634 ) ) ;
#28815=CARTESIAN_POINT ( 'NONE',  ( 119.7434548109119703, -2.527210466738042172, -8.967976844669124148 ) ) ;
#28833=DIRECTION ( 'NONE',  ( -1.000000000000000000, 0.000000000000000000, -0.000000000000000000 ) ) ;
#28864=AXIS2_PLACEMENT_3D ( 'NONE', #30716, #16359, #26845 ) ;
#28883=CARTESIAN_POINT ( 'NONE',  ( 120.0907204359119760, -10.25716656981731489, -12.88942061488890545 ) ) ;
#28903=CARTESIAN_POINT ( 'NONE',  ( 122.1048610609119720, -3.163656168406935087, -18.89861972220014508 ) ) ;
#28907=CARTESIAN_POINT ( 'NONE',  ( 120.6463454359119822, 0.5291689781388270175, -13.89700978578772705 ) ) ;
#28921=CARTESIAN_POINT ( 'NONE',  ( 125.0302870206147787, -11.97677892521326903, -10.86299592855657359 ) ) ;
#28941=CARTESIAN_POINT ( 'NONE',  ( 120.8160396737536928, -8.611453504372539314, -17.77011218421760574 ) ) ;
#28993=CARTESIAN_POINT ( 'NONE',  ( 120.3439060953690642, -6.001247023715329476, -18.26661038929047720 ) ) ;
#29008=CARTESIAN_POINT ( 'NONE',  ( 121.1325173109119788, 0.2312338769422704887, -16.08380026872395874 ) ) ;
#29021=CARTESIAN_POINT ( 'NONE',  ( 124.5685810787103662, -9.850217616288844624, -13.79100485233420770 ) ) ;
#29022=CARTESIAN_POINT ( 'NONE',  ( 122.0354079359119908, -5.444069387712269226, -19.60292469916370450 ) ) ;
#29045=CARTESIAN_POINT ( 'NONE',  ( 120.7979673576684831, -6.302457937304708935, -18.83702152638930372 ) ) ;
#29066=CARTESIAN_POINT ( 'NONE',  ( 125.3296504289713766, -7.415504751769019798, -6.746157367331738541 ) ) ;
#29080=DIRECTION ( 'NONE',  ( -1.000000000000000000, 0.000000000000000000, -0.000000000000000000 ) ) ;
#29099=CARTESIAN_POINT ( 'NONE',  ( 124.0495485609119584, -10.36940331770106916, -15.09355782777062061 ) ) ;
#29123=CARTESIAN_POINT ( 'NONE',  ( 122.6604860609119640, -6.564341423271550902, -7.887810678476487425 ) ) ;
#29136=CARTESIAN_POINT ( 'NONE',  ( 125.0526156892421454, -11.67076936788440022, -16.62222883760368930 ) ) ;
#29155=CARTESIAN_POINT ( 'NONE',  ( 120.8547048109119686, -7.554583864224885481, -18.48844787311982785 ) ) ;
#29158=VERTEX_POINT ( 'NONE', #37515 ) ;
#29180=AXIS2_PLACEMENT_3D ( 'NONE', #30454, #30683, #34313 ) ;
#29189=CARTESIAN_POINT ( 'NONE',  ( 125.3275354501026158, -3.173127855840466971, -20.30256202504349261 ) ) ;
#29192=CARTESIAN_POINT ( 'NONE',  ( 120.5074391859119913, -1.406689858478933353, -17.56299727309130887 ) ) ;
#29228=ADVANCED_FACE ( 'NONE', ( #118 ), #38857, .F. ) ;
#29230=CARTESIAN_POINT ( 'NONE',  ( 122.7299391859119737, -1.406689858478933353, -17.56299727309130887 ) ) ;
#29238=ORIENTED_EDGE ( 'NONE', *, *, #27263, .F. ) ;
#29291=CARTESIAN_POINT ( 'NONE',  ( 125.3566265649632072, -6.703367565947885964, -6.589706821340800325 ) ) ;
#29326=CARTESIAN_POINT ( 'NONE',  ( 120.9936110609119737, -6.340755971794695078, -8.611740276972781771 ) ) ;
#29338=AXIS2_PLACEMENT_3D ( 'NONE', #23619, #27712, #19963 ) ;
#29344=( GEOMETRIC_REPRESENTATION_CONTEXT ( 3 ) GLOBAL_UNCERTAINTY_ASSIGNED_CONTEXT ( ( #6911 ) ) GLOBAL_UNIT_ASSIGNED_CONTEXT ( ( #38688, #45107, #35024 ) ) REPRESENTATION_CONTEXT ( 'NONE', 'WORKASPACE' ) );
#29350=CARTESIAN_POINT ( 'NONE',  ( 122.7993923109119692, -9.959231468620755479, -10.70263013195267199 ) ) ;
#29357=CARTESIAN_POINT ( 'NONE',  ( 124.5338130785779072, -9.828743235481264051, -12.79707124658312090 ) ) ;
#29360=CARTESIAN_POINT ( 'NONE',  ( 121.0630641859119976, -0.8832429491016020595, -18.19431474523658565 ) ) ;
#29378=CARTESIAN_POINT ( 'NONE',  ( 122.1048610609119720, -6.340755971794695078, -8.611740276972781771 ) ) ;
#29382=CARTESIAN_POINT ( 'NONE',  ( 121.7575954359119805, -11.07370829466463569, -12.81314460846529002 ) ) ;
#29383=CARTESIAN_POINT ( 'NONE',  ( 122.5215798109119874, -2.173413727453600508, -8.297982527556802879 ) ) ;
#29408=CARTESIAN_POINT ( 'NONE',  ( 125.4584548109119737, -4.863998795839242995, -13.39321520033831447 ) ) ;
#29409=CARTESIAN_POINT ( 'NONE',  ( 125.4584548109119737, -2.316996251443989241, -21.63995271010855248 ) ) ;
#29411=DIRECTION ( 'NONE',  ( 0.000000000000000000, 0.4669533266896288004, 0.8842819633428518067 ) ) ;
#29429=ORIENTED_EDGE ( 'NONE', *, *, #10799, .T. ) ;
#29448=CARTESIAN_POINT ( 'NONE',  ( 123.1466579359119891, -4.360204210389833968, -8.000047426360245240 ) ) ;
#29512=EDGE_CURVE ( 'NONE', #15883, #1412, #43413, .T. ) ;
#29515=CARTESIAN_POINT ( 'NONE',  ( 124.1726284085847709, -5.853720688424037810, -5.454752289499457341 ) ) ;
#29545=CARTESIAN_POINT ( 'NONE',  ( 125.0048763211397471, 2.279351556901532128, -15.91318496429555296 ) ) ;
#29574=CARTESIAN_POINT ( 'NONE',  ( 121.1325173109119788, -9.289237151508434209, -11.05642687123711276 ) ) ;
#29586=CARTESIAN_POINT ( 'NONE',  ( 125.2559326335950232, -11.97226500772692681, -14.83370496690971940 ) ) ;
#29606=CARTESIAN_POINT ( 'NONE',  ( 120.0907204359119760, -10.25716656981731489, -12.88942061488890545 ) ) ;
#29607=CARTESIAN_POINT ( 'NONE',  ( 122.8688454359119646, -11.07370829466463569, -12.81314460846529002 ) ) ;
#29608=CARTESIAN_POINT ( 'NONE',  ( 123.6843602343419377, -8.309924745830986836, -17.19909913565936321 ) ) ;
#29624=( BOUNDED_CURVE ( )  B_SPLINE_CURVE ( 2, ( #12945, #6082, #22965, #29360, #16357, #15681, #5177, #29809, #44184, #12269, #39850, #33656, #33425, #2432, #5626, #22734, #36409 ),
 .UNSPECIFIED., .F., .F. ) 
 B_SPLINE_CURVE_WITH_KNOTS ( ( 3, 2, 2, 2, 2, 2, 2, 2, 3 ),
 ( 0.2589135524044680059, 0.2812500000000000000, 0.3125000000000000000, 0.3437500000000000000, 0.3750000000000000000, 0.4062500000000000000, 0.4375000000000000000, 0.4687500000000000000, 0.4910864475955319941 ),
 .UNSPECIFIED. ) 
 CURVE ( )  GEOMETRIC_REPRESENTATION_ITEM ( )  RATIONAL_B_SPLINE_CURVE ( ( 0.9689618144536780164, 0.9455916533437099813, 1.000000000000000000, 0.9238795325112869605, 1.000000000000000000, 0.9238795325112869605, 1.000000000000000000, 0.9238795325112869605, 1.000000000000000000, 0.9238795325112869605, 1.000000000000000000, 0.9238795325112869605, 1.000000000000000000, 0.9238795325112869605, 1.000000000000000000, 0.9455916533437099813, 0.9689618144536780164 ) ) 
 REPRESENTATION_ITEM ( '' )  );
#29633=DIRECTION ( 'NONE',  ( 0.000000000000000000, 0.4669533266896288004, 0.8842819633428518067 ) ) ;
#29639=CARTESIAN_POINT ( 'NONE',  ( 121.3105849628857129, -6.095137211460710525, -18.44441274085890115 ) ) ;
#29642=CARTESIAN_POINT ( 'NONE',  ( 120.4379860609119675, -6.564341423271550902, -7.887810678476487425 ) ) ;
#29657=CARTESIAN_POINT ( 'NONE',  ( 124.0495485609119584, -0.08252387247370973622, -11.91645802438287483 ) ) ;
#29675=CARTESIAN_POINT ( 'NONE',  ( 122.8688454359119646, -11.07370829466463569, -12.81314460846529002 ) ) ;
#29742=CARTESIAN_POINT ( 'NONE',  ( 123.3550173109119612, -9.289237151508434209, -11.05642687123711276 ) ) ;
#29747=B_SPLINE_CURVE_WITH_KNOTS ( 'NONE', 3,
 ( #42042, #28350, #38371, #39056, #31761, #10582, #7827, #25387, #18312, #17419 ),
 .UNSPECIFIED., .F., .F.,
 ( 4, 3, 3, 4 ),
 ( 6.115116239063360172E-19, 1.132108808049913944E-05, 5.660634449920369976E-05, 9.445515394676020900E-05 ),
 .UNSPECIFIED. ) ;
#29755=CARTESIAN_POINT ( 'NONE',  ( 122.5731102343419536, -8.309924745830986836, -17.19909913565936321 ) ) ;
#29767=CARTESIAN_POINT ( 'NONE',  ( 124.1726284085855951, 1.449181222348162157, -18.30671709505454103 ) ) ;
#29800=CARTESIAN_POINT ( 'NONE',  ( 122.5910329359119970, -5.367793381288652910, -18.78638297431638904 ) ) ;
#29809=CARTESIAN_POINT ( 'NONE',  ( 121.3408766859119794, -0.06289925094098414160, -9.412459353600681311 ) ) ;
#29811=CARTESIAN_POINT ( 'NONE',  ( 125.3519896833715848, -11.65604236765752688, -15.30335118913170156 ) ) ;
#29832=CARTESIAN_POINT ( 'NONE',  ( 120.0212673109119805, -9.289237151508434209, -11.05642687123711276 ) ) ;
#29833=CARTESIAN_POINT ( 'NONE',  ( 120.2296266859119953, -0.06289925094097943703, -9.412459353600674206 ) ) ;
#29857=EDGE_LOOP ( 'NONE', ( #31303, #45116, #30849, #39876 ) ) ;
#29860=FACE_OUTER_BOUND ( 'NONE', #36863, .T. ) ;
#29866=CARTESIAN_POINT ( 'NONE',  ( 125.2638605181402056, -3.430414653771011846, -20.49516738280293637 ) ) ;
#29870=CARTESIAN_POINT ( 'NONE',  ( 124.4662673109119737, -9.289237151508434209, -11.05642687123711276 ) ) ;
#29884=CARTESIAN_POINT ( 'NONE',  ( 124.4662673109119737, -9.289237151508427104, -11.05642687123710033 ) ) ;
#29891=CARTESIAN_POINT ( 'NONE',  ( 122.5664060953690466, -6.001247023715324147, -18.26661038929047010 ) ) ;
#29904=CARTESIAN_POINT ( 'NONE',  ( 121.7575954359119805, -11.07370829466463569, -12.81314460846529002 ) ) ;
#29906=ADVANCED_FACE ( 'NONE', ( #31016 ), #33574, .T. ) ;
#29911=CARTESIAN_POINT ( 'NONE',  ( 119.9518141859119851, -0.8832429491016019485, -18.19431474523657855 ) ) ;
#29932=CARTESIAN_POINT ( 'NONE',  ( 125.4584548109119737, -4.863998795839242995, -13.39321520033831447 ) ) ;
#29965=CARTESIAN_POINT ( 'NONE',  ( 120.7852516859119731, -0.6942167230862464899, -9.935906262978006609 ) ) ;
#29968=CARTESIAN_POINT ( 'NONE',  ( 124.3692356341924636, -8.482484215924628757, -6.318052624112218574 ) ) ;
#29994=CARTESIAN_POINT ( 'NONE',  ( 124.6574308310796937, 1.356445862163998095, -18.15072565491285417 ) ) ;
#29996=VECTOR ( 'NONE', #38715, 1000.000000000000000 ) ;
#30008=ORIENTED_EDGE ( 'NONE', *, *, #13912, .T. ) ;
#30031=CARTESIAN_POINT ( 'NONE',  ( 122.3132204359119868, 1.345710702986147034, -13.97328579221134603 ) ) ;
#30035=LINE ( 'NONE', #36636, #41330 ) ;
#30036=CARTESIAN_POINT ( 'NONE',  ( 125.3358932077582892, -11.73929824459550986, -15.14057442325835012 ) ) ;
#30039=CARTESIAN_POINT ( 'NONE',  ( 119.7434548109119561, -0.3205909622538446468, -16.32243156402693174 ) ) ;
#30059=ORIENTED_EDGE ( 'NONE', *, *, #37359, .F. ) ;
#30062=CARTESIAN_POINT ( 'NONE',  ( 120.7157985609119635, -0.08252387247370887580, -11.91645802438286417 ) ) ;
#30063=CARTESIAN_POINT ( 'NONE',  ( 121.6881423109119709, -9.959231468620755479, -10.70263013195267199 ) ) ;
#30091=CARTESIAN_POINT ( 'NONE',  ( 123.9584548109119737, -1.204716393658298523, -20.50726132761981901 ) ) ;
#30095=CARTESIAN_POINT ( 'NONE',  ( 121.4551560953690483, -6.001247023715324147, -18.26661038929047010 ) ) ;
#30098=CARTESIAN_POINT ( 'NONE',  ( 122.6604860609119640, -3.387241619883791355, -18.17469012370385073 ) ) ;
#30137=VERTEX_POINT ( 'NONE', #35080 ) ;
#30138=CARTESIAN_POINT ( 'NONE',  ( 124.0495485609119584, -0.08252387247370887580, -11.91645802438286417 ) ) ;
#30166=ORIENTED_EDGE ( 'NONE', *, *, #15266, .T. ) ;
#30175=CARTESIAN_POINT ( 'NONE',  ( 123.5633766859119760, -9.033780868592240054, -16.85052413769862056 ) ) ;
#30218=VERTEX_POINT ( 'NONE', #17273 ) ;
#30250=CARTESIAN_POINT ( 'NONE',  ( 122.9382985609119743, -0.08252387247370887580, -11.91645802438286417 ) ) ;
#30264=CARTESIAN_POINT ( 'NONE',  ( 119.7434548109119703, -2.686739459735783875, -18.49927484697928648 ) ) ;
#30283=CARTESIAN_POINT ( 'NONE',  ( 120.8547048109119686, -2.527210466738041728, -8.967976844669124148 ) ) ;
#30284=CARTESIAN_POINT ( 'NONE',  ( 124.0495485609119584, -10.36940331770106916, -15.09355782777062061 ) ) ;
#30285=ORIENTED_EDGE ( 'NONE', *, *, #44562, .F. ) ;
#30309=CYLINDRICAL_SURFACE ( 'NONE', #37136, 1.587500000000000355 ) ;
#30315=CARTESIAN_POINT ( 'NONE',  ( 125.4584548109119737, -2.316996251443989241, -21.63995271010855248 ) ) ;
#30319=CARTESIAN_POINT ( 'NONE',  ( 120.2296266859119953, -0.06289925094097943703, -9.412459353600674206 ) ) ;
#30355=CARTESIAN_POINT ( 'NONE',  ( 121.6881423109119709, -9.959231468620755479, -10.70263013195267199 ) ) ;
#30361=CARTESIAN_POINT ( 'NONE',  ( 121.0630641859119976, -8.321307733199551748, -9.223433127585318303 ) ) ;
#30384=CARTESIAN_POINT ( 'NONE',  ( 121.0067200565388958, -8.485573535863895955, -17.53172993199661178 ) ) ;
#30391=EDGE_LOOP ( 'NONE', ( #6434, #42080, #22118, #34276 ) ) ;
#30399=CARTESIAN_POINT ( 'NONE',  ( 124.9069617844024975, -8.274459215933877232, -17.13193711621141802 ) ) ;
#30417=VERTEX_POINT ( 'NONE', #3354 ) ;
#30425=CARTESIAN_POINT ( 'NONE',  ( 122.9382985609119743, -0.08252387247370887580, -11.91645802438286417 ) ) ;
#30454=CARTESIAN_POINT ( 'NONE',  ( 125.4584548109119737, -4.863998795839242995, -13.39321520033831447 ) ) ;
#30473=CARTESIAN_POINT ( 'NONE',  ( 124.1916298109119765, -2.529232162390850913, -8.971805383624186447 ) ) ;
#30480=CARTESIAN_POINT ( 'NONE',  ( 122.3826735609119680, 0.6414057260225851653, -11.69287257290601723 ) ) ;
#30488=CARTESIAN_POINT ( 'NONE',  ( 123.7717360609119766, -3.387241619883525789, -18.17469012370376191 ) ) ;
#30490=CARTESIAN_POINT ( 'NONE',  ( 119.7434548109119703, -0.05003288430990287389, -11.46608162719201829 ) ) ;
#30499=CARTESIAN_POINT ( 'NONE',  ( 124.9868051361382868, -12.36944789948101331, -14.53642012793133986 ) ) ;
#30508=CARTESIAN_POINT ( 'NONE',  ( 119.6045485609119794, -0.08252387247370887580, -11.91645802438286417 ) ) ;
#30509=CARTESIAN_POINT ( 'NONE',  ( 122.4521266859119635, -9.033780868592240054, -16.85052413769862056 ) ) ;
#30542=CARTESIAN_POINT ( 'NONE',  ( 121.8965016859119856, -0.6942167230862511529, -9.935906262978006609 ) ) ;
#30561=CARTESIAN_POINT ( 'NONE',  ( 123.6328298109119714, -2.173413727453596511, -8.297982527556804655 ) ) ;
#30575=CARTESIAN_POINT ( 'NONE',  ( 121.5492360609119800, -6.564341423271550902, -7.887810678476487425 ) ) ;
#30580=CARTESIAN_POINT ( 'NONE',  ( 121.9659548109119811, -2.527210466738041728, -8.967976844669124148 ) ) ;
#30591=CIRCLE ( 'NONE', #38805, 8.000000000000001776 ) ;
#30592=ADVANCED_FACE ( 'NONE', ( #33793 ), #30842, .F. ) ;
#30605=FACE_OUTER_BOUND ( 'NONE', #29857, .T. ) ;
#30607=CARTESIAN_POINT ( 'NONE',  ( 121.2778147965036339, -8.305800998871424312, -17.19128988610634678 ) ) ;
#30623=CARTESIAN_POINT ( 'NONE',  ( 119.6740016859119748, -0.6942167230862511529, -9.935906262978006609 ) ) ;
#30625=CARTESIAN_POINT ( 'NONE',  ( 123.2855641859119942, -8.321307733199551748, -9.223433127585318303 ) ) ;
#30642=CYLINDRICAL_SURFACE ( 'NONE', #40550, 8.000000000000001776 ) ;
#30649=CARTESIAN_POINT ( 'NONE',  ( 121.8270485609119760, -0.08252387247370887580, -11.91645802438286417 ) ) ;
#30650=ORIENTED_EDGE ( 'NONE', *, *, #39832, .T. ) ;
#30675=CARTESIAN_POINT ( 'NONE',  ( 122.6009548109119720, -1.204716393658298523, -20.50726132761981901 ) ) ;
#30679=CARTESIAN_POINT ( 'NONE',  ( 119.8823610609119754, -6.340755971794695078, -8.611740276972781771 ) ) ;
#30683=DIRECTION ( 'NONE',  ( -1.000000000000000000, 0.000000000000000000, -0.000000000000000000 ) ) ;
#30709=CARTESIAN_POINT ( 'NONE',  ( 124.6573089231390128, -8.937933314682689812, -16.35309209503746786 ) ) ;
#30716=CARTESIAN_POINT ( 'NONE',  ( 125.4584548109119737, 3.382738713931011443, -10.84621265594315176 ) ) ;
#30737=CARTESIAN_POINT ( 'NONE',  ( 123.4939235609119663, -9.645473719204776586, -14.86997237629376656 ) ) ;
#30738=CARTESIAN_POINT ( 'NONE',  ( 122.1048610609119720, -6.340755971794695078, -8.611740276972781771 ) ) ;
#30756=CARTESIAN_POINT ( 'NONE',  ( 120.8547048109119686, -7.554583864224885481, -18.48844787311982785 ) ) ;
#30762=PLANE ( 'NONE',  #17834 ) ;
#30767=FACE_OUTER_BOUND ( 'NONE', #30391, .T. ) ;
#30770=CARTESIAN_POINT ( 'NONE',  ( 123.1466579359119891, -5.444069387712269226, -19.60292469916370450 ) ) ;
#30809=CARTESIAN_POINT ( 'NONE',  ( 121.2019704359119743, -10.25716656981731489, -12.88942061488890545 ) ) ;
#30820=CARTESIAN_POINT ( 'NONE',  ( 123.9584548109119737, -4.863998795839242995, -13.39321520033831447 ) ) ;
#30827=( BOUNDED_SURFACE ( )  B_SPLINE_SURFACE ( 1, 2, ( 
 ( #41811, #18069, #13765, #27674, #27450, #41373, #42245, #20824, #11010, #17625, #28118, #31519, #6700, #24032, #38806, #7575, #69, #42025, #7349, #37923, #41589, #24254, #38143, #6917, #34704, #28564, #7808, #8480, #22384, #8027, #726, #32188, #8700, #14876, #39265, #29230, #18962, #32636, #42471, #43136, #42694, #29448, #21717, #43363, #36280, #18293, #11464, #18521, #39492, #1402, #14649, #11234, #39939, #19194, #15542, #26034, #25367, #11906, #32852, #28789, #12131, #25807, #15318, #21935, #25143 ),
 ( #11681, #35826, #5047, #1623, #960, #4600, #22161, #25588, #36055, #32413, #36505, #39036, #35602, #18745, #42917, #4375, #22605, #1186, #15099, #8255, #29008, #4822, #39716, #5275, #44495, #26713, #30575, #26257, #30355, #29904, #1844, #5947, #15772, #40167, #40854, #9609, #40395, #33072, #19412, #41086, #2075, #26490, #16455, #6183, #19870, #29675, #44281, #43821, #16683, #8930, #13260, #23526, #5492, #12586, #5718, #40622, #33759, #43587, #12357, #27165, #6418, #2757, #9844, #9159, #13034 ) ),
 .UNSPECIFIED., .F., .F., .T. ) 
 B_SPLINE_SURFACE_WITH_KNOTS ( ( 2, 2 ),
 ( 3, 2, 2, 2, 2, 2, 2, 2, 2, 2, 2, 2, 2, 2, 2, 2, 2, 2, 2, 2, 2, 2, 2, 2, 2, 2, 2, 2, 2, 2, 2, 2, 3 ),
 ( 0.000000000000000000, 1.000000000000000000 ),
 ( 0.000000000000000000, 0.03125000000000000000, 0.06250000000000000000, 0.09375000000000000000, 0.1250000000000000000, 0.1562500000000000000, 0.1875000000000000000, 0.2187500000000000000, 0.2500000000000000000, 0.2812500000000000000, 0.3125000000000000000, 0.3437500000000000000, 0.3750000000000000000, 0.4062500000000000000, 0.4375000000000000000, 0.4687500000000000000, 0.5000000000000000000, 0.5312500000000000000, 0.5625000000000000000, 0.5937500000000000000, 0.6250000000000000000, 0.6562500000000000000, 0.6875000000000000000, 0.7187500000000000000, 0.7500000000000000000, 0.7812500000000000000, 0.8125000000000000000, 0.8437500000000000000, 0.8750000000000000000, 0.9062500000000000000, 0.9375000000000000000, 0.9687500000000000000, 1.000000000000000000 ),
 .UNSPECIFIED. ) 
 GEOMETRIC_REPRESENTATION_ITEM ( )  RATIONAL_B_SPLINE_SURFACE ( (
 ( 1.000000000000000000, 0.9238795325112869605, 1.000000000000000000, 0.9238795325112869605, 1.000000000000000000, 0.9238795325112869605, 1.000000000000000000, 0.9238795325112869605, 1.000000000000000000, 0.9238795325112869605, 1.000000000000000000, 0.9238795325112869605, 1.000000000000000000, 0.9238795325112869605, 1.000000000000000000, 0.9238795325112869605, 1.000000000000000000, 0.9238795325112869605, 1.000000000000000000, 0.9238795325112869605, 1.000000000000000000, 0.9238795325112869605, 1.000000000000000000, 0.9238795325112869605, 1.000000000000000000, 0.9238795325112869605, 1.000000000000000000, 0.9238795325112869605, 1.000000000000000000, 0.9238795325112869605, 1.000000000000000000, 0.9238795325112869605, 1.000000000000000000, 0.9238795325112869605, 1.000000000000000000, 0.9238795325112869605, 1.000000000000000000, 0.9238795325112869605, 1.000000000000000000, 0.9238795325112869605, 1.000000000000000000, 0.9238795325112869605, 1.000000000000000000, 0.9238795325112869605, 1.000000000000000000, 0.9238795325112869605, 1.000000000000000000, 0.9238795325112869605, 1.000000000000000000, 0.9238795325112869605, 1.000000000000000000, 0.9238795325112869605, 1.000000000000000000, 0.9238795325112869605, 1.000000000000000000, 0.9238795325112869605, 1.000000000000000000, 0.9238795325112869605, 1.000000000000000000, 0.9238795325112869605, 1.000000000000000000, 0.9238795325112869605, 1.000000000000000000, 0.9238795325112869605, 1.000000000000000000),
 ( 1.000000000000000000, 0.9238795325112869605, 1.000000000000000000, 0.9238795325112869605, 1.000000000000000000, 0.9238795325112869605, 1.000000000000000000, 0.9238795325112869605, 1.000000000000000000, 0.9238795325112869605, 1.000000000000000000, 0.9238795325112869605, 1.000000000000000000, 0.9238795325112869605, 1.000000000000000000, 0.9238795325112869605, 1.000000000000000000, 0.9238795325112869605, 1.000000000000000000, 0.9238795325112869605, 1.000000000000000000, 0.9238795325112869605, 1.000000000000000000, 0.9238795325112869605, 1.000000000000000000, 0.9238795325112869605, 1.000000000000000000, 0.9238795325112869605, 1.000000000000000000, 0.9238795325112869605, 1.000000000000000000, 0.9238795325112869605, 1.000000000000000000, 0.9238795325112869605, 1.000000000000000000, 0.9238795325112869605, 1.000000000000000000, 0.9238795325112869605, 1.000000000000000000, 0.9238795325112869605, 1.000000000000000000, 0.9238795325112869605, 1.000000000000000000, 0.9238795325112869605, 1.000000000000000000, 0.9238795325112869605, 1.000000000000000000, 0.9238795325112869605, 1.000000000000000000, 0.9238795325112869605, 1.000000000000000000, 0.9238795325112869605, 1.000000000000000000, 0.9238795325112869605, 1.000000000000000000, 0.9238795325112869605, 1.000000000000000000, 0.9238795325112869605, 1.000000000000000000, 0.9238795325112869605, 1.000000000000000000, 0.9238795325112869605, 1.000000000000000000, 0.9238795325112869605, 1.000000000000000000) ) ) 
 REPRESENTATION_ITEM ( '' )  SURFACE ( )  );
#30842=PLANE ( 'NONE',  #13956 ) ;
#30845=CARTESIAN_POINT ( 'NONE',  ( 120.0907204359119760, -10.25716656981731489, -12.88942061488890545 ) ) ;
#30849=ORIENTED_EDGE ( 'NONE', *, *, #24771, .T. ) ;
#30865=CARTESIAN_POINT ( 'NONE',  ( 120.8547048109119686, -2.527210466738041283, -8.967976844669125924 ) ) ;
#30867=ORIENTED_EDGE ( 'NONE', *, *, #13050, .F. ) ;
#30874=CARTESIAN_POINT ( 'NONE',  ( 122.5910329359119970, -5.367793381288652910, -18.78638297431638904 ) ) ;
#30884=DIRECTION ( 'NONE',  ( -1.000000000000000000, 0.000000000000000000, -0.000000000000000000 ) ) ;
#30897=CARTESIAN_POINT ( 'NONE',  ( 125.4584548109119737, -8.963735245270648022, -18.43723750849711962 ) ) ;
#30904=CYLINDRICAL_SURFACE ( 'NONE', #29180, 8.000000000000001776 ) ;
#30923=CARTESIAN_POINT ( 'NONE',  ( 124.1221766859119811, -0.6978242514986119360, -9.938897388174531500 ) ) ;
#30956=CARTESIAN_POINT ( 'NONE',  ( 121.0630641859119976, -0.8832429491016019485, -18.19431474523657855 ) ) ;
#30962=CARTESIAN_POINT ( 'NONE',  ( 119.8129079359119942, -4.360204210389833968, -8.000047426360245240 ) ) ;
#30990=CIRCLE ( 'NONE', #3326, 1.587500000000000355 ) ;
#30994=CARTESIAN_POINT ( 'NONE',  ( 123.0077516859119839, -9.665098340737509730, -17.37397104707595474 ) ) ;
#31016=FACE_OUTER_BOUND ( 'NONE', #20027, .T. ) ;
#31026=CARTESIAN_POINT ( 'NONE',  ( 120.1601735609119856, 0.6414057260225851653, -11.69287257290600657 ) ) ;
#31047=EDGE_LOOP ( 'NONE', ( #12893, #16464, #27223, #30285 ) ) ;
#31091=CARTESIAN_POINT ( 'NONE',  ( 124.1884548109119777, -2.527210466738041728, -8.967976844669124148 ) ) ;
#31174=CARTESIAN_POINT ( 'NONE',  ( 122.4521266859119635, -0.06289925094097943703, -9.412459353600674206 ) ) ;
#31180=CARTESIAN_POINT ( 'NONE',  ( 123.0772048109119652, -2.527210466738041728, -8.967976844669124148 ) ) ;
#31190=CARTESIAN_POINT ( 'NONE',  ( 120.2524138005195482, -8.246127466884534130, -17.07828452773560812 ) ) ;
#31212=CARTESIAN_POINT ( 'NONE',  ( 122.9382985609119743, -10.36940331770106916, -15.09355782777062061 ) ) ;
#31246=CARTESIAN_POINT ( 'NONE',  ( 120.5074391859119913, -8.844754642576884152, -8.592115655440050404 ) ) ;
#31257=DIRECTION ( 'NONE',  ( 1.000000000000000000, 0.000000000000000000, 0.000000000000000000 ) ) ;
#31280=CARTESIAN_POINT ( 'NONE',  ( 119.1878298109119783, -7.200787124940443817, -17.81845355600750835 ) ) ;
#31288=AXIS2_PLACEMENT_3D ( 'NONE', #39005, #35341, #696 ) ;
#31303=ORIENTED_EDGE ( 'NONE', *, *, #24554, .T. ) ;
#31307=CARTESIAN_POINT ( 'NONE',  ( 123.4244704359119709, -10.25716656981731489, -12.88942061488890545 ) ) ;
#31310=CARTESIAN_POINT ( 'NONE',  ( 125.1375072647485638, -0.5766298686391078121, -7.327922817638773623 ) ) ;
#31313=LINE ( 'NONE', #23600, #5209 ) ;
#31367=CARTESIAN_POINT ( 'NONE',  ( 121.9272896737536911, -8.611453504372539314, -17.77011218421760574 ) ) ;
#31372=DIRECTION ( 'NONE',  ( 1.000000000000000000, 0.000000000000000000, 0.000000000000000000 ) ) ;
#31389=CARTESIAN_POINT ( 'NONE',  ( 122.7299391859119737, -8.844754642576884152, -8.592115655440050404 ) ) ;
#31396=CARTESIAN_POINT ( 'NONE',  ( 122.3826735609119680, -9.645473719204776586, -14.86997237629376656 ) ) ;
#31403=PRESENTATION_STYLE_ASSIGNMENT (( #17297 ) ) ;
#31413=CARTESIAN_POINT ( 'NONE',  ( 120.1601735609119856, 0.6414057260225851653, -11.69287257290600657 ) ) ;
#31420=CARTESIAN_POINT ( 'NONE',  ( 124.5059548109119731, -5.999156839134619723, -18.26265215102738892 ) ) ;
#31422=CARTESIAN_POINT ( 'NONE',  ( 124.4871289243369006, -9.531683815157249384, -11.52482648355480599 ) ) ;
#31427=CARTESIAN_POINT ( 'NONE',  ( 125.2512653913890830, -10.90577519989732558, -9.364198568131605782 ) ) ;
#31429=CARTESIAN_POINT ( 'NONE',  ( 122.7299391859119737, -8.844754642576884152, -8.592115655440050404 ) ) ;
#31497=VERTEX_POINT ( 'NONE', #210 ) ;
#31519=CARTESIAN_POINT ( 'NONE',  ( 121.0630641859119976, -8.321307733199551748, -9.223433127585318303 ) ) ;
#31532=CARTESIAN_POINT ( 'NONE',  ( 122.2437673109119629, 0.2312338769422704887, -16.08380026872395874 ) ) ;
#31536=CARTESIAN_POINT ( 'NONE',  ( 124.1685108350147857, -2.421128313536792032, -5.786646012007111040 ) ) ;
#31575=VECTOR ( 'NONE', #6223, 999.9999999999998863 ) ;
#31592=CARTESIAN_POINT ( 'NONE',  ( 121.6065266009169221, -8.403782945130238602, -17.37684090985456820 ) ) ;
#31604=ORIENTED_EDGE ( 'NONE', *, *, #44365, .T. ) ;
#31616=FACE_OUTER_BOUND ( 'NONE', #23270, .T. ) ;
#31623=CARTESIAN_POINT ( 'NONE',  ( 121.7575954359119805, 0.5291689781388270175, -13.89700978578772705 ) ) ;
#31644=CARTESIAN_POINT ( 'NONE',  ( 124.3999891859120055, -8.318316608003341273, -9.227040655997777563 ) ) ;
#31648=B_SPLINE_CURVE_WITH_KNOTS ( 'NONE', 3,
 ( #39625, #32758, #39167, #36405, #5175, #28694, #22070, #35962, #4732, #32323, #19093, #1754, #35506, #1312, #11361, #25270, #32541, #22293, #4953, #18866, #15453, #29357, #43272, #11477, #35840, #7823, #32201, #21730, #36068, #18758, #11023, #21502, #21276, #39051, #4391, #42708, #18082, #14662, #32426, #10798, #739, #24695, #11693, #28801, #3938, #29021, #4165, #25602, #39279, #7587, #42932, #35617, #38583, #21949, #31976, #35158, #7361, #14214, #28578, #17859, #31756, #8268, #39507, #42485, #22173, #14438, #28129 ),
 .UNSPECIFIED., .F., .F.,
 ( 4, 3, 3, 3, 3, 3, 3, 3, 3, 3, 3, 3, 3, 3, 3, 3, 3, 3, 3, 3, 3, 3, 4 ),
 ( 2.779028226719264772E-17, 1.132108768669561938E-05, 5.660629526298920192E-05, 0.0002378019964192440395, 0.0003283778960097989935, 0.0005095735978542089914, 0.0006001494977465600227, 0.0007813452071915360847, 0.0008719211078674949950, 0.0009624970091562879077, 0.001143692739419350157, 0.001234268642094720012, 0.001324844545703623934, 0.001506040307844935030, 0.001596616213391234725, 0.001777812005347669932, 0.001868387913206439720, 0.001958963822483724988, 0.002140159663056734936, 0.002230735575091844988, 0.002321311488774285316, 0.002474333065496200044, 0.002627496479460559795 ),
 .UNSPECIFIED. ) ;
#31652=CARTESIAN_POINT ( 'NONE',  ( 122.1048610609119720, -3.163656168406935087, -18.89861972220014508 ) ) ;
#31661=CARTESIAN_POINT ( 'NONE',  ( 121.8270485609119760, -0.08252387247370714107, -11.91645802438286950 ) ) ;
#31697=DIRECTION ( 'NONE',  ( 0.000000000000000000, -0.4669533266896290225, -0.8842819633428516957 ) ) ;
#31710=ADVANCED_FACE ( 'NONE', ( #30605 ), #16255, .T. ) ;
#31753=ORIENTED_EDGE ( 'NONE', *, *, #26771, .F. ) ;
#31756=CARTESIAN_POINT ( 'NONE',  ( 124.5867640960332068, -9.779101121451267531, -14.32922897161243903 ) ) ;
#31758=CARTESIAN_POINT ( 'NONE',  ( 122.1743141859119817, -0.8832429491016019485, -18.19431474523657855 ) ) ;
#31761=CARTESIAN_POINT ( 'NONE',  ( 119.7434548109119845, -2.551128697860804095, -8.956764161815621961 ) ) ;
#31784=VERTEX_POINT ( 'NONE', #38269 ) ;
#31860=ORIENTED_EDGE ( 'NONE', *, *, #10799, .F. ) ;
#31863=CARTESIAN_POINT ( 'NONE',  ( 119.9518141859119851, -8.321307733199551748, -9.223433127585318303 ) ) ;
#31876=CARTESIAN_POINT ( 'NONE',  ( 125.3566265649659073, -10.97543583693571989, -9.883038420138618108 ) ) ;
#31888=CARTESIAN_POINT ( 'NONE',  ( 122.0354079359119908, -4.360204210389830415, -8.000047426360247016 ) ) ;
#31893=CARTESIAN_POINT ( 'NONE',  ( 120.3685329359119862, -4.283928203966213211, -7.183505701512925334 ) ) ;
#31976=CARTESIAN_POINT ( 'NONE',  ( 124.5807827564429431, -9.809262384845451876, -14.15072059919280534 ) ) ;
#31977=CARTESIAN_POINT ( 'NONE',  ( 121.8965016859119856, -9.665098340737509730, -17.37397104707595474 ) ) ;
#31980=CARTESIAN_POINT ( 'NONE',  ( 125.2231329858125264, -2.209379012606767390, -6.577246691088228125 ) ) ;
#31983=EDGE_CURVE ( 'NONE', #5920, #39662, #18443, .T. ) ;
#31995=VERTEX_POINT ( 'NONE', #43055 ) ;
#32018=EDGE_LOOP ( 'NONE', ( #11336, #1544, #17253, #37791 ) ) ;
#32029=EDGE_CURVE ( 'NONE', #38271, #28617, #42834, .T. ) ;
#32062=CARTESIAN_POINT ( 'NONE',  ( 122.3826735609119680, -9.645473719204776586, -14.86997237629376656 ) ) ;
#32079=CARTESIAN_POINT ( 'NONE',  ( 123.9800954359119771, -11.07370829466463569, -12.81314460846529002 ) ) ;
#32083=CARTESIAN_POINT ( 'NONE',  ( 120.2990798109119766, -7.200787124940443817, -17.81845355600750835 ) ) ;
#32098=CARTESIAN_POINT ( 'NONE',  ( 124.6574308310802621, -11.08444345384245544, -8.635704745763826296 ) ) ;
#32116=CARTESIAN_POINT ( 'NONE',  ( 121.4103298109119748, -2.173413727453600508, -8.297982527556802879 ) ) ;
#32118=CARTESIAN_POINT ( 'NONE',  ( 120.2542535264548889, -8.247323210606168686, -17.08054893949881148 ) ) ;
#32157=CARTESIAN_POINT ( 'NONE',  ( 120.6463454359119822, 0.5291689781388270175, -13.89700978578772705 ) ) ;
#32188=CARTESIAN_POINT ( 'NONE',  ( 122.4521266859119635, -9.033780868592240054, -16.85052413769862056 ) ) ;
#32201=CARTESIAN_POINT ( 'NONE',  ( 124.5391625940361138, -9.844727480109712658, -12.94707959821569077 ) ) ;
#32203=CARTESIAN_POINT ( 'NONE',  ( 124.1190016859119680, -9.665098340737509730, -17.37397104707595474 ) ) ;
#32226=( GEOMETRIC_REPRESENTATION_CONTEXT ( 3 ) GLOBAL_UNCERTAINTY_ASSIGNED_CONTEXT ( ( #956 ) ) GLOBAL_UNIT_ASSIGNED_CONTEXT ( ( #5660, #34594, #3378 ) ) REPRESENTATION_CONTEXT ( 'NONE', 'WORKASPACE' ) );
#32279=( BOUNDED_CURVE ( )  B_SPLINE_CURVE ( 2, ( #33052, #3363, #1826, #3141, #15981, #43570, #29657, #23905, #43801, #12339, #22811, #45094, #29884, #40149, #36706 ),
 .UNSPECIFIED., .F., .T. ) 
 B_SPLINE_CURVE_WITH_KNOTS ( ( 3, 2, 2, 2, 2, 2, 2, 3 ),
 ( 0.7602707595410509445, 0.7812500000000000000, 0.8125000000000000000, 0.8437500000000000000, 0.8750000000000000000, 0.9062500000000000000, 0.9375000000000000000, 0.9667092643636859828 ),
 .UNSPECIFIED. ) 
 CURVE ( )  GEOMETRIC_REPRESENTATION_ITEM ( )  RATIONAL_B_SPLINE_CURVE ( ( 0.9664089390052280626, 0.9488976130786129781, 1.000000000000000000, 0.9238795325112869605, 1.000000000000000000, 0.9238795325112869605, 1.000000000000000000, 0.9238795325112869605, 1.000000000000000000, 0.9238795325112869605, 1.000000000000000000, 0.9238795325112869605, 1.000000000000000000, 0.9288504685323130117, 0.9907073674001189989 ) ) 
 REPRESENTATION_ITEM ( '' )  );
#32291=CARTESIAN_POINT ( 'NONE',  ( 121.2714235609119697, -9.645473719204776586, -14.86997237629376656 ) ) ;
#32311=CARTESIAN_POINT ( 'NONE',  ( 122.4521266859119635, -0.06289925094097943703, -9.412459353600674206 ) ) ;
#32315=CARTESIAN_POINT ( 'NONE',  ( 122.3132204359119868, 1.345710702986147034, -13.97328579221134426 ) ) ;
#32318=CARTESIAN_POINT ( 'NONE',  ( 122.4700493874820069, -6.063848558940142297, -18.38516058545102183 ) ) ;
#32323=CARTESIAN_POINT ( 'NONE',  ( 124.5144432999385913, -9.734490656202709147, -12.26242464252682396 ) ) ;
#32327=CARTESIAN_POINT ( 'NONE',  ( 125.0211000582884537, -11.98805063819766303, -10.86686075357930470 ) ) ;
#32339=CARTESIAN_POINT ( 'NONE',  ( 119.9518141859119851, -0.8832429491016020595, -18.19431474523658565 ) ) ;
#32374=CARTESIAN_POINT ( 'NONE',  ( 125.4584548109119737, 2.768327990826033425, -17.42353644532102308 ) ) ;
#32375=CIRCLE ( 'NONE', #7640, 1.587500000000000577 ) ;
#32403=VERTEX_POINT ( 'NONE', #39447 ) ;
#32413=CARTESIAN_POINT ( 'NONE',  ( 120.3685329359119862, -4.283928203966213211, -7.183505701512925334 ) ) ;
#32418=CARTESIAN_POINT ( 'NONE',  ( 124.1497896737536877, -8.611453504372539314, -17.77011218421760574 ) ) ;
#32426=CARTESIAN_POINT ( 'NONE',  ( 124.5571602873148294, -9.865299344075070920, -13.45945633590898538 ) ) ;
#32437=ORIENTED_EDGE ( 'NONE', *, *, #35385, .F. ) ;
#32451=CARTESIAN_POINT ( 'NONE',  ( 120.8456493241987317, -6.333924026435813204, -18.89660969823682279 ) ) ;
#32494=ORIENTED_EDGE ( 'NONE', *, *, #24246, .F. ) ;
#32508=CARTESIAN_POINT ( 'NONE',  ( 120.1601735609119856, -9.645473719204776586, -14.86997237629376656 ) ) ;
#32533=CARTESIAN_POINT ( 'NONE',  ( 120.7157985609119635, -0.08252387247370887580, -11.91645802438286417 ) ) ;
#32541=CARTESIAN_POINT ( 'NONE',  ( 124.5252192005878698, -9.794068186057833358, -12.55818921246619624 ) ) ;
#32546=CARTESIAN_POINT ( 'NONE',  ( 125.1670174127246469, -12.14974810887502521, -14.66706061084391699 ) ) ;
#32564=VERTEX_POINT ( 'NONE', #12312 ) ;
#32567=CARTESIAN_POINT ( 'NONE',  ( 123.2855641859119942, -0.8832429491016019485, -18.19431474523657855 ) ) ;
#32636=CARTESIAN_POINT ( 'NONE',  ( 122.8688454359119646, 0.5291689781388270175, -13.89700978578772705 ) ) ;
#32651=CARTESIAN_POINT ( 'NONE',  ( 119.7434548109119703, -4.863998795839242995, -13.39321520033831447 ) ) ;
#32695=CARTESIAN_POINT ( 'NONE',  ( 125.0211000582877006, -8.115061802111570799, -6.569347472097891050 ) ) ;
#32700=CARTESIAN_POINT ( 'NONE',  ( 123.0772048109119652, -2.527210466738041728, -8.967976844669124148 ) ) ;
#32721=CARTESIAN_POINT ( 'NONE',  ( 125.2231329858062878, 1.951969713414328123, -16.04783498356866644 ) ) ;
#32727=CARTESIAN_POINT ( 'NONE',  ( 124.1190016859119680, -9.665098340737509730, -17.37397104707595474 ) ) ;
#32739=CIRCLE ( 'NONE', #31288, 8.000000000000001776 ) ;
#32750=CARTESIAN_POINT ( 'NONE',  ( 119.5350954359119839, 0.5291689781388270175, -13.89700978578772705 ) ) ;
#32758=CARTESIAN_POINT ( 'NONE',  ( 124.5060894275148087, -9.676259452193004762, -12.03595266200289338 ) ) ;
#32763=CARTESIAN_POINT ( 'NONE',  ( 125.3495511204625927, -11.67227941590863871, -15.26752859910581606 ) ) ;
#32770=ORIENTED_EDGE ( 'NONE', *, *, #3188, .F. ) ;
#32782=CARTESIAN_POINT ( 'NONE',  ( 121.0630641859119976, -0.8832429491016019485, -18.19431474523657855 ) ) ;
#32783=CARTESIAN_POINT ( 'NONE',  ( 123.9106423109119675, -9.959231468620755479, -10.70263013195267199 ) ) ;
#32816=CARTESIAN_POINT ( 'NONE',  ( 124.9868051361299166, -1.575707845324203493, -20.23615509330177531 ) ) ;
#32852=CARTESIAN_POINT ( 'NONE',  ( 124.3273610609119686, -6.340755971794695078, -8.611740276972781771 ) ) ;
#32856=CARTESIAN_POINT ( 'NONE',  ( 120.4379860609119675, -3.387241619883791355, -18.17469012370385073 ) ) ;
#32857=ADVANCED_FACE ( 'NONE', ( #2935 ), #27459, .F. ) ;
#32920=CARTESIAN_POINT ( 'NONE',  ( 122.9382985609119743, -0.08252387247370887580, -11.91645802438286417 ) ) ;
#32971=CARTESIAN_POINT ( 'NONE',  ( 122.3826735609119680, -9.645473719204776586, -14.86997237629376656 ) ) ;
#32973=CARTESIAN_POINT ( 'NONE',  ( 122.4218349628857254, -6.095137211460710525, -18.44441274085890115 ) ) ;
#32984=DIRECTION ( 'NONE',  ( 1.000000000000000000, 0.000000000000000000, 0.000000000000000000 ) ) ;
#33004=CARTESIAN_POINT ( 'NONE',  ( 122.3826735609119680, 0.6414057260225851653, -11.69287257290600657 ) ) ;
#33005=CARTESIAN_POINT ( 'NONE',  ( 121.5492360609119800, -6.564341423271550902, -7.887810678476487425 ) ) ;
#33027=ORIENTED_EDGE ( 'NONE', *, *, #26712, .T. ) ;
#33035=CARTESIAN_POINT ( 'NONE',  ( 121.4069907289968313, -6.032552146994438758, -18.32589373581284420 ) ) ;
#33052=CARTESIAN_POINT ( 'NONE',  ( 123.6776560953690591, -6.001247023715324147, -18.26661038929047010 ) ) ;
#33064=EDGE_CURVE ( 'NONE', #11695, #22801, #23539, .T. ) ;
#33072=CARTESIAN_POINT ( 'NONE',  ( 122.3132204359119868, 1.345710702986147034, -13.97328579221134426 ) ) ;
#33076=CARTESIAN_POINT ( 'NONE',  ( 120.7157985609119635, -0.08252387247370887580, -11.91645802438286417 ) ) ;
#33098=VERTEX_POINT ( 'NONE', #44853 ) ;
#33168=CARTESIAN_POINT ( 'NONE',  ( 125.0302870206147503, 2.248781333534738636, -15.92343447212006957 ) ) ;
#33199=CARTESIAN_POINT ( 'NONE',  ( 122.3132204359119868, -10.25716656981731489, -12.88942061488890545 ) ) ;
#33203=CARTESIAN_POINT ( 'NONE',  ( 124.9009360172564556, 2.024339171940786386, -10.02384774242203136 ) ) ;
#33212=DIRECTION ( 'NONE',  ( -1.000000000000000000, 0.000000000000000000, -0.000000000000000000 ) ) ;
#33213=CYLINDRICAL_SURFACE ( 'NONE', #24509, 5.000000000000000888 ) ;
#33234=CARTESIAN_POINT ( 'NONE',  ( 123.0077516859119839, -9.665098340737509730, -17.37397104707595474 ) ) ;
#33235=CARTESIAN_POINT ( 'NONE',  ( 121.8270485609119760, -10.36940331770106916, -15.09355782777062061 ) ) ;
#33251=( NAMED_UNIT ( * ) PLANE_ANGLE_UNIT ( ) SI_UNIT ( $, .RADIAN. ) );
#33265=CARTESIAN_POINT ( 'NONE',  ( 125.3328280236779904, -3.140424913533931939, -20.28213322351574277 ) ) ;
#33268=CARTESIAN_POINT ( 'NONE',  ( 124.5357204359119550, -10.25716656981731489, -12.88942061488890545 ) ) ;
#33289=ORIENTED_EDGE ( 'NONE', *, *, #22336, .F. ) ;
#33303=CARTESIAN_POINT ( 'NONE',  ( 122.7993923109119692, -0.4387604401700512802, -15.73000352943951619 ) ) ;
#33336=CARTESIAN_POINT ( 'NONE',  ( 120.6550937114597275, -6.208002839291213881, -18.65814938918611077 ) ) ;
#33338=ORIENTED_EDGE ( 'NONE', *, *, #27263, .T. ) ;
#33357=CARTESIAN_POINT ( 'NONE',  ( 121.2019704359119885, -10.25716656981731489, -12.88942061488890545 ) ) ;
#33359=CARTESIAN_POINT ( 'NONE',  ( 125.3303382280772382, -6.508808502060079881, -6.467457712844120188 ) ) ;
#33388=CARTESIAN_POINT ( 'NONE',  ( 124.9774582099995683, 1.254580239582103962, -17.90916344451578368 ) ) ;
#33425=CARTESIAN_POINT ( 'NONE',  ( 121.6881423109119709, -9.959231468620755479, -10.70263013195267021 ) ) ;
#33430=CARTESIAN_POINT ( 'NONE',  ( 119.7434548109119703, -1.219197665648892759, -17.48381333488896061 ) ) ;
#33449=CARTESIAN_POINT ( 'NONE',  ( 120.5074391859119913, -1.406689858478933353, -17.56299727309130887 ) ) ;
#33450=CARTESIAN_POINT ( 'NONE',  ( 122.7299391859119737, -8.844754642576884152, -8.592115655440050404 ) ) ;
#33488=CARTESIAN_POINT ( 'NONE',  ( 122.5215798109119874, -7.200787124940443817, -17.81845355600750835 ) ) ;
#33513=VECTOR ( 'NONE', #16138, 1000.000000000000000 ) ;
#33521=AXIS2_PLACEMENT_3D ( 'NONE', #33623, #12916, #20653 ) ;
#33526=CARTESIAN_POINT ( 'NONE',  ( 120.0907204359119760, 1.345710702986147034, -13.97328579221134426 ) ) ;
#33527=B_SPLINE_CURVE_WITH_KNOTS ( 'NONE', 3,
 ( #5109, #22894, #25654, #29968, #12423, #5342, #12654, #25871, #36118, #43205, #19478, #36789, #32695, #4662, #5559, #8764, #29066, #8998, #29291, #33359, #19259, #26094, #11746, #1689, #8544, #1249, #15388, #22670, #8320, #35893, #39998, #15608, #22446, #39560, #29515, #11972 ),
 .UNSPECIFIED., .F., .F.,
 ( 4, 2, 2, 2, 2, 1, 2, 2, 2, 2, 2, 2, 2, 1, 2, 2, 2, 2, 4 ),
 ( 0.000000000000000000, 0.06250000000006282475, 0.1250000000001256495, 0.1875000000001884604, 0.2187500000002227940, 0.2343750000002370326, 0.2421875000002444156, 0.2500000000002517986, 0.3750000000002657874, 0.5000000000002797762, 0.6250000000002938760, 0.6875000000003008704, 0.7187500000003042011, 0.7343750000003009815, 0.7421875000002994271, 0.7500000000002977618, 0.8125000000002214895, 0.8750000000001452172, 1.000000000000000000 ),
 .UNSPECIFIED. ) ;
#33536=CYLINDRICAL_SURFACE ( 'NONE', #20022, 5.000000000000000888 ) ;
#33549=DIRECTION ( 'NONE',  ( -1.000000000000000000, 0.000000000000000000, -0.000000000000000000 ) ) ;
#33558=CARTESIAN_POINT ( 'NONE',  ( 119.7434548109119703, -2.613043214085062793, -8.928554074455437473 ) ) ;
#33562=CARTESIAN_POINT ( 'NONE',  ( 123.2067687714537811, -6.306599966548167124, -18.84486539759072699 ) ) ;
#33564=CARTESIAN_POINT ( 'NONE',  ( 125.4400992928798075, -8.599374347808629082, -17.74723756341217396 ) ) ;
#33565=CARTESIAN_POINT ( 'NONE',  ( 120.8547048109119686, -2.527210466738041728, -8.967976844669124148 ) ) ;
#33574=CYLINDRICAL_SURFACE ( 'NONE', #19750, 8.000000000000001776 ) ;
#33616=CARTESIAN_POINT ( 'NONE',  ( 124.8633137343444446, 2.423166897745142823, -15.87367557320988531 ) ) ;
#33623=CARTESIAN_POINT ( 'NONE',  ( 119.7434548109119703, -4.863998795839242995, -13.39321520033831447 ) ) ;
#33647=CARTESIAN_POINT ( 'NONE',  ( 123.2161110609119703, -6.340755971794695078, -8.611740276972781771 ) ) ;
#33656=CARTESIAN_POINT ( 'NONE',  ( 121.6186891859119754, -8.844754642576878823, -8.592115655440055733 ) ) ;
#33660=CARTESIAN_POINT ( 'NONE',  ( 124.0527235609119714, -0.08666061303663243065, -11.91773565553389425 ) ) ;
#33662=CARTESIAN_POINT ( 'NONE',  ( 119.7434548109119561, -0.09372932658121500837, -15.89155818700682943 ) ) ;
#33674=CARTESIAN_POINT ( 'NONE',  ( 124.1570456159114286, -12.80247570057301587, -14.38293432349187384 ) ) ;
#33680=ORIENTED_EDGE ( 'NONE', *, *, #37017, .F. ) ;
#33682=CYLINDRICAL_SURFACE ( 'NONE', #28406, 1.587500000000000577 ) ;
#33684=CARTESIAN_POINT ( 'NONE',  ( 122.9382985609119743, -10.36940331770106916, -15.09355782777062061 ) ) ;
#33685=CARTESIAN_POINT ( 'NONE',  ( 124.1884548109119777, -7.554583864224885481, -18.48844787311982785 ) ) ;
#33721=CARTESIAN_POINT ( 'NONE',  ( 125.2103759035168338, -1.921298038565348199, -20.10252925763280984 ) ) ;
#33724=CARTESIAN_POINT ( 'NONE',  ( 119.7434548109119703, -7.554583864224885481, -18.48844787311982785 ) ) ;
#33734=DIRECTION ( 'NONE',  ( -1.000000000000000000, 0.000000000000000000, -0.000000000000000000 ) ) ;
#33759=CARTESIAN_POINT ( 'NONE',  ( 123.6328298109119714, -2.173413727453600508, -8.297982527556802879 ) ) ;
#33763=ORIENTED_EDGE ( 'NONE', *, *, #2480, .F. ) ;
#33764=CARTESIAN_POINT ( 'NONE',  ( 121.4103298109119748, -7.200787124940443817, -17.81845355600750835 ) ) ;
#33790=VERTEX_POINT ( 'NONE', #43435 ) ;
#33793=FACE_OUTER_BOUND ( 'NONE', #15043, .T. ) ;
#33796=CARTESIAN_POINT ( 'NONE',  ( 123.1158699480702552, -6.365377317481717867, -18.95617363400926081 ) ) ;
#33804=ADVANCED_FACE ( 'NONE', ( #9227 ), #38477, .F. ) ;
#33825=CARTESIAN_POINT ( 'NONE',  ( 121.7575954359119805, 0.5291689781388270175, -13.89700978578772705 ) ) ;
#33880=CARTESIAN_POINT ( 'NONE',  ( 122.2437673109119629, -9.289237151508434209, -11.05642687123711276 ) ) ;
#33894=CARTESIAN_POINT ( 'NONE',  ( 119.7434548109119845, -3.753605393790139466, -18.88744880365131351 ) ) ;
#33913=CARTESIAN_POINT ( 'NONE',  ( 122.7299391859119737, -8.844754642576884152, -8.592115655440050404 ) ) ;
#33914=CARTESIAN_POINT ( 'NONE',  ( 121.9659548109119811, -2.527210466738041728, -8.967976844669124148 ) ) ;
#33923=B_SPLINE_CURVE_WITH_KNOTS ( 'NONE', 3,
 ( #37024, #40699, #44351, #34507, #41391, #10589, #11033, #14225, #17645, #17869 ),
 .UNSPECIFIED., .F., .F.,
 ( 4, 2, 2, 2, 4 ),
 ( 0.000000000000000000, 0.2500000000000000000, 0.5000000000000000000, 0.7500000000000000000, 1.000000000000000000 ),
 .UNSPECIFIED. ) ;
#33924=CARTESIAN_POINT ( 'NONE',  ( 120.2515881224973100, -8.245590802997449842, -17.07726823302562025 ) ) ;
#33955=CARTESIAN_POINT ( 'NONE',  ( 124.6051735609119646, -9.645473719204776586, -14.86997237629376656 ) ) ;
#33978=FACE_OUTER_BOUND ( 'NONE', #3648, .T. ) ;
#33986=ORIENTED_EDGE ( 'NONE', *, *, #20300, .T. ) ;
#33993=CARTESIAN_POINT ( 'NONE',  ( 121.8965016859119856, -0.6942167230862511529, -9.935906262978006609 ) ) ;
#34007=DIRECTION ( 'NONE',  ( -1.000000000000000000, 0.000000000000000000, -0.000000000000000000 ) ) ;
#34025=VERTEX_POINT ( 'NONE', #15644 ) ;
#34031=CARTESIAN_POINT ( 'NONE',  ( 119.4656423109119743, -0.4387604401700512802, -15.73000352943951619 ) ) ;
#34058=CARTESIAN_POINT ( 'NONE',  ( 124.7440798109119697, -7.200787124940443817, -17.81845355600750835 ) ) ;
#34059=ORIENTED_EDGE ( 'NONE', *, *, #20953, .T. ) ;
#34061=CARTESIAN_POINT ( 'NONE',  ( 124.1726284085826251, 3.074464114999942765, -12.40349330775361025 ) ) ;
#34109=CARTESIAN_POINT ( 'NONE',  ( 123.8443641859119992, -1.409680983675146271, -17.55938974467885316 ) ) ;
#34123=CARTESIAN_POINT ( 'NONE',  ( 122.9382985609119743, -0.08252387247370714107, -11.91645802438286950 ) ) ;
#34127=CARTESIAN_POINT ( 'NONE',  ( 119.7434548109119561, -4.073510663624176686, -18.95665693152923126 ) ) ;
#34141=ORIENTED_EDGE ( 'NONE', *, *, #11674, .F. ) ;
#34145=CARTESIAN_POINT ( 'NONE',  ( 121.6186891859119896, -1.406689858478933353, -17.56299727309130887 ) ) ;
#34146=CARTESIAN_POINT ( 'NONE',  ( 120.5768923109119868, -0.4387604401700512802, -15.73000352943951619 ) ) ;
#34155=CARTESIAN_POINT ( 'NONE',  ( 120.2542535264548889, -8.247323210606168686, -17.08054893949881148 ) ) ;
#34168=CARTESIAN_POINT ( 'NONE',  ( 125.4584548109119737, -6.396860573544808304, -19.01579431533362907 ) ) ;
#34173=CARTESIAN_POINT ( 'NONE',  ( 121.1658748871816300, -6.188980713775695364, -18.62212668298318619 ) ) ;
#34176=CARTESIAN_POINT ( 'NONE',  ( 123.0772048109119652, -2.527210466738041728, -8.967976844669124148 ) ) ;
#34197=CARTESIAN_POINT ( 'NONE',  ( 124.3880659103642188, -8.454079026182052203, -17.47208793939444149 ) ) ;
#34216=CARTESIAN_POINT ( 'NONE',  ( 122.9382985609119743, -0.08252387247370887580, -11.91645802438286417 ) ) ;
#34227=FACE_OUTER_BOUND ( 'NONE', #10619, .T. ) ;
#34255=CARTESIAN_POINT ( 'NONE',  ( 119.9486391859119863, -8.318316608003105017, -9.227040655997587493 ) ) ;
#34276=ORIENTED_EDGE ( 'NONE', *, *, #16779, .F. ) ;
#34282=CARTESIAN_POINT ( 'NONE',  ( 119.9518141859119851, -0.8832429491016019485, -18.19431474523657855 ) ) ;
#34285=CARTESIAN_POINT ( 'NONE',  ( 125.1433143116089894, 1.889641906327490073, -10.28863673848242577 ) ) ;
#34300=ORIENTED_EDGE ( 'NONE', *, *, #35612, .F. ) ;
#34313=DIRECTION ( 'NONE',  ( 0.000000000000000000, 0.4669533266896289669, 0.8842819633428518067 ) ) ;
#34360=CARTESIAN_POINT ( 'NONE',  ( 121.6186891859119896, -8.844754642576884152, -8.592115655440050404 ) ) ;
#34367=CARTESIAN_POINT ( 'NONE',  ( 122.0354079359119908, -4.360204210389833968, -8.000047426360245240 ) ) ;
#34376=CARTESIAN_POINT ( 'NONE',  ( 122.6009548109119720, -8.523281198020143279, -6.279169073056789507 ) ) ;
#34384=CARTESIAN_POINT ( 'NONE',  ( 120.0212673109119805, 0.2312338769422704887, -16.08380026872395874 ) ) ;
#34398=CARTESIAN_POINT ( 'NONE',  ( 123.2161110609119561, -3.163656168406935087, -18.89861972220014508 ) ) ;
#34434=CARTESIAN_POINT ( 'NONE',  ( 121.1325173109119788, 0.2312338769422704887, -16.08380026872395874 ) ) ;
#34453=EDGE_CURVE ( 'NONE', #25646, #32564, #20139, .T. ) ;
#34466=DIRECTION ( 'NONE',  ( 1.000000000000000000, 0.000000000000000000, 0.000000000000000000 ) ) ;
#34469=CARTESIAN_POINT ( 'NONE',  ( 119.8129079359119942, -4.360204210389833968, -8.000047426360245240 ) ) ;
#34471=CARTESIAN_POINT ( 'NONE',  ( 122.8688454359119646, 0.5291689781388270175, -13.89700978578772705 ) ) ;
#34497=CARTESIAN_POINT ( 'NONE',  ( 120.4379860609119675, -6.564341423271550902, -7.887810678476487425 ) ) ;
#34501=CARTESIAN_POINT ( 'NONE',  ( 124.9801526047685201, 1.982760200694134056, -10.09727770056924889 ) ) ;
#34507=CARTESIAN_POINT ( 'NONE',  ( 124.7201422582637349, -7.338191648192773364, -20.79841806650483704 ) ) ;
#34556=CARTESIAN_POINT ( 'NONE',  ( 125.4584548109119737, -4.863998795839242995, -13.39321520033831447 ) ) ;
#34565=DIRECTION ( 'NONE',  ( 0.000000000000000000, -0.4669533266896289669, -0.8842819633428519177 ) ) ;
#34581=CARTESIAN_POINT ( 'NONE',  ( 122.0354079359119908, -5.444069387712269226, -19.60292469916370450 ) ) ;
#34586=CARTESIAN_POINT ( 'NONE',  ( 122.0354079359119908, -4.360204210389833968, -8.000047426360245240 ) ) ;
#34594=( NAMED_UNIT ( * ) PLANE_ANGLE_UNIT ( ) SI_UNIT ( $, .RADIAN. ) );
#34600=CARTESIAN_POINT ( 'NONE',  ( 123.9584548109119737, -5.853704621469987934, -5.454671103420249523 ) ) ;
#34610=CARTESIAN_POINT ( 'NONE',  ( 124.5059548109119731, -2.529232162391097827, -8.971805383624054997 ) ) ;
#34613=DIRECTION ( 'NONE',  ( 0.000000000000000000, -0.4669533266896290225, -0.8842819633428516957 ) ) ;
#34618=CARTESIAN_POINT ( 'NONE',  ( 122.0354079359119908, -5.444069387712269226, -19.60292469916370450 ) ) ;
#34654=CARTESIAN_POINT ( 'NONE',  ( 121.2714235609119697, 0.6414057260225851653, -11.69287257290600657 ) ) ;
#34690=CARTESIAN_POINT ( 'NONE',  ( 123.3550173109119612, -9.289237151508434209, -11.05642687123711276 ) ) ;
#34704=CARTESIAN_POINT ( 'NONE',  ( 121.9659548109119811, -2.527210466738041728, -8.967976844669124148 ) ) ;
#34707=EDGE_LOOP ( 'NONE', ( #6472, #4751, #8841, #37875, #13305, #23725, #30650, #9727, #43957, #34059, #44665, #18283, #10682, #8934, #24683 ) ) ;
#34715=CARTESIAN_POINT ( 'NONE',  ( 121.9659548109119811, -2.527210466738041728, -8.967976844669124148 ) ) ;
#34718=CARTESIAN_POINT ( 'NONE',  ( 124.1726284085847851, 0.04950309887738641584, -7.080035182150737683 ) ) ;
#34771=CARTESIAN_POINT ( 'NONE',  ( 119.7434548109119703, -8.245233026025740486, -17.07659070123625611 ) ) ;
#34774=CARTESIAN_POINT ( 'NONE',  ( 124.5966688623432219, -9.713577380183913590, -14.62808432448665563 ) ) ;
#34784=ORIENTED_EDGE ( 'NONE', *, *, #13884, .F. ) ;
#34796=CARTESIAN_POINT ( 'NONE',  ( 122.8688454359119646, -11.07370829466463569, -12.81314460846529002 ) ) ;
#34802=CARTESIAN_POINT ( 'NONE',  ( 123.3550173109119612, -9.289237151508434209, -11.05642687123711276 ) ) ;
#34818=CARTESIAN_POINT ( 'NONE',  ( 120.0907204359119760, 1.345710702986147034, -13.97328579221134426 ) ) ;
#34820=ORIENTED_EDGE ( 'NONE', *, *, #41745, .T. ) ;
#34824=CARTESIAN_POINT ( 'NONE',  ( 124.7570620761208744, -6.011119092344218373, -18.28530538883421386 ) ) ;
#34831=CARTESIAN_POINT ( 'NONE',  ( 120.7157985609119635, -10.36940331770106916, -15.09355782777062061 ) ) ;
#34842=ORIENTED_EDGE ( 'NONE', *, *, #20886, .T. ) ;
#34847=EDGE_CURVE ( 'NONE', #16965, #16241, #27402, .T. ) ;
#34865=ORIENTED_EDGE ( 'NONE', *, *, #37614, .T. ) ;
#34900=CARTESIAN_POINT ( 'NONE',  ( 119.1846548109119794, -7.198765429287387718, -17.81462501705257395 ) ) ;
#34917=EDGE_CURVE ( 'NONE', #11067, #37731, #27146, .T. ) ;
#34929=CARTESIAN_POINT ( 'NONE',  ( 122.8688454359119646, -11.07370829466463569, -12.81314460846529002 ) ) ;
#34932=CARTESIAN_POINT ( 'NONE',  ( 125.0532895624263432, -0.4468654995609705471, -7.300568634099578347 ) ) ;
#34941=CARTESIAN_POINT ( 'NONE',  ( 119.7434548109119987, -3.285100104180844305, -18.74292181979904726 ) ) ;
#34989=CARTESIAN_POINT ( 'NONE',  ( 123.5393205993907486, -9.245649465415468171, -16.16453161350215950 ) ) ;
#34992=CARTESIAN_POINT ( 'NONE',  ( 119.7434548109119703, -4.863998795839242995, -13.39321520033831447 ) ) ;
#35012=CIRCLE ( 'NONE', #19755, 8.000000000000001776 ) ;
#35024=( NAMED_UNIT ( * ) SI_UNIT ( $, .STERADIAN. ) SOLID_ANGLE_UNIT ( ) );
#35049=CARTESIAN_POINT ( 'NONE',  ( 124.7472578386052362, -11.05872435226744344, -8.686341302686004795 ) ) ;
#35052=CARTESIAN_POINT ( 'NONE',  ( 120.6463454359119822, -11.07370829466463569, -12.81314460846529002 ) ) ;
#35054=DIRECTION ( 'NONE',  ( 0.000000000000000000, 0.4669533266896289669, 0.8842819633428518067 ) ) ;
#35071=CARTESIAN_POINT ( 'NONE',  ( 120.4470390828414139, -8.372502050422339082, -17.31760344562335519 ) ) ;
#35080=CARTESIAN_POINT ( 'NONE',  ( 119.7434548109119703, 2.753894863294152007, -15.83610205775420177 ) ) ;
#35106=CARTESIAN_POINT ( 'NONE',  ( 122.8775937114597241, -6.208002839291213881, -18.65814938918611077 ) ) ;
#35158=CARTESIAN_POINT ( 'NONE',  ( 124.5817866277113382, -9.804771881367848607, -14.18055866627750738 ) ) ;
#35160=CARTESIAN_POINT ( 'NONE',  ( 123.9800954359119771, -11.07370829466463569, -12.81314460846529002 ) ) ;
#35164=CARTESIAN_POINT ( 'NONE',  ( 124.9774582099985025, -0.3480505516612068528, -7.274636164916885583 ) ) ;
#35192=B_SPLINE_CURVE_WITH_KNOTS ( 'NONE', 3,
 ( #16257, #43614, #41114, #16484, #30384, #44307, #37439, #6210, #30607, #44524 ),
 .UNSPECIFIED., .F., .F.,
 ( 4, 3, 3, 4 ),
 ( 3.127317220692749988E-18, 0.0002476486808869855175, 0.0004952973797228669853, 0.0009539399846111519445 ),
 .UNSPECIFIED. ) ;
#35193=LINE ( 'NONE', #42743, #3722 ) ;
#35243=CARTESIAN_POINT ( 'NONE',  ( 121.8965016859119856, -9.665098340737509730, -17.37397104707595474 ) ) ;
#35261=CARTESIAN_POINT ( 'NONE',  ( 123.6800462736033239, -5.999693504163852609, -18.26366844790029731 ) ) ;
#35265=CARTESIAN_POINT ( 'NONE',  ( 124.0495485609119584, -10.36940331770106916, -15.09355782777062061 ) ) ;
#35280=CARTESIAN_POINT ( 'NONE',  ( 122.7993923109119692, -9.959231468620755479, -10.70263013195267199 ) ) ;
#35289=EDGE_CURVE ( 'NONE', #33790, #5920, #3444, .T. ) ;
#35292=CARTESIAN_POINT ( 'NONE',  ( 121.7575954359119521, 0.5291689781388270175, -13.89700978578772705 ) ) ;
#35298=CARTESIAN_POINT ( 'NONE',  ( 120.8547048109119686, -7.554583864224885481, -18.48844787311982785 ) ) ;
#35299=CARTESIAN_POINT ( 'NONE',  ( 125.4584548109119737, -7.476587315910852460, -21.06050163197695824 ) ) ;
#35341=DIRECTION ( 'NONE',  ( -1.000000000000000000, 0.000000000000000000, -0.000000000000000000 ) ) ;
#35378=DIRECTION ( 'NONE',  ( 0.000000000000000000, 0.4669533266896293000, 0.8842819633428516957 ) ) ;
#35385=EDGE_CURVE ( 'NONE', #36318, #7179, #8327, .T. ) ;
#35388=EDGE_CURVE ( 'NONE', #2916, #30417, #23020, .T. ) ;
#35391=CARTESIAN_POINT ( 'NONE',  ( 123.7022829359119811, -4.283928203966213211, -7.183505701512925334 ) ) ;
#35394=CARTESIAN_POINT ( 'NONE',  ( 125.1028739313145905, -0.5192815678331393903, -7.317066403780624562 ) ) ;
#35473=CARTESIAN_POINT ( 'NONE',  ( 119.1878298109119783, -7.200787124940443817, -17.81845355600750835 ) ) ;
#35481=ORIENTED_EDGE ( 'NONE', *, *, #25820, .F. ) ;
#35491=ADVANCED_FACE ( 'NONE', ( #2207 ), #5505, .F. ) ;
#35493=CARTESIAN_POINT ( 'NONE',  ( 123.6328298109119714, -2.173413727453600508, -8.297982527556802879 ) ) ;
#35497=CARTESIAN_POINT ( 'NONE',  ( 120.0907204359119760, -10.25716656981731489, -12.88942061488890545 ) ) ;
#35506=CARTESIAN_POINT ( 'NONE',  ( 124.5176775718272069, -9.754195700035083405, -12.35076824631977566 ) ) ;
#35510=CARTESIAN_POINT ( 'NONE',  ( 125.3303382280814020, -10.92430497713086979, -9.659021213111804727 ) ) ;
#35522=CARTESIAN_POINT ( 'NONE',  ( 122.4280705993907645, -9.245649465415468171, -16.16453161350215950 ) ) ;
#35525=APPLICATION_CONTEXT ( 'automotive_design' ) ;
#35562=CARTESIAN_POINT ( 'NONE',  ( 122.6540948253202998, -6.059724811980599313, -18.37735133589800540 ) ) ;
#35568=CARTESIAN_POINT ( 'NONE',  ( 120.2990798109119766, -7.200787124940443817, -17.81845355600750835 ) ) ;
#35585=CARTESIAN_POINT ( 'NONE',  ( 119.8730187714538005, -6.306599966548167124, -18.84486539759072699 ) ) ;
#35602=CARTESIAN_POINT ( 'NONE',  ( 120.5768923109119868, -9.959231468620755479, -10.70263013195267199 ) ) ;
#35606=EDGE_LOOP ( 'NONE', ( #21944, #13259, #19422, #22649 ) ) ;
#35612=EDGE_CURVE ( 'NONE', #2745, #27644, #15613, .T. ) ;
#35617=CARTESIAN_POINT ( 'NONE',  ( 124.5747187774675808, -9.832980137052690139, -13.97121560461364709 ) ) ;
#35619=CARTESIAN_POINT ( 'NONE',  ( 123.6328298109119714, -2.173413727453600508, -8.297982527556802879 ) ) ;
#35620=EDGE_LOOP ( 'NONE', ( #34784, #30008, #30059 ) ) ;
#35642=EDGE_CURVE ( 'NONE', #33098, #26479, #42576, .T. ) ;
#35681=CARTESIAN_POINT ( 'NONE',  ( 119.7434548109119703, -12.49632558250451986, -9.362893955355607645 ) ) ;
#35703=CARTESIAN_POINT ( 'NONE',  ( 121.6186891859119896, -1.406689858478933353, -17.56299727309130887 ) ) ;
#35723=CARTESIAN_POINT ( 'NONE',  ( 122.8688454359119646, -11.07370829466463569, -12.81314460846529002 ) ) ;
#35726=CARTESIAN_POINT ( 'NONE',  ( 119.8823610609119754, -6.340755971794695078, -8.611740276972781771 ) ) ;
#35741=CARTESIAN_POINT ( 'NONE',  ( 125.0048763211397187, -12.00734914858023039, -10.87324543638115237 ) ) ;
#35789=CYLINDRICAL_SURFACE ( 'NONE', #16348, 1.587500000000000355 ) ;
#35826=CARTESIAN_POINT ( 'NONE',  ( 119.8129079359119942, -5.444069387712269226, -19.60292469916370450 ) ) ;
#35840=CARTESIAN_POINT ( 'NONE',  ( 124.5370249113216801, -9.838819348832451794, -12.88702400009979065 ) ) ;
#35842=CARTESIAN_POINT ( 'NONE',  ( 121.0630641859119976, -0.8832429491016019485, -18.19431474523657855 ) ) ;
#35893=CARTESIAN_POINT ( 'NONE',  ( 124.9774582100001510, -5.997229896066199828, -5.873468846220863071 ) ) ;
#35930=CARTESIAN_POINT ( 'NONE',  ( 123.3550173109119612, 0.2312338769422704887, -16.08380026872395874 ) ) ;
#35949=CARTESIAN_POINT ( 'NONE',  ( 120.2296266859119953, -0.06289925094097943703, -9.412459353600674206 ) ) ;
#35953=CARTESIAN_POINT ( 'NONE',  ( 123.7717360609119623, -6.564341423271550902, -7.887810678476487425 ) ) ;
#35962=CARTESIAN_POINT ( 'NONE',  ( 124.5101297936590754, -9.706096323638551127, -12.14509628965581278 ) ) ;
#35978=CARTESIAN_POINT ( 'NONE',  ( 122.1743141859119817, -8.321307733199551748, -9.223433127585318303 ) ) ;
#35982=CARTESIAN_POINT ( 'NONE',  ( 121.2019704359119743, 1.345710702986147034, -13.97328579221134426 ) ) ;
#35983=CARTESIAN_POINT ( 'NONE',  ( 123.0077516859119839, -9.665098340737509730, -17.37397104707595474 ) ) ;
#36012=EDGE_CURVE ( 'NONE', #42758, #36318, #31648, .T. ) ;
#36013=DIRECTION ( 'NONE',  ( 0.000000000000000000, -0.4669533266896288004, -0.8842819633428518067 ) ) ;
#36015=CARTESIAN_POINT ( 'NONE',  ( 124.8603923818566273, -1.444759446862402097, -20.30530361472503387 ) ) ;
#36055=CARTESIAN_POINT ( 'NONE',  ( 120.2990798109119766, -2.173413727453600508, -8.297982527556802879 ) ) ;
#36068=CARTESIAN_POINT ( 'NONE',  ( 124.5423633126549561, -9.852374207079853008, -13.03727910468368201 ) ) ;
#36118=CARTESIAN_POINT ( 'NONE',  ( 124.9009360172555034, -8.233366253754685005, -6.504877232558810896 ) ) ;
#36146=CARTESIAN_POINT ( 'NONE',  ( 125.3563494635813242, 1.483268859736976308, -16.45799053132973455 ) ) ;
#36152=CARTESIAN_POINT ( 'NONE',  ( 119.4656423109119743, -0.4387604401700512802, -15.73000352943951619 ) ) ;
#36178=CARTESIAN_POINT ( 'NONE',  ( 123.7022829359119811, -4.283928203966213211, -7.183505701512925334 ) ) ;
#36182=CARTESIAN_POINT ( 'NONE',  ( 122.0046199480702569, -6.365377317481695663, -18.95617363400926081 ) ) ;
#36193=CARTESIAN_POINT ( 'NONE',  ( 125.0874013446012469, -12.26524233522089880, -14.59144684667939629 ) ) ;
#36208=CARTESIAN_POINT ( 'NONE',  ( 120.0212673109119805, 0.2312338769422704887, -16.08380026872395874 ) ) ;
#36213=CARTESIAN_POINT ( 'NONE',  ( 123.8411891859119862, -8.844754642576884152, -8.592115655440050404 ) ) ;
#36244=CARTESIAN_POINT ( 'NONE',  ( 125.3334400860417759, -2.410057117798671822, -20.05515415193855944 ) ) ;
#36247=CARTESIAN_POINT ( 'NONE',  ( 121.0630641859119976, -8.321307733199551748, -9.223433127585318303 ) ) ;
#36280=CARTESIAN_POINT ( 'NONE',  ( 123.3550173109119612, -9.289237151508434209, -11.05642687123711276 ) ) ;
#36289=EDGE_LOOP ( 'NONE', ( #2736, #9797, #38976, #457, #16518, #38504, #23012, #38408, #29238, #15863, #5122, #24833, #22489, #4657, #22160, #36495, #28063, #31860, #38415, #1136 ) ) ;
#36318=VERTEX_POINT ( 'NONE', #16012 ) ;
#36362=DIRECTION ( 'NONE',  ( 0.000000000000000000, -0.4669533266896288559, -0.8842819633428518067 ) ) ;
#36369=CARTESIAN_POINT ( 'NONE',  ( 125.0480389746926022, 1.230434822596612188, -17.81742975626465153 ) ) ;
#36405=CARTESIAN_POINT ( 'NONE',  ( 124.5063586819718324, -9.678300144053231691, -12.04321394670371603 ) ) ;
#36409=CARTESIAN_POINT ( 'NONE',  ( 121.9272896737536911, -8.611453504372539314, -17.77011218421760574 ) ) ;
#36411=CARTESIAN_POINT ( 'NONE',  ( 119.7434548109119703, -4.863998795839242995, -13.39321520033831447 ) ) ;
#36413=B_SPLINE_CURVE_WITH_KNOTS ( 'NONE', 3,
 ( #13902, #3189, #3414, #41725, #42392, #24390, #38494, #27811, #7058, #21635 ),
 .UNSPECIFIED., .F., .F.,
 ( 4, 3, 3, 4 ),
 ( 1.939479807224430197E-18, 0.0002476486808869839996, 0.0004952973797228669853, 0.0009539399846111490172 ),
 .UNSPECIFIED. ) ;
#36415=ADVANCED_FACE ( 'NONE', ( #34227 ), #33536, .F. ) ;
#36429=CARTESIAN_POINT ( 'NONE',  ( 120.6463454359119822, -11.07370829466463569, -12.81314460846529002 ) ) ;
#36434=CARTESIAN_POINT ( 'NONE',  ( 122.3132204359119868, 1.345710702986147034, -13.97328579221134426 ) ) ;
#36435=CARTESIAN_POINT ( 'NONE',  ( 123.1466579359119891, -5.444069387712269226, -19.60292469916370450 ) ) ;
#36445=CARTESIAN_POINT ( 'NONE',  ( 119.7434548109119703, -11.17722486020181627, -8.479644537342501565 ) ) ;
#36456=EDGE_CURVE ( 'NONE', #38956, #11695, #27632, .T. ) ;
#36471=CARTESIAN_POINT ( 'NONE',  ( 125.1602731999475537, -1.814607927093800255, -20.13360068303625283 ) ) ;
#36495=ORIENTED_EDGE ( 'NONE', *, *, #13684, .F. ) ;
#36496=CARTESIAN_POINT ( 'NONE',  ( 122.4767535264548854, -8.247323210606174015, -17.08054893949881858 ) ) ;
#36505=CARTESIAN_POINT ( 'NONE',  ( 120.4379860609119675, -6.564341423271550902, -7.887810678476487425 ) ) ;
#36543=LINE ( 'NONE', #22871, #6086 ) ;
#36569=CARTESIAN_POINT ( 'NONE',  ( 121.0630641859119976, -8.321307733199551748, -9.223433127585318303 ) ) ;
#36609=CARTESIAN_POINT ( 'NONE',  ( 124.6894688159050872, -8.253847584685239269, -17.09290432062678278 ) ) ;
#36619=AXIS2_PLACEMENT_3D ( 'NONE', #12259, #40059, #22725 ) ;
#36636=CARTESIAN_POINT ( 'NONE',  ( 125.4584548109119737, -5.999156839134895947, -18.26265215102791473 ) ) ;
#36638=CARTESIAN_POINT ( 'NONE',  ( 125.3447737754104736, -11.69827971232593455, -15.21530341384118401 ) ) ;
#36657=CARTESIAN_POINT ( 'NONE',  ( 123.2855641859119942, -0.8832429491016019485, -18.19431474523657855 ) ) ;
#36658=CARTESIAN_POINT ( 'NONE',  ( 121.9659548109119811, -7.554583864224885481, -18.48844787311982785 ) ) ;
#36681=CARTESIAN_POINT ( 'NONE',  ( 120.2023751563572347, -9.242038528452065194, -16.16155152458310695 ) ) ;
#36687=CARTESIAN_POINT ( 'NONE',  ( 125.3194757386390847, -2.314088454569425135, -20.05232376479858658 ) ) ;
#36690=CARTESIAN_POINT ( 'NONE',  ( 123.2161110609119703, -6.340755971794695078, -8.611740276972781771 ) ) ;
#36706=CARTESIAN_POINT ( 'NONE',  ( 124.5966688623432219, -9.713577380183913590, -14.62808432448665563 ) ) ;
#36730=CARTESIAN_POINT ( 'NONE',  ( 120.7852516859119731, -0.6942167230862511529, -9.935906262978006609 ) ) ;
#36789=CARTESIAN_POINT ( 'NONE',  ( 125.0048763211383829, -8.133222562175093984, -6.560216017044333547 ) ) ;
#36793=CARTESIAN_POINT ( 'NONE',  ( 120.7852516859119731, -0.6942167230862511529, -9.935906262978006609 ) ) ;
#36836=EDGE_CURVE ( 'NONE', #17122, #25324, #8810, .T. ) ;
#36846=DIRECTION ( 'NONE',  ( 1.000000000000000000, 0.000000000000000000, 0.000000000000000000 ) ) ;
#36852=CARTESIAN_POINT ( 'NONE',  ( 124.6574308310811858, 2.898587707825708293, -12.35876450466414056 ) ) ;
#36859=CARTESIAN_POINT ( 'NONE',  ( 125.3513934876002764, -11.54857932371512419, -15.65469058310272210 ) ) ;
#36862=CARTESIAN_POINT ( 'NONE',  ( 119.7434548109119561, -1.843432898259047992, -17.99896722079169464 ) ) ;
#36863=EDGE_LOOP ( 'NONE', ( #43905, #11404, #34300, #11244, #16710, #23930, #32437 ) ) ;
#36880=CARTESIAN_POINT ( 'NONE',  ( 120.5768923109119868, -0.4387604401700512802, -15.73000352943951619 ) ) ;
#36881=CARTESIAN_POINT ( 'NONE',  ( 122.4521266859119635, -0.06289925094097943703, -9.412459353600674206 ) ) ;
#36911=CARTESIAN_POINT ( 'NONE',  ( 125.0488419420234010, -3.685100071787774212, -20.83256261096772732 ) ) ;
#36914=CARTESIAN_POINT ( 'NONE',  ( 124.1190016859119680, -0.6942167230862511529, -9.935906262978006609 ) ) ;
#36927=ORIENTED_EDGE ( 'NONE', *, *, #33064, .T. ) ;
#36937=ORIENTED_EDGE ( 'NONE', *, *, #41745, .F. ) ;
#36951=CARTESIAN_POINT ( 'NONE',  ( 119.7434548109119703, -7.554583864224885481, -18.48844787311982785 ) ) ;
#36985=CARTESIAN_POINT ( 'NONE',  ( 123.6776560953690591, -6.001247023715324147, -18.26661038929047010 ) ) ;
#36986=CARTESIAN_POINT ( 'NONE',  ( 120.7026895652850556, -6.239497348973052304, -18.71779138178827040 ) ) ;
#36987=CARTESIAN_POINT ( 'NONE',  ( 120.2990798109119766, -7.200787124940443817, -17.81845355600750835 ) ) ;
#37005=VERTEX_POINT ( 'NONE', #25771 ) ;
#37017=EDGE_CURVE ( 'NONE', #7972, #24335, #9843, .T. ) ;
#37024=CARTESIAN_POINT ( 'NONE',  ( 123.9584548109119737, -7.429215134363809092, -20.97079166887802160 ) ) ;
#37025=ADVANCED_FACE ( 'NONE', ( #19827 ), #30762, .F. ) ;
#37042=CARTESIAN_POINT ( 'NONE',  ( 125.0660727672603372, 1.224322542308768247, -17.79270567365541567 ) ) ;
#37071=CARTESIAN_POINT ( 'NONE',  ( 122.4521266859119635, -9.033780868592240054, -16.85052413769862056 ) ) ;
#37075=CARTESIAN_POINT ( 'NONE',  ( 122.7299391859119737, -8.844754642576873493, -8.592115655440052180 ) ) ;
#37086=ADVANCED_FACE ( 'NONE', ( #3173 ), #20731, .F. ) ;
#37103=CARTESIAN_POINT ( 'NONE',  ( 119.1878298109119783, -7.200787124940443817, -17.81845355600750835 ) ) ;
#37104=CARTESIAN_POINT ( 'NONE',  ( 121.5492360609119800, -3.387241619883791355, -18.17469012370385073 ) ) ;
#37105=B_SPLINE_CURVE_WITH_KNOTS ( 'NONE', 3,
 ( #32816, #43553, #40130, #8895, #36471, #23254, #19834, #33721, #22568, #22793, #43328, #40586, #12547, #22350, #36687, #2491, #40356, #5457, #36244, #1586, #9345, #12096, #12773, #9120, #5682, #19376, #2038, #33265, #29189, #43101, #26001, #5238, #5011, #15963, #29866, #43782, #23022, #36911, #12321, #18928, #19154, #15507, #11871, #15736, #25775, #39682, #19601, #26674, #37138 ),
 .UNSPECIFIED., .F., .F.,
 ( 4, 2, 2, 1, 2, 2, 2, 2, 1, 2, 2, 2, 2, 2, 2, 2, 1, 2, 2, 2, 2, 2, 2, 2, 2, 4 ),
 ( 0.000000000000000000, 0.06250000000003677614, 0.09375000000004964085, 0.1093750000000515560, 0.1171875000000521388, 0.1250000000000527078, 0.1875000000000492106, 0.2187500000000477396, 0.2343750000000468792, 0.2421875000000479616, 0.2500000000000490719, 0.3125000000000444089, 0.3437500000000421330, 0.3750000000000398015, 0.4375000000000360822, 0.4687500000000349720, 0.4843750000000360267, 0.4921875000000336398, 0.5000000000000311973, 0.6250000000000193179, 0.6875000000000134337, 0.7187500000000103251, 0.7500000000000073275, 0.8125000000000028866, 0.8749999999999984457, 1.000000000000000000 ),
 .UNSPECIFIED. ) ;
#37136=AXIS2_PLACEMENT_3D ( 'NONE', #29409, #43321, #29633 ) ;
#37138=CARTESIAN_POINT ( 'NONE',  ( 123.9584548109119737, -3.874292970208447873, -21.33175929725637587 ) ) ;
#37141=CARTESIAN_POINT ( 'NONE',  ( 124.2579079359120016, -4.360204210389833968, -8.000047426360245240 ) ) ;
#37178=CARTESIAN_POINT ( 'NONE',  ( 123.9800954359119771, 0.5291689781388270175, -13.89700978578772705 ) ) ;
#37183=ORIENTED_EDGE ( 'NONE', *, *, #15266, .F. ) ;
#37217=CARTESIAN_POINT ( 'NONE',  ( 123.4244704359119709, -10.25716656981731489, -12.88942061488890545 ) ) ;
#37235=DIRECTION ( 'NONE',  ( -1.000000000000000000, 0.000000000000000000, -0.000000000000000000 ) ) ;
#37243=CARTESIAN_POINT ( 'NONE',  ( 123.0077516859119839, -0.6942167230862511529, -9.935906262978006609 ) ) ;
#37276=CARTESIAN_POINT ( 'NONE',  ( 120.1601735609119856, -9.645473719204776586, -14.86997237629376656 ) ) ;
#37298=ADVANCED_FACE ( 'NONE', ( #7253 ), #18430, .T. ) ;
#37319=CARTESIAN_POINT ( 'NONE',  ( 119.7434548109119561, -0.5813642816343631559, -16.73924225410030431 ) ) ;
#37331=CARTESIAN_POINT ( 'NONE',  ( 124.8533330496100859, -12.49533689344159981, -14.47573569507178171 ) ) ;
#37340=CARTESIAN_POINT ( 'NONE',  ( 119.3961891859119930, -1.406689858478933353, -17.56299727309130887 ) ) ;
#37341=CARTESIAN_POINT ( 'NONE',  ( 121.7575954359119805, 0.5291689781388270175, -13.89700978578772705 ) ) ;
#37359=EDGE_CURVE ( 'NONE', #17793, #42758, #22697, .T. ) ;
#37376=DIRECTION ( 'NONE',  ( -1.000000000000000000, 0.000000000000000000, -0.000000000000000000 ) ) ;
#37379=CARTESIAN_POINT ( 'NONE',  ( 123.4939235609119663, -9.645473719204776586, -14.86997237629376656 ) ) ;
#37398=STYLED_ITEM('',(#45190),#21657);
#37418=CARTESIAN_POINT ( 'NONE',  ( 121.2714235609119697, -9.645473719204776586, -14.86997237629376656 ) ) ;
#37439=CARTESIAN_POINT ( 'NONE',  ( 121.1018636130535384, -8.422568683347405383, -17.41241596312870854 ) ) ;
#37478=( BOUNDED_CURVE ( )  B_SPLINE_CURVE ( 2, ( #13401, #6319, #19775, #27303, #23889, #17046, #34123, #12946, #41442, #44406, #38649, #18379, #42547, #21566, #38434, #34989, #6994 ),
 .UNSPECIFIED., .F., .T. ) 
 B_SPLINE_CURVE_WITH_KNOTS ( ( 3, 2, 2, 2, 2, 2, 2, 2, 3 ),
 ( 0.7602707595410509445, 0.7812500000000000000, 0.8125000000000000000, 0.8437500000000000000, 0.8750000000000000000, 0.9062500000000000000, 0.9375000000000000000, 0.9687500000000000000, 0.9897292404589489445 ),
 .UNSPECIFIED. ) 
 CURVE ( )  GEOMETRIC_REPRESENTATION_ITEM ( )  RATIONAL_B_SPLINE_CURVE ( ( 0.9664089390052280626, 0.9488976130786129781, 1.000000000000000000, 0.9238795325112869605, 1.000000000000000000, 0.9238795325112869605, 1.000000000000000000, 0.9238795325112869605, 1.000000000000000000, 0.9238795325112869605, 1.000000000000000000, 0.9238795325112869605, 1.000000000000000000, 0.9238795325112869605, 1.000000000000000000, 0.9488976130786129781, 0.9664089390052290618 ) ) 
 REPRESENTATION_ITEM ( '' )  );
#37480=CARTESIAN_POINT ( 'NONE',  ( 124.0495485609119584, -0.08252387247370887580, -11.91645802438286417 ) ) ;
#37483=AXIS2_PLACEMENT_3D ( 'NONE', #41272, #10249, #13222 ) ;
#37485=DIRECTION ( 'NONE',  ( -1.000000000000000000, 0.000000000000000000, -0.000000000000000000 ) ) ;
#37489=ORIENTED_EDGE ( 'NONE', *, *, #27729, .F. ) ;
#37515=CARTESIAN_POINT ( 'NONE',  ( 120.8160396737536928, -8.611453504372539314, -17.77011218421760574 ) ) ;
#37547=CARTESIAN_POINT ( 'NONE',  ( 125.4584548109119737, -4.863998795839242995, -13.39321520033831447 ) ) ;
#37548=CARTESIAN_POINT ( 'NONE',  ( 124.3999891859119913, -8.318316608003341273, -9.227040655997777563 ) ) ;
#37554=CARTESIAN_POINT ( 'NONE',  ( 122.2131136130535367, -8.422568683347400054, -17.41241596312869788 ) ) ;
#37564=CARTESIAN_POINT ( 'NONE',  ( 124.3454436379668380, -12.76346192841408467, -14.38917066012018431 ) ) ;
#37574=CARTESIAN_POINT ( 'NONE',  ( 121.2714235609119697, -9.645473719204776586, -14.86997237629376656 ) ) ;
#37575=CARTESIAN_POINT ( 'NONE',  ( 119.3267360609119692, -3.387241619883791355, -18.17469012370385073 ) ) ;
#37599=ORIENTED_EDGE ( 'NONE', *, *, #34917, .T. ) ;
#37610=CARTESIAN_POINT ( 'NONE',  ( 119.8823610609119754, -3.163656168406935087, -18.89861972220014508 ) ) ;
#37614=EDGE_CURVE ( 'NONE', #7363, #4044, #24783, .T. ) ;
#37648=CARTESIAN_POINT ( 'NONE',  ( 123.0077516859119839, -0.6942167230862511529, -9.935906262978006609 ) ) ;
#37679=ORIENTED_EDGE ( 'NONE', *, *, #11844, .F. ) ;
#37686=CARTESIAN_POINT ( 'NONE',  ( 119.8097329359119811, -4.360640073283683193, -8.004713379073654878 ) ) ;
#37713=CARTESIAN_POINT ( 'NONE',  ( 123.0772048109119652, -2.527210466738041728, -8.967976844669124148 ) ) ;
#37716=CARTESIAN_POINT ( 'NONE',  ( 125.3566265649645715, 1.939509583157688954, -11.55384643022778945 ) ) ;
#37731=VERTEX_POINT ( 'NONE', #17916 ) ;
#37740=CARTESIAN_POINT ( 'NONE',  ( 120.2055705993907679, -9.245649465415469948, -16.16453161350215240 ) ) ;
#37769=CARTESIAN_POINT ( 'NONE',  ( 121.6547847346423055, -8.435056900666539903, -17.43606523319152757 ) ) ;
#37789=CARTESIAN_POINT ( 'NONE',  ( 119.8823610609119754, -3.163656168406935087, -18.89861972220014508 ) ) ;
#37791=ORIENTED_EDGE ( 'NONE', *, *, #9156, .F. ) ;
#37795=CARTESIAN_POINT ( 'NONE',  ( 120.2296266859119953, -9.033780868592240054, -16.85052413769862056 ) ) ;
#37810=ORIENTED_EDGE ( 'NONE', *, *, #4687, .T. ) ;
#37827=CARTESIAN_POINT ( 'NONE',  ( 120.9936110609119737, -3.163656168406935087, -18.89861972220014508 ) ) ;
#37867=CARTESIAN_POINT ( 'NONE',  ( 123.4939235609119663, 0.6414057260225851653, -11.69287257290600657 ) ) ;
#37869=ADVANCED_FACE ( 'NONE', ( #38209 ), #14494, .T. ) ;
#37875=ORIENTED_EDGE ( 'NONE', *, *, #15813, .T. ) ;
#37890=ORIENTED_EDGE ( 'NONE', *, *, #3188, .T. ) ;
#37905=CARTESIAN_POINT ( 'NONE',  ( 120.0212673109119805, -9.289237151508434209, -11.05642687123711276 ) ) ;
#37907=CARTESIAN_POINT ( 'NONE',  ( 123.2161110609119703, -6.340755971794695078, -8.611740276972781771 ) ) ;
#37923=CARTESIAN_POINT ( 'NONE',  ( 121.6186891859119896, -1.406689858478933353, -17.56299727309130887 ) ) ;
#37925=CARTESIAN_POINT ( 'NONE',  ( 121.3655035264548872, -8.247323210606168686, -17.08054893949881148 ) ) ;
#37936=CARTESIAN_POINT ( 'NONE',  ( 120.2990798109119766, -2.173413727453600508, -8.297982527556802879 ) ) ;
#38001=VECTOR ( 'NONE', #4741, 1000.000000000000000 ) ;
#38004=DIRECTION ( 'NONE',  ( 1.000000000000000000, 0.000000000000000000, 0.000000000000000000 ) ) ;
#38018=CARTESIAN_POINT ( 'NONE',  ( 122.2437673109119629, 0.2312338769422704887, -16.08380026872395874 ) ) ;
#38046=DIRECTION ( 'NONE',  ( 0.000000000000000000, 0.9554676365605390131, 0.2950959089608289343 ) ) ;
#38055=CARTESIAN_POINT ( 'NONE',  ( 121.8270485609119760, -10.36940331770106916, -15.09355782777062061 ) ) ;
#38070=LINE ( 'NONE', #38284, #22663 ) ;
#38090=CARTESIAN_POINT ( 'NONE',  ( 120.8547048109119686, -7.554583864224885481, -18.48844787311982785 ) ) ;
#38110=EDGE_LOOP ( 'NONE', ( #3021, #28647, #6406, #13159, #44803 ) ) ;
#38143=CARTESIAN_POINT ( 'NONE',  ( 121.8270485609119760, -0.08252387247370887580, -11.91645802438286417 ) ) ;
#38147=CYLINDRICAL_SURFACE ( 'NONE', #44233, 1.587500000000000577 ) ;
#38148=TOROIDAL_SURFACE ( 'NONE', #6126, 6.500000000000000000, 1.500000000000000000 ) ;
#38154=CARTESIAN_POINT ( 'NONE',  ( 124.6746266859119743, -9.033780868592240054, -16.85052413769862056 ) ) ;
#38157=CARTESIAN_POINT ( 'NONE',  ( 125.0048763211386245, 1.969000387454901801, -10.12399143400218904 ) ) ;
#38209=FACE_OUTER_BOUND ( 'NONE', #41432, .T. ) ;
#38210=CARTESIAN_POINT ( 'NONE',  ( 121.5100746589382226, -8.341213398351550623, -17.25835129106723542 ) ) ;
#38217=CARTESIAN_POINT ( 'NONE',  ( 124.4662673109119879, -9.289237151508565660, -11.05642687123736145 ) ) ;
#38231=CARTESIAN_POINT ( 'NONE',  ( 122.6604860609119640, -6.564341423271550902, -7.887810678476487425 ) ) ;
#38244=FILL_AREA_STYLE_COLOUR ( '', #23535 ) ;
#38252=CARTESIAN_POINT ( 'NONE',  ( 120.7852516859119731, -9.665098340737509730, -17.37397104707595474 ) ) ;
#38267=CARTESIAN_POINT ( 'NONE',  ( 123.6328298109119714, -2.173413727453600508, -8.297982527556802879 ) ) ;
#38269=CARTESIAN_POINT ( 'NONE',  ( 119.7434548109119703, -2.421111938423274879, -5.775321541204940345 ) ) ;
#38271=VERTEX_POINT ( 'NONE', #13945 ) ;
#38284=CARTESIAN_POINT ( 'NONE',  ( 125.4584548109119737, -2.529232162391097827, -8.971805383624054997 ) ) ;
#38287=DIRECTION ( 'NONE',  ( 0.000000000000000000, -0.4669533266896274681, -0.8842819633428525838 ) ) ;
#38290=DIRECTION ( 'NONE',  ( 0.000000000000000000, 0.4669533266896293000, 0.8842819633428516957 ) ) ;
#38368=CARTESIAN_POINT ( 'NONE',  ( 120.7852516859119731, -9.665098340737509730, -17.37397104707595474 ) ) ;
#38371=CARTESIAN_POINT ( 'NONE',  ( 119.7434548109119845, -2.534040247545263469, -8.964764792708688645 ) ) ;
#38408=ORIENTED_EDGE ( 'NONE', *, *, #44365, .F. ) ;
#38415=ORIENTED_EDGE ( 'NONE', *, *, #34847, .F. ) ;
#38434=CARTESIAN_POINT ( 'NONE',  ( 123.4939235609119663, -9.645473719204776586, -14.86997237629375590 ) ) ;
#38440=CARTESIAN_POINT ( 'NONE',  ( 122.1179700565388941, -8.485573535863895955, -17.53172993199661178 ) ) ;
#38451=CARTESIAN_POINT ( 'NONE',  ( 120.5768923109119868, -9.959231468620755479, -10.70263013195267199 ) ) ;
#38477=( BOUNDED_SURFACE ( )  B_SPLINE_SURFACE ( 1, 2, ( 
 ( #19029, #1692, #26097, #40002, #22899, #2135, #22673, #36793, #5562, #16065, #40467, #36569, #5346, #23136, #10359, #3276, #10579, #23826, #6014, #19938, #9677, #33825, #30649, #2596, #34715, #6711, #27005, #6928, #27237, #3499, #17199, #44567, #20836, #30874, #16526, #45017, #41152, #44344, #30425, #37243, #37713, #13103, #40926, #27686, #17416, #31307, #2825, #24265, #3054, #9913, #80, #13993, #27462, #23595, #37480, #16753, #31091, #41821, #10138, #13333, #6254, #20174, #27909, #38154, #34058 ),
 ( #6483, #20398, #13552, #34282, #16980, #44793, #41383, #24043, #37936, #20620, #34497, #13775, #41600, #39280, #8045, #38368, #14663, #21950, #38584, #35842, #38819, #14439, #4614, #7589, #14215, #741, #7824, #7141, #975, #18084, #42486, #31977, #1201, #29022, #21277, #31758, #31532, #4166, #28579, #21731, #28347, #24924, #42711, #21052, #11024, #34929, #21503, #42259, #15115, #3716, #14891, #17636, #28131, #11248, #25157, #39053, #35619, #35391, #303, #528, #4392, #35160, #18309, #32203, #42039 ) ),
 .UNSPECIFIED., .F., .F., .F. ) 
 B_SPLINE_SURFACE_WITH_KNOTS ( ( 2, 2 ),
 ( 3, 2, 2, 2, 2, 2, 2, 2, 2, 2, 2, 2, 2, 2, 2, 2, 2, 2, 2, 2, 2, 2, 2, 2, 2, 2, 2, 2, 2, 2, 2, 2, 3 ),
 ( 0.000000000000000000, 1.000000000000000000 ),
 ( 0.000000000000000000, 0.03125000000000000000, 0.06250000000000000000, 0.09375000000000000000, 0.1250000000000000000, 0.1562500000000000000, 0.1875000000000000000, 0.2187500000000000000, 0.2500000000000000000, 0.2812500000000000000, 0.3125000000000000000, 0.3437500000000000000, 0.3750000000000000000, 0.4062500000000000000, 0.4375000000000000000, 0.4687500000000000000, 0.5000000000000000000, 0.5312500000000000000, 0.5625000000000000000, 0.5937500000000000000, 0.6250000000000000000, 0.6562500000000000000, 0.6875000000000000000, 0.7187500000000000000, 0.7500000000000000000, 0.7812500000000000000, 0.8125000000000000000, 0.8437500000000000000, 0.8750000000000000000, 0.9062500000000000000, 0.9375000000000000000, 0.9687500000000000000, 1.000000000000000000 ),
 .UNSPECIFIED. ) 
 GEOMETRIC_REPRESENTATION_ITEM ( )  RATIONAL_B_SPLINE_SURFACE ( (
 ( 1.000000000000000000, 0.9238795325112869605, 1.000000000000000000, 0.9238795325112869605, 1.000000000000000000, 0.9238795325112869605, 1.000000000000000000, 0.9238795325112869605, 1.000000000000000000, 0.9238795325112869605, 1.000000000000000000, 0.9238795325112869605, 1.000000000000000000, 0.9238795325112869605, 1.000000000000000000, 0.9238795325112869605, 1.000000000000000000, 0.9238795325112869605, 1.000000000000000000, 0.9238795325112869605, 1.000000000000000000, 0.9238795325112869605, 1.000000000000000000, 0.9238795325112869605, 1.000000000000000000, 0.9238795325112869605, 1.000000000000000000, 0.9238795325112869605, 1.000000000000000000, 0.9238795325112869605, 1.000000000000000000, 0.9238795325112869605, 1.000000000000000000, 0.9238795325112869605, 1.000000000000000000, 0.9238795325112869605, 1.000000000000000000, 0.9238795325112869605, 1.000000000000000000, 0.9238795325112869605, 1.000000000000000000, 0.9238795325112869605, 1.000000000000000000, 0.9238795325112869605, 1.000000000000000000, 0.9238795325112869605, 1.000000000000000000, 0.9238795325112869605, 1.000000000000000000, 0.9238795325112869605, 1.000000000000000000, 0.9238795325112869605, 1.000000000000000000, 0.9238795325112869605, 1.000000000000000000, 0.9238795325112869605, 1.000000000000000000, 0.9238795325112869605, 1.000000000000000000, 0.9238795325112869605, 1.000000000000000000, 0.9238795325112869605, 1.000000000000000000, 0.9238795325112869605, 1.000000000000000000),
 ( 1.000000000000000000, 0.9238795325112869605, 1.000000000000000000, 0.9238795325112869605, 1.000000000000000000, 0.9238795325112869605, 1.000000000000000000, 0.9238795325112869605, 1.000000000000000000, 0.9238795325112869605, 1.000000000000000000, 0.9238795325112869605, 1.000000000000000000, 0.9238795325112869605, 1.000000000000000000, 0.9238795325112869605, 1.000000000000000000, 0.9238795325112869605, 1.000000000000000000, 0.9238795325112869605, 1.000000000000000000, 0.9238795325112869605, 1.000000000000000000, 0.9238795325112869605, 1.000000000000000000, 0.9238795325112869605, 1.000000000000000000, 0.9238795325112869605, 1.000000000000000000, 0.9238795325112869605, 1.000000000000000000, 0.9238795325112869605, 1.000000000000000000, 0.9238795325112869605, 1.000000000000000000, 0.9238795325112869605, 1.000000000000000000, 0.9238795325112869605, 1.000000000000000000, 0.9238795325112869605, 1.000000000000000000, 0.9238795325112869605, 1.000000000000000000, 0.9238795325112869605, 1.000000000000000000, 0.9238795325112869605, 1.000000000000000000, 0.9238795325112869605, 1.000000000000000000, 0.9238795325112869605, 1.000000000000000000, 0.9238795325112869605, 1.000000000000000000, 0.9238795325112869605, 1.000000000000000000, 0.9238795325112869605, 1.000000000000000000, 0.9238795325112869605, 1.000000000000000000, 0.9238795325112869605, 1.000000000000000000, 0.9238795325112869605, 1.000000000000000000, 0.9238795325112869605, 1.000000000000000000) ) ) 
 REPRESENTATION_ITEM ( '' )  SURFACE ( )  );
#38483=CARTESIAN_POINT ( 'NONE',  ( 125.0660727672602803, -10.95232013398726423, -8.993724727021167098 ) ) ;
#38485=CARTESIAN_POINT ( 'NONE',  ( 123.4244704359119709, 1.345710702986147034, -13.97328579221134426 ) ) ;
#38494=CARTESIAN_POINT ( 'NONE',  ( 123.3243636130535350, -8.422568683347405383, -17.41241596312870854 ) ) ;
#38496=ORIENTED_EDGE ( 'NONE', *, *, #22278, .T. ) ;
#38499=CARTESIAN_POINT ( 'NONE',  ( 125.1063270177812115, -8.332880733164756748, -17.24257150086102897 ) ) ;
#38503=CARTESIAN_POINT ( 'NONE',  ( 124.6050267045123690, -8.310145695945278632, -17.19951755478114563 ) ) ;
#38504=ORIENTED_EDGE ( 'NONE', *, *, #16469, .F. ) ;
#38509=CARTESIAN_POINT ( 'NONE',  ( 125.4584548109119737, -4.863998795839242995, -13.39321520033831447 ) ) ;
#38572=CIRCLE ( 'NONE', #21104, 8.000000000000001776 ) ;
#38583=CARTESIAN_POINT ( 'NONE',  ( 124.5767528389142029, -9.826152869829959613, -14.03118282328476596 ) ) ;
#38584=CARTESIAN_POINT ( 'NONE',  ( 120.9936110609119737, -3.163656168406935087, -18.89861972220014508 ) ) ;
#38587=CARTESIAN_POINT ( 'NONE',  ( 124.3692356341917105, -2.419758938359494849, -5.831664186524730731 ) ) ;
#38612=CARTESIAN_POINT ( 'NONE',  ( 121.9568993241987300, -6.333924026435813204, -18.89660969823682279 ) ) ;
#38644=EDGE_CURVE ( 'NONE', #25324, #32403, #37105, .T. ) ;
#38649=CARTESIAN_POINT ( 'NONE',  ( 123.2161110609119703, -6.340755971794695078, -8.611740276972781771 ) ) ;
#38657=ORIENTED_EDGE ( 'NONE', *, *, #43179, .T. ) ;
#38675=EDGE_CURVE ( 'NONE', #31995, #13929, #22422, .T. ) ;
#38688=( LENGTH_UNIT ( ) NAMED_UNIT ( * ) SI_UNIT ( .MILLI., .METRE. ) );
#38697=CARTESIAN_POINT ( 'NONE',  ( 123.0077516859119839, -9.665098340737509730, -17.37397104707595474 ) ) ;
#38705=CARTESIAN_POINT ( 'NONE',  ( 124.2610829359119862, -4.360640073283670759, -8.004713379073534085 ) ) ;
#38712=CARTESIAN_POINT ( 'NONE',  ( 122.5215798109119874, -2.173413727453600508, -8.297982527556802879 ) ) ;
#38715=DIRECTION ( 'NONE',  ( -1.000000000000000000, 0.000000000000000000, -0.000000000000000000 ) ) ;
#38727=CARTESIAN_POINT ( 'NONE',  ( 120.5768923109119868, -9.959231468620755479, -10.70263013195267199 ) ) ;
#38743=ADVANCED_FACE ( 'NONE', ( #30767 ), #7046, .F. ) ;
#38750=SHAPE_REPRESENTATION ( 'Adjuster Locknut', ( #12375 ), #32226 ) ;
#38761=MECHANICAL_DESIGN_GEOMETRIC_PRESENTATION_REPRESENTATION('',(#13317),#29344);
#38764=CARTESIAN_POINT ( 'NONE',  ( 122.9251895652850521, -6.239497348973043422, -18.71779138178828106 ) ) ;
#38801=UNCERTAINTY_MEASURE_WITH_UNIT (LENGTH_MEASURE( 1.000000000000000082E-05 ), #15721, 'distance_accuracy_value', 'NONE');
#38805=AXIS2_PLACEMENT_3D ( 'NONE', #27742, #42315, #136 ) ;
#38806=CARTESIAN_POINT ( 'NONE',  ( 121.2714235609119697, -9.645473719204776586, -14.86997237629376656 ) ) ;
#38819=CARTESIAN_POINT ( 'NONE',  ( 121.1325173109119788, 0.2312338769422704887, -16.08380026872395874 ) ) ;
#38830=ORIENTED_EDGE ( 'NONE', *, *, #6443, .T. ) ;
#38839=CARTESIAN_POINT ( 'NONE',  ( 123.9584548109119737, -11.17722486020181627, -8.479644537342501565 ) ) ;
#38857=CYLINDRICAL_SURFACE ( 'NONE', #59, 5.000000000000000888 ) ;
#38901=CARTESIAN_POINT ( 'NONE',  ( 123.9800954359119771, -11.07370829466463569, -12.81314460846529002 ) ) ;
#38921=CARTESIAN_POINT ( 'NONE',  ( 123.6781775979231384, -6.000908072660331882, -18.26596850864147470 ) ) ;
#38924=CARTESIAN_POINT ( 'NONE',  ( 121.8270485609119760, -10.36940331770106916, -15.09355782777062061 ) ) ;
#38956=VERTEX_POINT ( 'NONE', #10918 ) ;
#38961=CARTESIAN_POINT ( 'NONE',  ( 120.3506102343419428, -8.309924745830986836, -17.19909913565936321 ) ) ;
#38976=ORIENTED_EDGE ( 'NONE', *, *, #38644, .F. ) ;
#38994=EDGE_CURVE ( 'NONE', #22801, #7584, #1646, .T. ) ;
#38998=B_SPLINE_CURVE_WITH_KNOTS ( 'NONE', 3,
 ( #8128, #22030, #15869, #15641, #12452, #5372, #19289, #33616, #43233, #5812, #2393, #29545, #16322, #33168, #22251, #32721, #2162, #36146, #26124, #9027, #26578, #23161, #1944, #9253, #5587, #22700, #37042, #19510, #36369, #33388, #16089, #11999, #29994, #43462, #29767, #25902 ),
 .UNSPECIFIED., .F., .F.,
 ( 4, 2, 2, 2, 2, 1, 2, 2, 2, 2, 2, 2, 2, 1, 2, 2, 2, 2, 4 ),
 ( 0.000000000000000000, 0.06250000000003873291, 0.1250000000000774658, 0.1875000000001161848, 0.2187500000001320610, 0.2343750000001399159, 0.2421875000001464662, 0.2500000000001529887, 0.3750000000000988098, 0.5000000000000446310, 0.6249999999999905631, 0.6874999999999634737, 0.7187499999999548139, 0.7343749999999514833, 0.7421874999999552580, 0.7499999999999589217, 0.8124999999999692468, 0.8749999999999795719, 1.000000000000000000 ),
 .UNSPECIFIED. ) ;
#39005=CARTESIAN_POINT ( 'NONE',  ( 123.9584548109119737, -4.863998795839242995, -13.39321520033831447 ) ) ;
#39036=CARTESIAN_POINT ( 'NONE',  ( 120.5074391859119913, -8.844754642576884152, -8.592115655440050404 ) ) ;
#39051=CARTESIAN_POINT ( 'NONE',  ( 124.5497899996740614, -9.862906267826742734, -13.24824213233555170 ) ) ;
#39053=CARTESIAN_POINT ( 'NONE',  ( 123.5633766859119760, -0.06289925094097943703, -9.412459353600674206 ) ) ;
#39056=CARTESIAN_POINT ( 'NONE',  ( 119.7434548109119845, -2.537457910315239040, -8.963164679308437854 ) ) ;
#39109=EDGE_CURVE ( 'NONE', #38271, #43772, #9842, .T. ) ;
#39113=DIRECTION ( 'NONE',  ( -1.000000000000000000, 0.000000000000000000, -0.000000000000000000 ) ) ;
#39118=CARTESIAN_POINT ( 'NONE',  ( 123.9584548109119737, 1.449227268523328505, -18.30678586333412738 ) ) ;
#39135=EDGE_CURVE ( 'NONE', #37731, #17949, #42703, .T. ) ;
#39136=CARTESIAN_POINT ( 'NONE',  ( 120.7157985609119635, -0.08252387247370887580, -11.91645802438286417 ) ) ;
#39155=CARTESIAN_POINT ( 'NONE',  ( 121.6186891859119896, -8.844754642576884152, -8.592115655440050404 ) ) ;
#39158=CARTESIAN_POINT ( 'NONE',  ( 120.5074391859119913, -1.406689858478933353, -17.56299727309130887 ) ) ;
#39167=CARTESIAN_POINT ( 'NONE',  ( 124.5062240513757246, -9.677281838892072940, -12.03958273341976337 ) ) ;
#39171=CARTESIAN_POINT ( 'NONE',  ( 124.9009360172596530, -12.11729186176019013, -10.90492729001751293 ) ) ;
#39206=ADVANCED_FACE ( 'NONE', ( #19327 ), #33213, .F. ) ;
#39211=( BOUNDED_SURFACE ( )  B_SPLINE_SURFACE ( 1, 2, ( 
 ( #23906, #41898, #37789, #17063, #385, #14297, #17283, #9997, #41458, #17942, #24125, #3364, #38451, #10883, #10661, #20480, #3792, #6794, #7439, #30956, #21360, #24781, #27546, #20703, #41680, #17491, #24565, #34360, #3142, #4020, #28434, #35243, #610, #34581, #14521, #44880, #38018, #13635, #10217, #31174, #10440, #24346, #38231, #31389, #7012, #34796, #159, #14075, #14749, #1282, #1055, #43010, #35930, #4697, #19677, #829, #25238, #39368, #14971, #15194, #25908, #38901, #29099, #32727, #7671 ),
 ( #35473, #9200, #18617, #40439, #36152, #8135, #23109, #4920, #21809, #18835, #1501, #28661, #15421, #28883, #32508, #11328, #36987, #11779, #21586, #11557, #39593, #12005, #39136, #25686, #33565, #16271, #29326, #8354, #5756, #22258, #32291, #43240, #7902, #42347, #25007, #35703, #2342, #4478, #22036, #42566, #18165, #11105, #18398, #42795, #4248, #25464, #32062, #41128, #16953, #9652, #12857, #41574, #23798, #34471, #9888, #24019, #23573, #9419, #37907, #30625, #34690, #37217, #5990, #30175, #3478 ) ),
 .UNSPECIFIED., .F., .F., .F. ) 
 B_SPLINE_SURFACE_WITH_KNOTS ( ( 2, 2 ),
 ( 3, 2, 2, 2, 2, 2, 2, 2, 2, 2, 2, 2, 2, 2, 2, 2, 2, 2, 2, 2, 2, 2, 2, 2, 2, 2, 2, 2, 2, 2, 2, 2, 3 ),
 ( 0.000000000000000000, 1.000000000000000000 ),
 ( 0.000000000000000000, 0.03125000000000000000, 0.06250000000000000000, 0.09375000000000000000, 0.1250000000000000000, 0.1562500000000000000, 0.1875000000000000000, 0.2187500000000000000, 0.2500000000000000000, 0.2812500000000000000, 0.3125000000000000000, 0.3437500000000000000, 0.3750000000000000000, 0.4062500000000000000, 0.4375000000000000000, 0.4687500000000000000, 0.5000000000000000000, 0.5312500000000000000, 0.5625000000000000000, 0.5937500000000000000, 0.6250000000000000000, 0.6562500000000000000, 0.6875000000000000000, 0.7187500000000000000, 0.7500000000000000000, 0.7812500000000000000, 0.8125000000000000000, 0.8437500000000000000, 0.8750000000000000000, 0.9062500000000000000, 0.9375000000000000000, 0.9687500000000000000, 1.000000000000000000 ),
 .UNSPECIFIED. ) 
 GEOMETRIC_REPRESENTATION_ITEM ( )  RATIONAL_B_SPLINE_SURFACE ( (
 ( 1.000000000000000000, 0.9238795325112869605, 1.000000000000000000, 0.9238795325112869605, 1.000000000000000000, 0.9238795325112869605, 1.000000000000000000, 0.9238795325112869605, 1.000000000000000000, 0.9238795325112869605, 1.000000000000000000, 0.9238795325112869605, 1.000000000000000000, 0.9238795325112869605, 1.000000000000000000, 0.9238795325112869605, 1.000000000000000000, 0.9238795325112869605, 1.000000000000000000, 0.9238795325112869605, 1.000000000000000000, 0.9238795325112869605, 1.000000000000000000, 0.9238795325112869605, 1.000000000000000000, 0.9238795325112869605, 1.000000000000000000, 0.9238795325112869605, 1.000000000000000000, 0.9238795325112869605, 1.000000000000000000, 0.9238795325112869605, 1.000000000000000000, 0.9238795325112869605, 1.000000000000000000, 0.9238795325112869605, 1.000000000000000000, 0.9238795325112869605, 1.000000000000000000, 0.9238795325112869605, 1.000000000000000000, 0.9238795325112869605, 1.000000000000000000, 0.9238795325112869605, 1.000000000000000000, 0.9238795325112869605, 1.000000000000000000, 0.9238795325112869605, 1.000000000000000000, 0.9238795325112869605, 1.000000000000000000, 0.9238795325112869605, 1.000000000000000000, 0.9238795325112869605, 1.000000000000000000, 0.9238795325112869605, 1.000000000000000000, 0.9238795325112869605, 1.000000000000000000, 0.9238795325112869605, 1.000000000000000000, 0.9238795325112869605, 1.000000000000000000, 0.9238795325112869605, 1.000000000000000000),
 ( 1.000000000000000000, 0.9238795325112869605, 1.000000000000000000, 0.9238795325112869605, 1.000000000000000000, 0.9238795325112869605, 1.000000000000000000, 0.9238795325112869605, 1.000000000000000000, 0.9238795325112869605, 1.000000000000000000, 0.9238795325112869605, 1.000000000000000000, 0.9238795325112869605, 1.000000000000000000, 0.9238795325112869605, 1.000000000000000000, 0.9238795325112869605, 1.000000000000000000, 0.9238795325112869605, 1.000000000000000000, 0.9238795325112869605, 1.000000000000000000, 0.9238795325112869605, 1.000000000000000000, 0.9238795325112869605, 1.000000000000000000, 0.9238795325112869605, 1.000000000000000000, 0.9238795325112869605, 1.000000000000000000, 0.9238795325112869605, 1.000000000000000000, 0.9238795325112869605, 1.000000000000000000, 0.9238795325112869605, 1.000000000000000000, 0.9238795325112869605, 1.000000000000000000, 0.9238795325112869605, 1.000000000000000000, 0.9238795325112869605, 1.000000000000000000, 0.9238795325112869605, 1.000000000000000000, 0.9238795325112869605, 1.000000000000000000, 0.9238795325112869605, 1.000000000000000000, 0.9238795325112869605, 1.000000000000000000, 0.9238795325112869605, 1.000000000000000000, 0.9238795325112869605, 1.000000000000000000, 0.9238795325112869605, 1.000000000000000000, 0.9238795325112869605, 1.000000000000000000, 0.9238795325112869605, 1.000000000000000000, 0.9238795325112869605, 1.000000000000000000, 0.9238795325112869605, 1.000000000000000000) ) ) 
 REPRESENTATION_ITEM ( '' )  SURFACE ( )  );
#39249=ADVANCED_FACE ( 'NONE', ( #6320 ), #20463, .F. ) ;
#39259=PRODUCT_DEFINITION_CONTEXT ( 'detailed design', #35525, 'design' ) ;
#39265=CARTESIAN_POINT ( 'NONE',  ( 122.6604860609119640, -3.387241619883791355, -18.17469012370385073 ) ) ;
#39279=CARTESIAN_POINT ( 'NONE',  ( 124.5716588232362625, -9.842409859139314321, -13.88118749700920418 ) ) ;
#39280=CARTESIAN_POINT ( 'NONE',  ( 120.6463454359119822, -11.07370829466463569, -12.81314460846529002 ) ) ;
#39308=DIRECTION ( 'NONE',  ( 0.000000000000000000, -0.4669533266896290225, -0.8842819633428516957 ) ) ;
#39321=ORIENTED_EDGE ( 'NONE', *, *, #18686, .T. ) ;
#39348=CARTESIAN_POINT ( 'NONE',  ( 122.9476408503701492, -8.552676153439012552, -17.65880394779906837 ) ) ;
#39368=CARTESIAN_POINT ( 'NONE',  ( 123.7022829359119811, -4.283928203966213211, -7.183505701512925334 ) ) ;
#39387=CARTESIAN_POINT ( 'NONE',  ( 121.3408766859119794, -0.06289925094097943703, -9.412459353600674206 ) ) ;
#39390=CARTESIAN_POINT ( 'NONE',  ( 120.2296266859119953, -9.033780868592240054, -16.85052413769862056 ) ) ;
#39421=CARTESIAN_POINT ( 'NONE',  ( 119.9518141859119851, -0.8832429491016019485, -18.19431474523657855 ) ) ;
#39434=CARTESIAN_POINT ( 'NONE',  ( 119.7434548109119703, -8.523281198020143279, -6.279169073056789507 ) ) ;
#39447=CARTESIAN_POINT ( 'NONE',  ( 123.9584548109119737, -3.874292970208447873, -21.33175929725637587 ) ) ;
#39492=CARTESIAN_POINT ( 'NONE',  ( 123.6328298109119714, -7.200787124940443817, -17.81845355600750835 ) ) ;
#39507=CARTESIAN_POINT ( 'NONE',  ( 124.5900975541519244, -9.759545612246029123, -14.42929304450613159 ) ) ;
#39560=CARTESIAN_POINT ( 'NONE',  ( 124.3741441133358876, -5.860671235867299877, -5.499845748860171746 ) ) ;
#39593=CARTESIAN_POINT ( 'NONE',  ( 120.5768923109119868, -0.4387604401700512802, -15.73000352943951619 ) ) ;
#39617=CARTESIAN_POINT ( 'NONE',  ( 122.4521266859119635, -0.06289925094097943703, -9.412459353600674206 ) ) ;
#39620=CARTESIAN_POINT ( 'NONE',  ( 122.2771248871816141, -6.188980713775695364, -18.62212668298318619 ) ) ;
#39625=CARTESIAN_POINT ( 'NONE',  ( 124.5059548109119731, -9.675232987814487373, -12.03232374619203249 ) ) ;
#39629=CARTESIAN_POINT ( 'NONE',  ( 125.3240071284520951, -11.78859274923427947, -15.05733176109422544 ) ) ;
#39645=CARTESIAN_POINT ( 'NONE',  ( 120.5768923109119868, -9.959231468620755479, -10.70263013195267199 ) ) ;
#39650=CARTESIAN_POINT ( 'NONE',  ( 123.3550173109119612, 0.2312338769422704887, -16.08380026872395874 ) ) ;
#39662=VERTEX_POINT ( 'NONE', #39118 ) ;
#39676=CARTESIAN_POINT ( 'NONE',  ( 124.0578213371693721, -1.204740764657090679, -20.50723739579558824 ) ) ;
#39682=CARTESIAN_POINT ( 'NONE',  ( 124.5036465538288581, -3.850231221856767139, -21.22756876946701254 ) ) ;
#39685=CARTESIAN_POINT ( 'NONE',  ( 120.8547048109119686, -2.527210466738041728, -8.967976844669124148 ) ) ;
#39695=CIRCLE ( 'NONE', #41183, 6.500000000000003553 ) ;
#39700=CARTESIAN_POINT ( 'NONE',  ( 120.2957407289968330, -6.032552146994436981, -18.32589373581284420 ) ) ;
#39716=CARTESIAN_POINT ( 'NONE',  ( 121.2714235609119697, 0.6414057260225851653, -11.69287257290600657 ) ) ;
#39753=CARTESIAN_POINT ( 'NONE',  ( 120.5194882662982963, -6.118135741080345191, -18.48796566952144005 ) ) ;
#39803=EDGE_CURVE ( 'NONE', #23418, #28617, #15120, .T. ) ;
#39832=EDGE_CURVE ( 'NONE', #42647, #4044, #25089, .T. ) ;
#39850=CARTESIAN_POINT ( 'NONE',  ( 121.5492360609119800, -6.564341423271553566, -7.887810678476492754 ) ) ;
#39852=CARTESIAN_POINT ( 'NONE',  ( 123.9584548109119737, -11.97804492312075553, -17.05249760251923163 ) ) ;
#39871=CARTESIAN_POINT ( 'NONE',  ( 122.1048610609119720, -3.163656168406935087, -18.89861972220014508 ) ) ;
#39872=CARTESIAN_POINT ( 'NONE',  ( 122.3132204359119868, 1.345710702986147034, -13.97328579221134426 ) ) ;
#39876=ORIENTED_EDGE ( 'NONE', *, *, #12758, .T. ) ;
#39939=CARTESIAN_POINT ( 'NONE',  ( 123.9106423109119675, -0.4387604401700512802, -15.73000352943951619 ) ) ;
#39952=ORIENTED_EDGE ( 'NONE', *, *, #26730, .T. ) ;
#39998=CARTESIAN_POINT ( 'NONE',  ( 124.9063227527197313, -5.965318915412476386, -5.805585508435772368 ) ) ;
#40002=CARTESIAN_POINT ( 'NONE',  ( 120.5074391859119913, -1.406689858478933353, -17.56299727309130887 ) ) ;
#40042=ORIENTED_EDGE ( 'NONE', *, *, #35289, .F. ) ;
#40054=CARTESIAN_POINT ( 'NONE',  ( 124.9868051361382868, -12.36944789948101331, -14.53642012793133986 ) ) ;
#40059=DIRECTION ( 'NONE',  ( -1.000000000000000000, 0.000000000000000000, -0.000000000000000000 ) ) ;
#40062=CARTESIAN_POINT ( 'NONE',  ( 122.0955187714537828, -6.306599966548167124, -18.84486539759072699 ) ) ;
#40073=CARTESIAN_POINT ( 'NONE',  ( 124.6793944118516464, -11.84801880692714704, -16.90254992618838514 ) ) ;
#40092=CARTESIAN_POINT ( 'NONE',  ( 122.2437673109119629, -9.289237151508428880, -11.05642687123710388 ) ) ;
#40097=CARTESIAN_POINT ( 'NONE',  ( 122.7993923109119692, -9.959231468620755479, -10.70263013195267199 ) ) ;
#40098=CARTESIAN_POINT ( 'NONE',  ( 120.5074391859119913, -8.844754642576884152, -8.592115655440050404 ) ) ;
#40130=CARTESIAN_POINT ( 'NONE',  ( 125.0820341042009858, -1.685509051457968921, -20.18185560315022187 ) ) ;
#40133=CARTESIAN_POINT ( 'NONE',  ( 123.9800954359119771, 0.5291689781388270175, -13.89700978578772705 ) ) ;
#40149=CARTESIAN_POINT ( 'NONE',  ( 124.5308374810065430, -10.18911555409675707, -12.76055059223490318 ) ) ;
#40167=CARTESIAN_POINT ( 'NONE',  ( 122.0354079359119908, -5.444069387712269226, -19.60292469916370450 ) ) ;
#40171=CARTESIAN_POINT ( 'NONE',  ( 124.1884548109119777, -2.527210466738041728, -8.967976844669124148 ) ) ;
#40227=ORIENTED_EDGE ( 'NONE', *, *, #8365, .T. ) ;
#40231=B_SPLINE_CURVE_WITH_KNOTS ( 'NONE', 3,
 ( #30499, #6333, #37331, #5868, #19791, #37564, #33674, #12962 ),
 .UNSPECIFIED., .F., .F.,
 ( 4, 2, 2, 4 ),
 ( 0.000000000000000000, 0.2499999999999996669, 0.4999999999999993339, 1.000000000000000000 ),
 .UNSPECIFIED. ) ;
#40295=CARTESIAN_POINT ( 'NONE',  ( 125.0660727672600956, 2.552004055856275322, -12.19903144353943603 ) ) ;
#40303=CARTESIAN_POINT ( 'NONE',  ( 124.2749441479622021, -11.95494744398080655, -17.02855821661913183 ) ) ;
#40307=ORIENTED_EDGE ( 'NONE', *, *, #37017, .T. ) ;
#40324=CARTESIAN_POINT ( 'NONE',  ( 120.2296266859119953, -9.033780868592240054, -16.85052413769862056 ) ) ;
#40325=CARTESIAN_POINT ( 'NONE',  ( 121.8965016859119856, -9.665098340737509730, -17.37397104707595474 ) ) ;
#40340=ORIENTED_EDGE ( 'NONE', *, *, #38994, .T. ) ;
#40350=DIRECTION ( 'NONE',  ( 1.000000000000000000, 0.000000000000000000, 0.000000000000000000 ) ) ;
#40356=CARTESIAN_POINT ( 'NONE',  ( 125.3290191022591529, -2.376857512254589189, -20.05354607378702525 ) ) ;
#40359=CARTESIAN_POINT ( 'NONE',  ( 121.6881423109119709, -0.4387604401700512802, -15.73000352943951619 ) ) ;
#40363=CIRCLE ( 'NONE', #23648, 5.952500000000000568 ) ;
#40395=CARTESIAN_POINT ( 'NONE',  ( 122.2437673109119629, 0.2312338769422704887, -16.08380026872395874 ) ) ;
#40400=CARTESIAN_POINT ( 'NONE',  ( 122.1743141859119817, -8.321307733199551748, -9.223433127585318303 ) ) ;
#40408=ORIENTED_EDGE ( 'NONE', *, *, #6377, .T. ) ;
#40439=CARTESIAN_POINT ( 'NONE',  ( 119.3961891859119930, -1.406689858478933353, -17.56299727309130887 ) ) ;
#40467=CARTESIAN_POINT ( 'NONE',  ( 120.9936110609119737, -6.340755971794695078, -8.611740276972781771 ) ) ;
#40487=CARTESIAN_POINT ( 'NONE',  ( 125.4584548109119737, -4.863998795839242995, -13.39321520033831447 ) ) ;
#40532=CARTESIAN_POINT ( 'NONE',  ( 125.2320293092190013, -12.02258392215929561, -14.78429556032320669 ) ) ;
#40534=CARTESIAN_POINT ( 'NONE',  ( 123.9832704359119759, 0.5245030254254422486, -13.89657392289357141 ) ) ;
#40550=AXIS2_PLACEMENT_3D ( 'NONE', #24037, #37235, #2362 ) ;
#40555=CARTESIAN_POINT ( 'NONE',  ( 120.3685329359119862, -5.367793381288652910, -18.78638297431638904 ) ) ;
#40556=CARTESIAN_POINT ( 'NONE',  ( 122.3132204359119868, -10.25716656981731489, -12.88942061488890545 ) ) ;
#40580=CARTESIAN_POINT ( 'NONE',  ( 119.9486391859119863, -8.318316608003105017, -9.227040655997587493 ) ) ;
#40586=CARTESIAN_POINT ( 'NONE',  ( 125.2732466787873591, -2.097490018383950439, -20.06580088923637106 ) ) ;
#40589=CARTESIAN_POINT ( 'NONE',  ( 123.3550173109119612, -9.289237151508434209, -11.05642687123711276 ) ) ;
#40612=CARTESIAN_POINT ( 'NONE',  ( 125.4584548109119737, -0.8336775508564547854, -5.760888413673081132 ) ) ;
#40622=CARTESIAN_POINT ( 'NONE',  ( 123.5633766859119760, -0.06289925094097943703, -9.412459353600674206 ) ) ;
#40626=CARTESIAN_POINT ( 'NONE',  ( 123.3550173109119612, -9.289237151508434209, -11.05642687123711276 ) ) ;
#40662=EDGE_CURVE ( 'NONE', #30417, #42647, #22815, .T. ) ;
#40687=CARTESIAN_POINT ( 'NONE',  ( 120.9936110609119737, -6.340755971794696855, -8.611740276972787100 ) ) ;
#40699=CARTESIAN_POINT ( 'NONE',  ( 124.1585801725099998, -7.429215134363809092, -20.97079166887802160 ) ) ;
#40723=CARTESIAN_POINT ( 'NONE',  ( 119.7434548109119703, -0.8336775508564547854, -5.760888413673081132 ) ) ;
#40748=CARTESIAN_POINT ( 'NONE',  ( 123.4244704359119709, -10.25716656981731489, -12.88942061488890545 ) ) ;
#40759=CARTESIAN_POINT ( 'NONE',  ( 124.6778016859120015, -9.030173340179786123, -16.84753301250241009 ) ) ;
#40761=CARTESIAN_POINT ( 'NONE',  ( 119.7434548109120271, -0.1940514955484507198, -11.17407767511812899 ) ) ;
#40782=CARTESIAN_POINT ( 'NONE',  ( 120.9936110609119737, -6.340755971794695078, -8.611740276972781771 ) ) ;
#40783=CARTESIAN_POINT ( 'NONE',  ( 121.6881423109119709, -0.4387604401700512802, -15.73000352943951619 ) ) ;
#40811=DIRECTION ( 'NONE',  ( 0.000000000000000000, 0.4669533266896288004, 0.8842819633428518067 ) ) ;
#40822=CARTESIAN_POINT ( 'NONE',  ( 123.7717360609119623, -3.387241619883791355, -18.17469012370385073 ) ) ;
#40836=CARTESIAN_POINT ( 'NONE',  ( 125.4584548109119737, -7.429215134363809092, -20.97079166887802160 ) ) ;
#40854=CARTESIAN_POINT ( 'NONE',  ( 122.1048610609119720, -3.163656168406935087, -18.89861972220014508 ) ) ;
#40860=CARTESIAN_POINT ( 'NONE',  ( 123.1466579359119891, -4.360204210389833968, -8.000047426360245240 ) ) ;
#40869=DIRECTION ( 'NONE',  ( 0.000000000000000000, 0.4669533266896289669, 0.8842819633428516957 ) ) ;
#40881=DIRECTION ( 'NONE',  ( -1.000000000000000000, 0.000000000000000000, -0.000000000000000000 ) ) ;
#40882=DIRECTION ( 'NONE',  ( 0.000000000000000000, 0.4669533266896289669, 0.8842819633428518067 ) ) ;
#40926=CARTESIAN_POINT ( 'NONE',  ( 123.2161110609119703, -6.340755971794695078, -8.611740276972781771 ) ) ;
#40974=( BOUNDED_CURVE ( )  B_SPLINE_CURVE ( 2, ( #4528, #18451, #42842, #32339, #36208, #18669, #25739, #1329, #4975, #15023, #1106, #1774, #39645, #36429, #15242, #18886, #26184 ),
 .UNSPECIFIED., .F., .F. ) 
 B_SPLINE_CURVE_WITH_KNOTS ( ( 3, 2, 2, 2, 2, 2, 2, 2, 3 ),
 ( 0.008913552404467750892, 0.03125000000000000000, 0.06250000000000000000, 0.09375000000000000000, 0.1250000000000000000, 0.1562500000000000000, 0.1875000000000000000, 0.2187500000000000000, 0.2410864475955325215 ),
 .UNSPECIFIED. ) 
 CURVE ( )  GEOMETRIC_REPRESENTATION_ITEM ( )  RATIONAL_B_SPLINE_CURVE ( ( 0.9689618144536780164, 0.9455916533437099813, 1.000000000000000000, 0.9238795325112869605, 1.000000000000000000, 0.9238795325112869605, 1.000000000000000000, 0.9238795325112869605, 1.000000000000000000, 0.9238795325112869605, 1.000000000000000000, 0.9238795325112869605, 1.000000000000000000, 0.9238795325112869605, 1.000000000000000000, 0.9455916533437099813, 0.9689618144536780164 ) ) 
 REPRESENTATION_ITEM ( '' )  );
#40982=EDGE_CURVE ( 'NONE', #1412, #16965, #39695, .T. ) ;
#40997=CARTESIAN_POINT ( 'NONE',  ( 124.6083485609119776, -9.641336978641852795, -14.86869474514273648 ) ) ;
#40999=CARTESIAN_POINT ( 'NONE',  ( 119.7434548109119703, -5.531992483615866263, -19.02952050076702051 ) ) ;
#41019=CARTESIAN_POINT ( 'NONE',  ( 122.3132204359119868, -10.25716656981731489, -12.88942061488890545 ) ) ;
#41020=CARTESIAN_POINT ( 'NONE',  ( 120.7852516859119731, -0.6942167230862511529, -9.935906262978006609 ) ) ;
#41054=CARTESIAN_POINT ( 'NONE',  ( 122.2437673109119629, -9.289237151508434209, -11.05642687123711276 ) ) ;
#41086=CARTESIAN_POINT ( 'NONE',  ( 122.4521266859119635, -0.06289925094097943703, -9.412459353600674206 ) ) ;
#41087=VECTOR ( 'NONE', #18142, 1000.000000000000000 ) ;
#41091=CARTESIAN_POINT ( 'NONE',  ( 121.6186891859119896, -1.406689858478933353, -17.56299727309130887 ) ) ;
#41114=CARTESIAN_POINT ( 'NONE',  ( 120.9114422641554540, -8.548534124195553474, -17.65096007659764510 ) ) ;
#41126=CARTESIAN_POINT ( 'NONE',  ( 120.2990798109119766, -7.200787124940443817, -17.81845355600750835 ) ) ;
#41128=CARTESIAN_POINT ( 'NONE',  ( 122.4521266859119635, -9.033780868592240054, -16.85052413769862056 ) ) ;
#41152=CARTESIAN_POINT ( 'NONE',  ( 122.7993923109119692, -0.4387604401700512802, -15.73000352943951619 ) ) ;
#41155=CARTESIAN_POINT ( 'NONE',  ( 125.2183010572621669, 2.324478367502957443, -12.03255835460978318 ) ) ;
#41163=CARTESIAN_POINT ( 'NONE',  ( 119.7434548109119703, -2.316996251443989241, -21.63995271010855248 ) ) ;
#41183=AXIS2_PLACEMENT_3D ( 'NONE', #40487, #9246, #36362 ) ;
#41210=CARTESIAN_POINT ( 'NONE',  ( 125.4584548109119737, -4.863998795839242995, -13.39321520033831447 ) ) ;
#41222=CARTESIAN_POINT ( 'NONE',  ( 123.6328298109119714, -7.200787124940195127, -17.81845355600763625 ) ) ;
#41243=DIRECTION ( 'NONE',  ( 0.000000000000000000, 0.2950959089608259922, -0.9554676365605399013 ) ) ;
#41245=CARTESIAN_POINT ( 'NONE',  ( 119.8823610609119754, -6.340755971794695078, -8.611740276972781771 ) ) ;
#41266=CARTESIAN_POINT ( 'NONE',  ( 121.3408766859119794, -0.06289925094097943703, -9.412459353600674206 ) ) ;
#41272=CARTESIAN_POINT ( 'NONE',  ( 119.7434548109119703, -4.863998795839242995, -13.39321520033831447 ) ) ;
#41280=CARTESIAN_POINT ( 'NONE',  ( 120.5768923109119868, -9.959231468620755479, -10.70263013195267199 ) ) ;
#41319=CARTESIAN_POINT ( 'NONE',  ( 123.4244704359119709, 1.345710702986147034, -13.97328579221134426 ) ) ;
#41330=VECTOR ( 'NONE', #33212, 1000.000000000000000 ) ;
#41361=EDGE_LOOP ( 'NONE', ( #33027, #40227, #34820, #17854 ) ) ;
#41373=CARTESIAN_POINT ( 'NONE',  ( 120.6463454359119822, 0.5291689781388270175, -13.89700978578772705 ) ) ;
#41383=CARTESIAN_POINT ( 'NONE',  ( 120.1601735609119856, 0.6414057260225851653, -11.69287257290600657 ) ) ;
#41384=ORIENTED_EDGE ( 'NONE', *, *, #41766, .F. ) ;
#41391=CARTESIAN_POINT ( 'NONE',  ( 124.8837246474731728, -7.285888985094468140, -20.69937111904969385 ) ) ;
#41432=EDGE_LOOP ( 'NONE', ( #34842, #37599, #17929, #23451 ) ) ;
#41435=DIRECTION ( 'NONE',  ( -1.000000000000000000, 0.000000000000000000, -0.000000000000000000 ) ) ;
#41438=CARTESIAN_POINT ( 'NONE',  ( 124.6040088552590959, -9.657516929632931735, -14.85109078001513083 ) ) ;
#41442=CARTESIAN_POINT ( 'NONE',  ( 123.0772048109119652, -2.527210466738039063, -8.967976844669125924 ) ) ;
#41447=CARTESIAN_POINT ( 'NONE',  ( 122.3011713555256534, -8.364211927971188842, -17.30190421972978143 ) ) ;
#41458=CARTESIAN_POINT ( 'NONE',  ( 120.2990798109119766, -2.173413727453600508, -8.297982527556802879 ) ) ;
#41463=CARTESIAN_POINT ( 'NONE',  ( 122.7299391859119737, -1.406689858478933353, -17.56299727309130887 ) ) ;
#41464=CARTESIAN_POINT ( 'NONE',  ( 121.4797829359119987, -5.367793381288652910, -18.78638297431638904 ) ) ;
#41483=CARTESIAN_POINT ( 'NONE',  ( 119.8823610609119754, -3.163656168406935087, -18.89861972220014508 ) ) ;
#41516=CARTESIAN_POINT ( 'NONE',  ( 123.7717360609119623, -6.564341423271550902, -7.887810678476487425 ) ) ;
#41535=CARTESIAN_POINT ( 'NONE',  ( 120.5768923109119868, -9.959231468620755479, -10.70263013195267199 ) ) ;
#41572=CARTESIAN_POINT ( 'NONE',  ( 119.3961891859119930, -1.406689858478933353, -17.56299727309130887 ) ) ;
#41574=CARTESIAN_POINT ( 'NONE',  ( 122.7299391859119737, -1.406689858478933353, -17.56299727309130887 ) ) ;
#41589=CARTESIAN_POINT ( 'NONE',  ( 121.6881423109119709, -0.4387604401700512802, -15.73000352943951619 ) ) ;
#41593=ORIENTED_EDGE ( 'NONE', *, *, #31983, .F. ) ;
#41600=CARTESIAN_POINT ( 'NONE',  ( 120.5768923109119868, -9.959231468620755479, -10.70263013195267199 ) ) ;
#41603=CARTESIAN_POINT ( 'NONE',  ( 125.1028739313161964, 2.504666235963327381, -12.16890819705307614 ) ) ;
#41668=CARTESIAN_POINT ( 'NONE',  ( 124.6746266859119743, -9.033780868592048208, -16.85052413769886215 ) ) ;
#41680=CARTESIAN_POINT ( 'NONE',  ( 121.4103298109119748, -2.173413727453600508, -8.297982527556802879 ) ) ;
#41706=CARTESIAN_POINT ( 'NONE',  ( 125.3400398954497632, -6.228147054556873563, -18.69629702666285809 ) ) ;
#41714=CARTESIAN_POINT ( 'NONE',  ( 121.0751082044368303, -6.247802574075781656, -18.73351920797576042 ) ) ;
#41725=CARTESIAN_POINT ( 'NONE',  ( 123.1815811593281751, -8.517053830703076756, -17.59134500557230396 ) ) ;
#41745=EDGE_CURVE ( 'NONE', #31784, #7134, #4065, .T. ) ;
#41753=CARTESIAN_POINT ( 'NONE',  ( 123.9106423109119675, -9.959231468620755479, -10.70263013195267199 ) ) ;
#41766=EDGE_CURVE ( 'NONE', #7363, #31995, #26615, .T. ) ;
#41811=CARTESIAN_POINT ( 'NONE',  ( 120.2990798109119766, -7.200787124940443817, -17.81845355600750835 ) ) ;
#41821=CARTESIAN_POINT ( 'NONE',  ( 124.2579079359120016, -4.360204210389833968, -8.000047426360245240 ) ) ;
#41824=CARTESIAN_POINT ( 'NONE',  ( 123.9584548109119737, 0.04957186715663468302, -7.079989135975798042 ) ) ;
#41898=CARTESIAN_POINT ( 'NONE',  ( 119.8129079359119942, -5.444069387712269226, -19.60292469916370450 ) ) ;
#41904=CARTESIAN_POINT ( 'NONE',  ( 121.9659548109119811, -2.527210466738041728, -8.967976844669124148 ) ) ;
#41934=CARTESIAN_POINT ( 'NONE',  ( 125.0849378844219046, -10.94598263288078321, -9.020557899002023206 ) ) ;
#41936=CARTESIAN_POINT ( 'NONE',  ( 123.8411891859119862, -8.844754642576884152, -8.592115655440050404 ) ) ;
#41944=CARTESIAN_POINT ( 'NONE',  ( 123.9584548109119737, 2.250047331442289966, -9.733932798157443500 ) ) ;
#41986=CARTESIAN_POINT ( 'NONE',  ( 119.7434548109119703, -4.863998795839242995, -13.39321520033831447 ) ) ;
#42025=CARTESIAN_POINT ( 'NONE',  ( 121.4797829359119987, -5.367793381288652910, -18.78638297431638904 ) ) ;
#42039=CARTESIAN_POINT ( 'NONE',  ( 124.1884548109119777, -7.554583864224885481, -18.48844787311982785 ) ) ;
#42042=CARTESIAN_POINT ( 'NONE',  ( 119.7434548109119703, -2.527210466738042172, -8.967976844669124148 ) ) ;
#42054=CARTESIAN_POINT ( 'NONE',  ( 119.7434548109119561, -1.948846192371206598, -9.275183199048456117 ) ) ;
#42080=ORIENTED_EDGE ( 'NONE', *, *, #16655, .T. ) ;
#42102=CARTESIAN_POINT ( 'NONE',  ( 125.4584548109119737, -9.675291321254654520, -19.78473021908636298 ) ) ;
#42104=DIRECTION ( 'NONE',  ( 1.000000000000000000, 0.000000000000000000, 0.000000000000000000 ) ) ;
#42111=CARTESIAN_POINT ( 'NONE',  ( 122.4767535264548854, -8.247323210606174015, -17.08054893949881858 ) ) ;
#42135=SURFACE_SIDE_STYLE ('',( #10454 ) ) ;
#42142=VERTEX_POINT ( 'NONE', #20599 ) ;
#42152=CARTESIAN_POINT ( 'NONE',  ( 124.1916298109119765, -2.529232162390850913, -8.971805383624186447 ) ) ;
#42157=CARTESIAN_POINT ( 'NONE',  ( 125.0480389746926306, -10.95843241427508730, -8.969000644412037815 ) ) ;
#42185=CARTESIAN_POINT ( 'NONE',  ( 0.000000000000000000, 0.000000000000000000, 0.000000000000000000 ) ) ;
#42244=ORIENTED_EDGE ( 'NONE', *, *, #10043, .F. ) ;
#42245=CARTESIAN_POINT ( 'NONE',  ( 120.7157985609119635, -0.08252387247370887580, -11.91645802438286417 ) ) ;
#42259=CARTESIAN_POINT ( 'NONE',  ( 123.0077516859119839, -9.665098340737509730, -17.37397104707595474 ) ) ;
#42288=CARTESIAN_POINT ( 'NONE',  ( 121.5428448253203015, -6.059724811980599313, -18.37735133589800540 ) ) ;
#42315=DIRECTION ( 'NONE',  ( -1.000000000000000000, 0.000000000000000000, -0.000000000000000000 ) ) ;
#42347=CARTESIAN_POINT ( 'NONE',  ( 121.4797829359119987, -5.367793381288652910, -18.78638297431638904 ) ) ;
#42368=CARTESIAN_POINT ( 'NONE',  ( 122.5215798109119874, -2.173413727453600508, -8.297982527556802879 ) ) ;
#42373=CARTESIAN_POINT ( 'NONE',  ( 119.7434548109119703, 1.449227268523328505, -18.30678586333412738 ) ) ;
#42392=CARTESIAN_POINT ( 'NONE',  ( 123.2292200565388782, -8.485573535863887074, -17.53172993199662599 ) ) ;
#42471=CARTESIAN_POINT ( 'NONE',  ( 122.9382985609119743, -0.08252387247370887580, -11.91645802438286417 ) ) ;
#42485=CARTESIAN_POINT ( 'NONE',  ( 124.5917477490678777, -9.748629547111955063, -14.47908513545650955 ) ) ;
#42486=CARTESIAN_POINT ( 'NONE',  ( 121.8270485609119760, -10.36940331770106916, -15.09355782777062061 ) ) ;
#42490=CARTESIAN_POINT ( 'NONE',  ( 125.3303382280751492, -1.129804808602307586, -7.332909019048677202 ) ) ;
#42518=LINE ( 'NONE', #4197, #17573 ) ;
#42547=CARTESIAN_POINT ( 'NONE',  ( 123.3550173109119612, -9.289237151508428880, -11.05642687123710211 ) ) ;
#42566=CARTESIAN_POINT ( 'NONE',  ( 121.8965016859119856, -0.6942167230862511529, -9.935906262978006609 ) ) ;
#42576=CIRCLE ( 'NONE', #6145, 8.000000000000001776 ) ;
#42585=CARTESIAN_POINT ( 'NONE',  ( 121.4797829359119987, -4.283928203966213211, -7.183505701512925334 ) ) ;
#42586=CARTESIAN_POINT ( 'NONE',  ( 123.6803214993270643, -5.999514616106329967, -18.26332968281675662 ) ) ;
#42589=CARTESIAN_POINT ( 'NONE',  ( 122.8688454359119646, -11.07370829466463569, -12.81314460846529002 ) ) ;
#42600=CARTESIAN_POINT ( 'NONE',  ( 123.6776560953690591, -6.001247023715324147, -18.26661038929047010 ) ) ;
#42618=CARTESIAN_POINT ( 'NONE',  ( 122.3132204359119868, -10.25716656981731489, -12.88942061488890545 ) ) ;
#42647=VERTEX_POINT ( 'NONE', #36496 ) ;
#42653=ADVANCED_FACE ( 'NONE', ( #44037 ), #12801, .F. ) ;
#42659=CARTESIAN_POINT ( 'NONE',  ( 120.7852516859119731, -0.6942167230862511529, -9.935906262978006609 ) ) ;
#42694=CARTESIAN_POINT ( 'NONE',  ( 123.0772048109119652, -2.527210466738041728, -8.967976844669124148 ) ) ;
#42703=CIRCLE ( 'NONE', #5550, 8.000000000000001776 ) ;
#42708=CARTESIAN_POINT ( 'NONE',  ( 124.5519021741527581, -9.864481698965258616, -13.30856797738673336 ) ) ;
#42710=CIRCLE ( 'NONE', #28130, 8.000000000000001776 ) ;
#42711=CARTESIAN_POINT ( 'NONE',  ( 122.6604860609119640, -6.564341423271550902, -7.887810678476487425 ) ) ;
#42714=CARTESIAN_POINT ( 'NONE',  ( 125.0302870206144945, -2.333779524057464361, -6.280435070964202282 ) ) ;
#42723=CARTESIAN_POINT ( 'NONE',  ( 119.7434548109119845, -1.178581368880148084, -9.878999011044413692 ) ) ;
#42743=CARTESIAN_POINT ( 'NONE',  ( 125.4584548109119737, -12.36944789948969614, -14.53642012792675509 ) ) ;
#42752=EDGE_LOOP ( 'NONE', ( #34141, #41384, #34865, #13744 ) ) ;
#42758=VERTEX_POINT ( 'NONE', #23052 ) ;
#42795=CARTESIAN_POINT ( 'NONE',  ( 122.1743141859119817, -8.321307733199551748, -9.223433127585318303 ) ) ;
#42813=CARTESIAN_POINT ( 'NONE',  ( 120.7852516859119731, -9.665098340737509730, -17.37397104707595474 ) ) ;
#42816=CARTESIAN_POINT ( 'NONE',  ( 119.1878298109119783, -7.200787124940443817, -17.81845355600750835 ) ) ;
#42829=CARTESIAN_POINT ( 'NONE',  ( 125.3296504289671844, -11.36836562817265950, -10.49722269535554098 ) ) ;
#42834=LINE ( 'NONE', #24823, #29996 ) ;
#42836=ORIENTED_EDGE ( 'NONE', *, *, #44562, .T. ) ;
#42842=CARTESIAN_POINT ( 'NONE',  ( 119.8823610609119754, -3.163656168406935087, -18.89861972220014508 ) ) ;
#42869=ADVANCED_FACE ( 'NONE', ( #33978 ), #3199, .F. ) ;
#42888=ORIENTED_EDGE ( 'NONE', *, *, #26138, .T. ) ;
#42917=CARTESIAN_POINT ( 'NONE',  ( 120.7157985609119635, -10.36940331770106916, -15.09355782777062061 ) ) ;
#42920=ORIENTED_EDGE ( 'NONE', *, *, #8365, .F. ) ;
#42932=CARTESIAN_POINT ( 'NONE',  ( 124.5737018702985779, -9.836393355957630646, -13.94123563784690667 ) ) ;
#42956=CARTESIAN_POINT ( 'NONE',  ( 121.9092173576684957, -6.302457937304696500, -18.83702152638931082 ) ) ;
#43010=CARTESIAN_POINT ( 'NONE',  ( 123.2855641859119942, -0.8832429491016019485, -18.19431474523657855 ) ) ;
#43029=ADVANCED_FACE ( 'NONE', ( #9221 ), #30642, .T. ) ;
#43034=CARTESIAN_POINT ( 'NONE',  ( 120.9936110609119737, -6.340755971794695078, -8.611740276972781771 ) ) ;
#43047=VECTOR ( 'NONE', #5326, 1000.000000000000000 ) ;
#43048=CARTESIAN_POINT ( 'NONE',  ( 125.2014504115533668, -11.57818613074989855, -16.36145069722488898 ) ) ;
#43055=CARTESIAN_POINT ( 'NONE',  ( 121.4551560953690483, -6.001247023715324147, -18.26661038929047010 ) ) ;
#43067=CARTESIAN_POINT ( 'NONE',  ( 120.0907204359119760, 1.345710702986147034, -13.97328579221134426 ) ) ;
#43068=CARTESIAN_POINT ( 'NONE',  ( 120.1601735609119856, 0.6414057260225851653, -11.69287257290600657 ) ) ;
#43069=CARTESIAN_POINT ( 'NONE',  ( 124.0588908503701475, -8.552676153439012552, -17.65880394779906837 ) ) ;
#43101=CARTESIAN_POINT ( 'NONE',  ( 125.3184118084099623, -3.219979270944925087, -20.33414543254830420 ) ) ;
#43136=CARTESIAN_POINT ( 'NONE',  ( 123.0077516859119839, -0.6942167230862511529, -9.935906262978006609 ) ) ;
#43173=ORIENTED_EDGE ( 'NONE', *, *, #17225, .T. ) ;
#43179=EDGE_CURVE ( 'NONE', #34025, #2916, #22773, .T. ) ;
#43205=CARTESIAN_POINT ( 'NONE',  ( 124.9542645564588526, -8.185087495464536289, -6.532584163191488713 ) ) ;
#43233=CARTESIAN_POINT ( 'NONE',  ( 124.9009360172597098, 2.389294270081054439, -15.88150311065928832 ) ) ;
#43240=CARTESIAN_POINT ( 'NONE',  ( 121.3408766859119794, -9.033780868592240054, -16.85052413769862056 ) ) ;
#43264=CARTESIAN_POINT ( 'NONE',  ( 122.7993923109119692, -0.4387604401700512802, -15.73000352943951619 ) ) ;
#43272=CARTESIAN_POINT ( 'NONE',  ( 124.5348847846778852, -9.832371414934382159, -12.82702404581066880 ) ) ;
#43275=CARTESIAN_POINT ( 'NONE',  ( 124.3500856911477399, -11.94161027609003334, -17.01447758398505172 ) ) ;
#43290=CARTESIAN_POINT ( 'NONE',  ( 123.9584548109119737, -12.80254289275730173, -14.38292102596908784 ) ) ;
#43295=CARTESIAN_POINT ( 'NONE',  ( 119.9518141859119851, -0.8832429491016019485, -18.19431474523657855 ) ) ;
#43321=DIRECTION ( 'NONE',  ( -1.000000000000000000, 0.000000000000000000, -0.000000000000000000 ) ) ;
#43328=CARTESIAN_POINT ( 'NONE',  ( 125.2512474355150260, -2.025430522367418718, -20.07795600484094933 ) ) ;
#43331=CARTESIAN_POINT ( 'NONE',  ( 123.9584548109119737, 0.04957186715663468302, -7.079989135975798042 ) ) ;
#43354=DIRECTION ( 'NONE',  ( -1.000000000000000000, 0.000000000000000000, -0.000000000000000000 ) ) ;
#43363=CARTESIAN_POINT ( 'NONE',  ( 123.2855641859119942, -8.321307733199551748, -9.223433127585318303 ) ) ;
#43402=CARTESIAN_POINT ( 'NONE',  ( 123.6294907289968279, -6.032552146994431652, -18.32589373581284775 ) ) ;
#43413=LINE ( 'NONE', #5096, #43047 ) ;
#43433=ADVANCED_FACE ( 'NONE', ( #11238 ), #38147, .F. ) ;
#43435=CARTESIAN_POINT ( 'NONE',  ( 119.7434548109119703, -1.204716393658298523, -20.50726132761981901 ) ) ;
#43462=CARTESIAN_POINT ( 'NONE',  ( 124.3741441133367545, 1.422210110677154971, -18.26991642492331636 ) ) ;
#43475=VERTEX_POINT ( 'NONE', #32418 ) ;
#43494=CARTESIAN_POINT ( 'NONE',  ( 125.0302870206147219, 1.954631471695863487, -10.15285534273483847 ) ) ;
#43522=CARTESIAN_POINT ( 'NONE',  ( 123.6328298109119714, -2.173413727453600508, -8.297982527556802879 ) ) ;
#43524=CARTESIAN_POINT ( 'NONE',  ( 123.7807890828414230, -8.372502050422333753, -17.31760344562334808 ) ) ;
#43547=PLANE ( 'NONE',  #12146 ) ;
#43549=CARTESIAN_POINT ( 'NONE',  ( 124.9868051361299166, -1.575707845324203493, -20.23615509330177531 ) ) ;
#43553=CARTESIAN_POINT ( 'NONE',  ( 125.0370334466769151, -1.627738329600721290, -20.20867991148268317 ) ) ;
#43556=CARTESIAN_POINT ( 'NONE',  ( 121.7575954359119805, 0.5291689781388270175, -13.89700978578772705 ) ) ;
#43570=CARTESIAN_POINT ( 'NONE',  ( 123.9800954359119913, 0.5291689781388270175, -13.89700978578772705 ) ) ;
#43587=CARTESIAN_POINT ( 'NONE',  ( 123.7022829359119811, -4.283928203966213211, -7.183505701512925334 ) ) ;
#43602=DIRECTION ( 'NONE',  ( 1.000000000000000000, 0.000000000000000000, 0.000000000000000000 ) ) ;
#43608=( BOUNDED_CURVE ( )  B_SPLINE_CURVE ( 2, ( #16896, #2513, #13473, #44935, #6167, #9594, #16439, #13693, #30561, #27602, #41516, #10272, #6847, #20755, #13247, #26918, #23510 ),
 .UNSPECIFIED., .F., .F. ) 
 B_SPLINE_CURVE_WITH_KNOTS ( ( 3, 2, 2, 2, 2, 2, 2, 2, 3 ),
 ( 0.7589135524044680059, 0.7812500000000000000, 0.8125000000000000000, 0.8437500000000000000, 0.8750000000000000000, 0.9062500000000000000, 0.9375000000000000000, 0.9687500000000000000, 0.9910864475955319941 ),
 .UNSPECIFIED. ) 
 CURVE ( )  GEOMETRIC_REPRESENTATION_ITEM ( )  RATIONAL_B_SPLINE_CURVE ( ( 0.9689618144536780164, 0.9455916533437099813, 1.000000000000000000, 0.9238795325112869605, 1.000000000000000000, 0.9238795325112869605, 1.000000000000000000, 0.9238795325112869605, 1.000000000000000000, 0.9238795325112869605, 1.000000000000000000, 0.9238795325112869605, 1.000000000000000000, 0.9238795325112869605, 1.000000000000000000, 0.9455916533437099813, 0.9689618144536780164 ) ) 
 REPRESENTATION_ITEM ( '' )  );
#43614=CARTESIAN_POINT ( 'NONE',  ( 120.8637602976252055, -8.580000213326620440, -17.71054824844518905 ) ) ;
#43619=ORIENTED_EDGE ( 'NONE', *, *, #23139, .T. ) ;
#43625=CARTESIAN_POINT ( 'NONE',  ( 123.2976082044368127, -6.247802574075781656, -18.73351920797576042 ) ) ;
#43626=CARTESIAN_POINT ( 'NONE',  ( 120.4315948253203032, -6.059724811980584214, -18.37735133589801606 ) ) ;
#43654=CARTESIAN_POINT ( 'NONE',  ( 123.6328298109119714, -7.200787124940443817, -17.81845355600750835 ) ) ;
#43667=CARTESIAN_POINT ( 'NONE',  ( 122.6695390828414105, -8.372502050422333753, -17.31760344562334808 ) ) ;
#43683=ADVANCED_FACE ( 'NONE', ( #4382 ), #24526, .F. ) ;
#43708=B_SPLINE_CURVE_WITH_KNOTS ( 'NONE', 3,
 ( #22288, #28689, #32318, #32973, #12261, #7926, #39620, #8825, #40062, #36182 ),
 .UNSPECIFIED., .F., .F.,
 ( 4, 3, 3, 4 ),
 ( 6.254634441385499976E-18, 0.0002476486541971039844, 0.0004952973025691049819, 0.0009610892161188140746 ),
 .UNSPECIFIED. ) ;
#43712=CARTESIAN_POINT ( 'NONE',  ( 123.2855641859119942, -8.321307733199551748, -9.223433127585318303 ) ) ;
#43716=CARTESIAN_POINT ( 'NONE',  ( 125.3563494635826743, 1.791320624781802318, -11.07214261843091663 ) ) ;
#43727=CARTESIAN_POINT ( 'NONE',  ( 125.2293180859949899, -12.02800175804190630, -14.77921087193282546 ) ) ;
#43749=CARTESIAN_POINT ( 'NONE',  ( 123.7717360609119623, -6.564341423271550902, -7.887810678476487425 ) ) ;
#43750=CARTESIAN_POINT ( 'NONE',  ( 120.6463454359119822, -11.07370829466463569, -12.81314460846529002 ) ) ;
#43772=VERTEX_POINT ( 'NONE', #40054 ) ;
#43782=CARTESIAN_POINT ( 'NONE',  ( 125.2070578882556475, -3.534371629016498151, -20.61203076238330567 ) ) ;
#43785=CARTESIAN_POINT ( 'NONE',  ( 123.8411891859119862, -1.406689858478933353, -17.56299727309130887 ) ) ;
#43801=CARTESIAN_POINT ( 'NONE',  ( 124.1884548109119777, -2.527210466738037731, -8.967976844669125924 ) ) ;
#43821=CARTESIAN_POINT ( 'NONE',  ( 123.0077516859119839, -9.665098340737509730, -17.37397104707595474 ) ) ;
#43825=CARTESIAN_POINT ( 'NONE',  ( 123.2855641859119942, -8.321307733199551748, -9.223433127585318303 ) ) ;
#43859=CARTESIAN_POINT ( 'NONE',  ( 120.6075460087703988, -6.176492496456559955, -18.59847741292036716 ) ) ;
#43865=EDGE_CURVE ( 'NONE', #2517, #17793, #13397, .T. ) ;
#43905=ORIENTED_EDGE ( 'NONE', *, *, #36012, .F. ) ;
#43942=CARTESIAN_POINT ( 'NONE',  ( 121.2019704359119743, -10.25716656981731489, -12.88942061488890545 ) ) ;
#43945=CARTESIAN_POINT ( 'NONE',  ( 122.1048610609119720, -3.163656168406932423, -18.89861972220013797 ) ) ;
#43953=CARTESIAN_POINT ( 'NONE',  ( 124.8099926109736657, -11.79476081310281010, -16.82845685095609412 ) ) ;
#43954=CARTESIAN_POINT ( 'NONE',  ( 123.7749110609119754, -3.388519251034822766, -18.17055338314092694 ) ) ;
#43956=CARTESIAN_POINT ( 'NONE',  ( 119.7434548109119703, -0.02790360340439231729, -15.74607173546667482 ) ) ;
#43957=ORIENTED_EDGE ( 'NONE', *, *, #9156, .T. ) ;
#43975=CARTESIAN_POINT ( 'NONE',  ( 122.1743141859119817, -0.8832429491016019485, -18.19431474523657855 ) ) ;
#43976=CARTESIAN_POINT ( 'NONE',  ( 119.7434548109119703, -7.554583864224885481, -18.48844787311982785 ) ) ;
#44002=CARTESIAN_POINT ( 'NONE',  ( 119.7434548109119703, -2.316996251443989241, -21.63995271010855248 ) ) ;
#44003=CARTESIAN_POINT ( 'NONE',  ( 120.1569985609119726, -9.641336978641936284, -14.86869474514246647 ) ) ;
#44011=CARTESIAN_POINT ( 'NONE',  ( 121.2623705389825233, -6.126425863531494542, -18.50366489541501380 ) ) ;
#44014=CARTESIAN_POINT ( 'NONE',  ( 122.0354079359119908, -4.360204210389833968, -8.000047426360245240 ) ) ;
#44028=DIRECTION ( 'NONE',  ( -1.000000000000000000, 0.000000000000000000, -0.000000000000000000 ) ) ;
#44037=FACE_OUTER_BOUND ( 'NONE', #2279, .T. ) ;
#44052=CARTESIAN_POINT ( 'NONE',  ( 124.1190016859119680, -0.6942167230862511529, -9.935906262978006609 ) ) ;
#44062=EDGE_CURVE ( 'NONE', #2526, #21997, #33527, .T. ) ;
#44066=EDGE_CURVE ( 'NONE', #17949, #32403, #22223, .T. ) ;
#44148=CARTESIAN_POINT ( 'NONE',  ( 120.2542535264548889, -8.247323210606168686, -17.08054893949881148 ) ) ;
#44174=ORIENTED_EDGE ( 'NONE', *, *, #13884, .T. ) ;
#44175=CARTESIAN_POINT ( 'NONE',  ( 122.1048610609119720, -6.340755971794695078, -8.611740276972781771 ) ) ;
#44178=CARTESIAN_POINT ( 'NONE',  ( 119.7434548109119703, -7.411001340234434132, -5.146477690568067587 ) ) ;
#44184=CARTESIAN_POINT ( 'NONE',  ( 121.4103298109119748, -2.173413727453599176, -8.297982527556802879 ) ) ;
#44185=AXIS2_PLACEMENT_3D ( 'NONE', #18702, #2256, #36013 ) ;
#44190=CARTESIAN_POINT ( 'NONE',  ( 119.7434548109119703, 0.3824594525549545043, -13.03383199448628460 ) ) ;
#44207=CARTESIAN_POINT ( 'NONE',  ( 119.7821199480702603, -6.365377317481695663, -18.95617363400926081 ) ) ;
#44209=CARTESIAN_POINT ( 'NONE',  ( 120.9241579359119925, -4.360204210389833968, -8.000047426360245240 ) ) ;
#44210=CARTESIAN_POINT ( 'NONE',  ( 120.1601735609119856, -9.645473719204776586, -14.86997237629376656 ) ) ;
#44233=AXIS2_PLACEMENT_3D ( 'NONE', #17629, #27900, #35378 ) ;
#44245=CARTESIAN_POINT ( 'NONE',  ( 120.2990798109119766, -2.173413727453600508, -8.297982527556802879 ) ) ;
#44281=CARTESIAN_POINT ( 'NONE',  ( 122.9382985609119743, -10.36940331770106916, -15.09355782777062061 ) ) ;
#44285=CARTESIAN_POINT ( 'NONE',  ( 121.7575954359119805, 0.5291689781388270175, -13.89700978578772705 ) ) ;
#44307=CARTESIAN_POINT ( 'NONE',  ( 121.0543159103642239, -8.454079026182057532, -17.47208793939445215 ) ) ;
#44344=CARTESIAN_POINT ( 'NONE',  ( 122.8688454359119646, 0.5291689781388270175, -13.89700978578772705 ) ) ;
#44351=CARTESIAN_POINT ( 'NONE',  ( 124.3521044615884392, -7.410781304726307361, -20.93588303426278685 ) ) ;
#44365=EDGE_CURVE ( 'NONE', #8725, #42142, #8034, .T. ) ;
#44406=CARTESIAN_POINT ( 'NONE',  ( 123.1466579359119891, -4.360204210389825086, -8.000047426360248792 ) ) ;
#44429=CARTESIAN_POINT ( 'NONE',  ( 124.1884548109119777, -7.554583864224885481, -18.48844787311982785 ) ) ;
#44430=CARTESIAN_POINT ( 'NONE',  ( 122.5215798109119874, -7.200787124940443817, -17.81845355600750835 ) ) ;
#44464=CARTESIAN_POINT ( 'NONE',  ( 122.7299391859119737, -1.406689858478933353, -17.56299727309130887 ) ) ;
#44492=CARTESIAN_POINT ( 'NONE',  ( 119.7434548109119703, -3.874292970208447873, -21.33175929725637587 ) ) ;
#44495=CARTESIAN_POINT ( 'NONE',  ( 121.4103298109119748, -2.173413727453600508, -8.297982527556802879 ) ) ;
#44501=CARTESIAN_POINT ( 'NONE',  ( 122.3826735609119680, -9.645473719204776586, -14.86997237629376656 ) ) ;
#44506=ORIENTED_EDGE ( 'NONE', *, *, #40982, .T. ) ;
#44524=CARTESIAN_POINT ( 'NONE',  ( 121.3655035264548872, -8.247323210606168686, -17.08054893949881148 ) ) ;
#44538=FACE_OUTER_BOUND ( 'NONE', #31047, .T. ) ;
#44553=EDGE_CURVE ( 'NONE', #26397, #2604, #19993, .T. ) ;
#44562=EDGE_CURVE ( 'NONE', #25646, #7972, #29747, .T. ) ;
#44567=CARTESIAN_POINT ( 'NONE',  ( 122.4521266859119635, -9.033780868592240054, -16.85052413769862056 ) ) ;
#44571=CARTESIAN_POINT ( 'NONE',  ( 125.3296504289692876, 1.783059037167336491, -10.84170924441004402 ) ) ;
#44602=FACE_OUTER_BOUND ( 'NONE', #41361, .T. ) ;
#44628=CARTESIAN_POINT ( 'NONE',  ( 119.7434548109119703, -6.339884145921025116, -18.90789653539788517 ) ) ;
#44632=CARTESIAN_POINT ( 'NONE',  ( 121.3655035264548872, -8.247323210606168686, -17.08054893949881148 ) ) ;
#44638=CARTESIAN_POINT ( 'NONE',  ( 124.1916298109119765, -2.529232162391345184, -8.971805383623923547 ) ) ;
#44660=CARTESIAN_POINT ( 'NONE',  ( 123.5633766859119760, -9.033780868592240054, -16.85052413769862056 ) ) ;
#44661=CARTESIAN_POINT ( 'NONE',  ( 122.6604860609119640, -3.387241619883791355, -18.17469012370385073 ) ) ;
#44665=ORIENTED_EDGE ( 'NONE', *, *, #17514, .T. ) ;
#44670=DIRECTION ( 'NONE',  ( -1.000000000000000000, 0.000000000000000000, -0.000000000000000000 ) ) ;
#44680=CARTESIAN_POINT ( 'NONE',  ( 120.2296266859119953, -0.06289925094097943703, -9.412459353600674206 ) ) ;
#44693=DIRECTION ( 'NONE',  ( 0.000000000000000000, 0.4669533266896288004, 0.8842819633428518067 ) ) ;
#44696=CARTESIAN_POINT ( 'NONE',  ( 121.2019704359119743, 1.345710702986147034, -13.97328579221134426 ) ) ;
#44733=CARTESIAN_POINT ( 'NONE',  ( 122.5215798109119874, -2.173413727453600508, -8.297982527556802879 ) ) ;
#44768=CARTESIAN_POINT ( 'NONE',  ( 120.2264516859119681, -9.030173340179972641, -16.84753301250217561 ) ) ;
#44788=CARTESIAN_POINT ( 'NONE',  ( 121.2714235609119697, -9.645473719204778362, -14.86997237629376123 ) ) ;
#44793=CARTESIAN_POINT ( 'NONE',  ( 120.0907204359119760, 1.345710702986147034, -13.97328579221134426 ) ) ;
#44803=ORIENTED_EDGE ( 'NONE', *, *, #25820, .T. ) ;
#44823=CARTESIAN_POINT ( 'NONE',  ( 120.0212673109119805, -9.289237151508434209, -11.05642687123711454 ) ) ;
#44853=CARTESIAN_POINT ( 'NONE',  ( 119.7434548109119703, 2.250047331442289966, -9.733932798157443500 ) ) ;
#44880=CARTESIAN_POINT ( 'NONE',  ( 122.1743141859119817, -0.8832429491016019485, -18.19431474523657855 ) ) ;
#44885=CARTESIAN_POINT ( 'NONE',  ( 122.5215798109119874, -7.200787124940443817, -17.81845355600750835 ) ) ;
#44886=CARTESIAN_POINT ( 'NONE',  ( 120.5074391859119913, -1.406689858478933353, -17.56299727309130887 ) ) ;
#44920=CARTESIAN_POINT ( 'NONE',  ( 123.9106423109119675, -9.959231468620755479, -10.70263013195267199 ) ) ;
#44935=CARTESIAN_POINT ( 'NONE',  ( 123.2855641859119800, -0.8832429491016133838, -18.19431474523658565 ) ) ;
#44957=CARTESIAN_POINT ( 'NONE',  ( 123.7717360609119623, -6.564341423271550902, -7.887810678476487425 ) ) ;
#44968=DIRECTION ( 'NONE',  ( 0.000000000000000000, -0.4669533266896290225, -0.8842819633428516957 ) ) ;
#44975=CARTESIAN_POINT ( 'NONE',  ( 125.4584548109119737, -8.702576499751430106, -17.94267422983053706 ) ) ;
#45005=FACE_OUTER_BOUND ( 'NONE', #19644, .T. ) ;
#45017=CARTESIAN_POINT ( 'NONE',  ( 122.7299391859119737, -1.406689858478933353, -17.56299727309130887 ) ) ;
#45020=CARTESIAN_POINT ( 'NONE',  ( 124.9542645564595631, 1.996632241307949140, -10.07212650071240923 ) ) ;
#45043=CARTESIAN_POINT ( 'NONE',  ( 119.9518141859119851, -8.321307733199551748, -9.223433127585318303 ) ) ;
#45054=VERTEX_POINT ( 'NONE', #36445 ) ;
#45069=DIRECTION ( 'NONE',  ( 0.000000000000000000, 0.4669533266896289669, 0.8842819633428518067 ) ) ;
#45094=CARTESIAN_POINT ( 'NONE',  ( 124.3968141859119783, -8.321307733199551748, -9.223433127585318303 ) ) ;
#45107=( NAMED_UNIT ( * ) PLANE_ANGLE_UNIT ( ) SI_UNIT ( $, .RADIAN. ) );
#45108=CARTESIAN_POINT ( 'NONE',  ( 120.2532105243962235, -8.246645307473400521, -17.07926517626395224 ) ) ;
#45116=ORIENTED_EDGE ( 'NONE', *, *, #20330, .T. ) ;
#45136=CARTESIAN_POINT ( 'NONE',  ( 123.2855641859119942, -0.8832429491016019485, -18.19431474523657855 ) ) ;
#45184=COLOUR_RGB('Black',0.12,0.14,0.17);
#45185=FILL_AREA_STYLE_COLOUR('',#45184);
#45186=FILL_AREA_STYLE('',(#45185));
#45187=SURFACE_STYLE_FILL_AREA(#45186);
#45188=SURFACE_SIDE_STYLE('',(#45187));
#45189=SURFACE_STYLE_USAGE(.BOTH.,#45188);
#45190=PRESENTATION_STYLE_ASSIGNMENT((#45189));
ENDSEC;
END-ISO-10303-21;
